ISO-10303-21;
HEADER;
/* Generated by software containing ST-Developer
 * from STEP Tools, Inc. (www.steptools.com) 
 */

FILE_DESCRIPTION(
/* description */ (''),
/* implementation_level */ '2;1');

FILE_NAME(
/* name */ 'Nut_02.step',
/* time_stamp */ '2026-10-04T16:49:01-07:00',
/* author */ (''),
/* organization */ (''),
/* preprocessor_version */ 'ST-DEVELOPER v20.2',
/* originating_system */ 'Autodesk Translation Framework v15.15.0.0',
/* authorisation */ '');

FILE_SCHEMA (('AUTOMOTIVE_DESIGN { 1 0 10303 214 3 1 1 }'));
ENDSEC;

DATA;
#10=MECHANICAL_DESIGN_GEOMETRIC_PRESENTATION_REPRESENTATION('',(#82),#51553);
#58=B_SPLINE_SURFACE_WITH_KNOTS('',3,3,((#27435,#27436,#27437,#27438,#27439,
#27440,#27441,#27442,#27443,#27444,#27445,#27446,#27447,#27448,#27449,#27450,
#27451,#27452,#27453,#27454,#27455,#27456,#27457,#27458,#27459,#27460,#27461,
#27462,#27463,#27464,#27465),(#27466,#27467,#27468,#27469,#27470,#27471,
#27472,#27473,#27474,#27475,#27476,#27477,#27478,#27479,#27480,#27481,#27482,
#27483,#27484,#27485,#27486,#27487,#27488,#27489,#27490,#27491,#27492,#27493,
#27494,#27495,#27496),(#27497,#27498,#27499,#27500,#27501,#27502,#27503,
#27504,#27505,#27506,#27507,#27508,#27509,#27510,#27511,#27512,#27513,#27514,
#27515,#27516,#27517,#27518,#27519,#27520,#27521,#27522,#27523,#27524,#27525,
#27526,#27527),(#27528,#27529,#27530,#27531,#27532,#27533,#27534,#27535,
#27536,#27537,#27538,#27539,#27540,#27541,#27542,#27543,#27544,#27545,#27546,
#27547,#27548,#27549,#27550,#27551,#27552,#27553,#27554,#27555,#27556,#27557,
#27558)),.UNSPECIFIED.,.F.,.F.,.F.,(4,4),(4,1,1,1,1,1,1,1,1,1,1,1,1,1,1,
1,1,1,1,1,1,1,1,1,1,1,1,1,4),(-0.000628230388590609,0.0805634975574235),
(11.8569095924278,12.8271953814412,13.7968529400659,14.7665104986906,15.7361680573154,
16.7058256159401,17.6754831745648,18.6451407331896,19.6147982918143,20.584455850439,
21.5541134090638,22.5237709676885,23.4934285263132,24.4630860849379,25.4327436435627,
26.4024012021874,27.3720587608121,28.3417163194369,29.3113738780616,30.2810314366863,
31.2506889953111,32.2203465539358,33.1900041125605,34.1596616711853,35.12931922981,
36.0989767884347,37.0686343470595,38.0382919056842,39.0079494643089),
 .UNSPECIFIED.);
#59=B_SPLINE_SURFACE_WITH_KNOTS('',3,3,((#27743,#27744,#27745,#27746,#27747,
#27748,#27749,#27750,#27751,#27752,#27753,#27754,#27755,#27756,#27757,#27758,
#27759,#27760,#27761,#27762,#27763,#27764,#27765,#27766,#27767,#27768,#27769,
#27770,#27771,#27772,#27773),(#27774,#27775,#27776,#27777,#27778,#27779,
#27780,#27781,#27782,#27783,#27784,#27785,#27786,#27787,#27788,#27789,#27790,
#27791,#27792,#27793,#27794,#27795,#27796,#27797,#27798,#27799,#27800,#27801,
#27802,#27803,#27804),(#27805,#27806,#27807,#27808,#27809,#27810,#27811,
#27812,#27813,#27814,#27815,#27816,#27817,#27818,#27819,#27820,#27821,#27822,
#27823,#27824,#27825,#27826,#27827,#27828,#27829,#27830,#27831,#27832,#27833,
#27834,#27835),(#27836,#27837,#27838,#27839,#27840,#27841,#27842,#27843,
#27844,#27845,#27846,#27847,#27848,#27849,#27850,#27851,#27852,#27853,#27854,
#27855,#27856,#27857,#27858,#27859,#27860,#27861,#27862,#27863,#27864,#27865,
#27866)),.UNSPECIFIED.,.F.,.F.,.F.,(4,4),(4,1,1,1,1,1,1,1,1,1,1,1,1,1,1,
1,1,1,1,1,1,1,1,1,1,1,1,1,4),(-0.000286423065855878,0.0807675649255769),
(14.3991256467175,15.3687832053423,16.338440763967,17.3080983225917,18.2777558812165,
19.2474134398412,20.2170709984659,21.1867285570907,22.1563861157154,23.1260436743401,
24.0957012329649,25.0653587915896,26.0350163502143,27.0046739088391,27.9743314674638,
28.9439890260885,29.9136465847132,30.883304143338,31.8529617019627,32.8226192605874,
33.7922768192122,34.7619343778369,35.7315919364616,36.7012494950864,37.6709070537111,
38.6405646123358,39.6102221709606,40.5798797295853,41.54953728821),
 .UNSPECIFIED.);
#66=SHAPE_REPRESENTATION_RELATIONSHIP('SRR','None',#51587,#74);
#74=ADVANCED_BREP_SHAPE_REPRESENTATION('',(#91),#51547);
#82=STYLED_ITEM('',(#51634),#91);
#91=MANIFOLD_SOLID_BREP('Body1',#4261);
#104=FACE_BOUND('',#469,.T.);
#105=FACE_BOUND('',#477,.T.);
#139=PLANE('',#4481);
#140=PLANE('',#4482);
#141=PLANE('',#4483);
#142=PLANE('',#4484);
#143=PLANE('',#4485);
#144=PLANE('',#4486);
#145=PLANE('',#4487);
#146=PLANE('',#4488);
#255=FACE_OUTER_BOUND('',#456,.T.);
#256=FACE_OUTER_BOUND('',#457,.T.);
#257=FACE_OUTER_BOUND('',#458,.T.);
#258=FACE_OUTER_BOUND('',#459,.T.);
#259=FACE_OUTER_BOUND('',#460,.T.);
#260=FACE_OUTER_BOUND('',#461,.T.);
#261=FACE_OUTER_BOUND('',#462,.T.);
#262=FACE_OUTER_BOUND('',#463,.T.);
#263=FACE_OUTER_BOUND('',#464,.T.);
#264=FACE_OUTER_BOUND('',#465,.T.);
#265=FACE_OUTER_BOUND('',#466,.T.);
#266=FACE_OUTER_BOUND('',#467,.T.);
#267=FACE_OUTER_BOUND('',#468,.T.);
#268=FACE_OUTER_BOUND('',#470,.T.);
#269=FACE_OUTER_BOUND('',#471,.T.);
#270=FACE_OUTER_BOUND('',#472,.T.);
#271=FACE_OUTER_BOUND('',#473,.T.);
#272=FACE_OUTER_BOUND('',#474,.T.);
#273=FACE_OUTER_BOUND('',#475,.T.);
#274=FACE_OUTER_BOUND('',#476,.T.);
#456=EDGE_LOOP('',(#3139,#3140,#3141,#3142));
#457=EDGE_LOOP('',(#3143,#3144,#3145,#3146,#3147,#3148));
#458=EDGE_LOOP('',(#3149,#3150,#3151,#3152,#3153,#3154));
#459=EDGE_LOOP('',(#3155,#3156,#3157,#3158,#3159,#3160));
#460=EDGE_LOOP('',(#3161,#3162,#3163,#3164,#3165));
#461=EDGE_LOOP('',(#3166,#3167,#3168,#3169,#3170));
#462=EDGE_LOOP('',(#3171,#3172,#3173,#3174,#3175));
#463=EDGE_LOOP('',(#3176,#3177,#3178,#3179,#3180));
#464=EDGE_LOOP('',(#3181,#3182,#3183,#3184));
#465=EDGE_LOOP('',(#3185,#3186,#3187,#3188,#3189,#3190));
#466=EDGE_LOOP('',(#3191,#3192,#3193,#3194,#3195,#3196,#3197,#3198,#3199,
#3200,#3201,#3202,#3203,#3204,#3205,#3206,#3207));
#467=EDGE_LOOP('',(#3208,#3209,#3210,#3211,#3212,#3213,#3214,#3215,#3216,
#3217,#3218,#3219,#3220,#3221,#3222,#3223,#3224,#3225,#3226,#3227));
#468=EDGE_LOOP('',(#3228,#3229,#3230,#3231,#3232,#3233));
#469=EDGE_LOOP('',(#3234,#3235,#3236,#3237));
#470=EDGE_LOOP('',(#3238,#3239,#3240,#3241));
#471=EDGE_LOOP('',(#3242,#3243,#3244,#3245));
#472=EDGE_LOOP('',(#3246,#3247,#3248,#3249));
#473=EDGE_LOOP('',(#3250,#3251,#3252,#3253));
#474=EDGE_LOOP('',(#3254,#3255,#3256,#3257));
#475=EDGE_LOOP('',(#3258,#3259,#3260,#3261));
#476=EDGE_LOOP('',(#3262,#3263,#3264,#3265,#3266,#3267));
#477=EDGE_LOOP('',(#3268,#3269,#3270,#3271,#3272));
#635=CIRCLE('',#4468,4.08499999999996);
#636=CIRCLE('',#4473,3.38975);
#637=CIRCLE('',#4478,3.38975);
#638=CIRCLE('',#4480,4.08499999999996);
#798=LINE('',#25104,#1026);
#799=LINE('',#25120,#1027);
#800=LINE('',#25341,#1028);
#801=LINE('',#25763,#1029);
#802=LINE('',#25836,#1030);
#803=LINE('',#26135,#1031);
#804=LINE('',#26483,#1032);
#805=LINE('',#26838,#1033);
#806=LINE('',#28049,#1034);
#807=LINE('',#28051,#1035);
#808=LINE('',#28053,#1036);
#809=LINE('',#28055,#1037);
#810=LINE('',#28057,#1038);
#811=LINE('',#28058,#1039);
#812=LINE('',#28061,#1040);
#813=LINE('',#28063,#1041);
#814=LINE('',#28064,#1042);
#815=LINE('',#28067,#1043);
#816=LINE('',#28068,#1044);
#817=LINE('',#28071,#1045);
#818=LINE('',#28072,#1046);
#819=LINE('',#28075,#1047);
#820=LINE('',#28076,#1048);
#821=LINE('',#28079,#1049);
#822=LINE('',#28080,#1050);
#823=LINE('',#28082,#1051);
#1026=VECTOR('',#4980,4.08499999999997);
#1027=VECTOR('',#4985,4.08499999999997);
#1028=VECTOR('',#4988,4.08499999999997);
#1029=VECTOR('',#4991,4.08499999999997);
#1030=VECTOR('',#4994,3.38975);
#1031=VECTOR('',#4999,3.38975);
#1032=VECTOR('',#5002,3.38975);
#1033=VECTOR('',#5005,3.38975);
#1034=VECTOR('',#5016,10.);
#1035=VECTOR('',#5017,10.);
#1036=VECTOR('',#5018,10.);
#1037=VECTOR('',#5019,10.);
#1038=VECTOR('',#5020,10.);
#1039=VECTOR('',#5021,10.);
#1040=VECTOR('',#5024,10.);
#1041=VECTOR('',#5025,10.);
#1042=VECTOR('',#5026,10.);
#1043=VECTOR('',#5029,10.);
#1044=VECTOR('',#5030,10.);
#1045=VECTOR('',#5033,10.);
#1046=VECTOR('',#5034,10.);
#1047=VECTOR('',#5037,10.);
#1048=VECTOR('',#5038,10.);
#1049=VECTOR('',#5041,10.);
#1050=VECTOR('',#5042,10.);
#1051=VECTOR('',#5045,10.);
#1293=B_SPLINE_CURVE_WITH_KNOTS('',3,(#25106,#25107,#25108,#25109,#25110),
 .UNSPECIFIED.,.F.,.F.,(4,1,4),(13.8752082355906,14.7665104986906,15.0541924217381),
 .UNSPECIFIED.);
#1294=B_SPLINE_CURVE_WITH_KNOTS('',3,(#25113,#25114,#25115,#25116),
 .UNSPECIFIED.,.F.,.F.,(4,4),(14.3991256467175,15.0523450926205),
 .UNSPECIFIED.);
#1295=B_SPLINE_CURVE_WITH_KNOTS('',3,(#25122,#25123,#25124,#25125,#25126,
#25127,#25128,#25129,#25130,#25131),.UNSPECIFIED.,.F.,.F.,(4,1,1,1,1,1,
1,4),(15.707963267949,15.7361680573154,16.7058256159401,17.6754831745648,
18.6451407331896,19.6147982918143,20.584455850439,21.3359364871903),
 .UNSPECIFIED.);
#1296=B_SPLINE_CURVE_WITH_KNOTS('',3,(#25132,#25133,#25134,#25135),
 .UNSPECIFIED.,.F.,.F.,(4,4),(15.0541924217381,15.707963267949),
 .UNSPECIFIED.);
#1297=B_SPLINE_CURVE_WITH_KNOTS('',3,(#25137,#25138,#25139,#25140,#25141),
 .UNSPECIFIED.,.F.,.F.,(4,1,4),(15.0523450926205,15.3687832053423,15.7079559920353),
 .UNSPECIFIED.);
#1298=B_SPLINE_CURVE_WITH_KNOTS('',3,(#25142,#25143,#25144,#25145,#25146,
#25147,#25148,#25149,#25150,#25151,#25152,#25153,#25154,#25155,#25156,#25157,
#25158,#25159,#25160,#25161,#25162,#25163,#25164,#25165,#25166,#25167,#25168,
#25169,#25170,#25171,#25172,#25173,#25174,#25175,#25176,#25177,#25178,#25179,
#25180,#25181,#25182,#25183,#25184,#25185,#25186,#25187,#25188,#25189,#25190,
#25191,#25192,#25193,#25194,#25195,#25196,#25197,#25198,#25199,#25200,#25201,
#25202,#25203,#25204,#25205,#25206,#25207,#25208,#25209,#25210,#25211,#25212,
#25213,#25214,#25215,#25216,#25217,#25218,#25219,#25220,#25221,#25222,#25223,
#25224,#25225,#25226,#25227,#25228,#25229,#25230,#25231,#25232,#25233,#25234,
#25235,#25236,#25237,#25238,#25239,#25240,#25241,#25242,#25243,#25244,#25245,
#25246,#25247,#25248,#25249,#25250,#25251,#25252,#25253,#25254,#25255,#25256,
#25257,#25258,#25259,#25260,#25261,#25262,#25263,#25264,#25265,#25266,#25267,
#25268,#25269,#25270,#25271,#25272,#25273,#25274,#25275,#25276,#25277,#25278,
#25279,#25280,#25281,#25282,#25283,#25284,#25285,#25286,#25287,#25288,#25289,
#25290,#25291,#25292,#25293,#25294,#25295,#25296,#25297,#25298,#25299,#25300,
#25301,#25302,#25303,#25304,#25305,#25306,#25307,#25308,#25309,#25310,#25311,
#25312,#25313,#25314,#25315,#25316,#25317,#25318,#25319,#25320,#25321,#25322,
#25323,#25324,#25325,#25326,#25327,#25328,#25329,#25330,#25331,#25332,#25333,
#25334,#25335,#25336,#25337),.UNSPECIFIED.,.F.,.F.,(4,3,3,3,3,3,3,3,3,3,
3,3,3,3,3,3,3,3,3,3,3,3,3,3,3,3,3,3,3,3,3,3,3,3,3,3,3,3,3,3,3,3,3,3,3,3,
3,3,3,3,3,3,3,3,3,3,3,3,3,3,3,3,3,3,3,4),(15.707963267949,15.7953191781018,
15.882666103131,15.9700247548158,16.0574158483864,16.1449087968635,16.2324629526336,
16.3201451818259,16.338440763967,16.4265915804881,16.5146360954676,16.6025968319756,
16.6907845183026,16.7786538304492,16.8665116399313,16.9543781872225,17.0428082210648,
17.1307958621293,17.2194470923605,17.3080983225917,17.39627025819,17.4843382017312,
17.5723246356153,17.6605035413154,17.7484039692419,17.8362948905087,17.9241965166447,
18.0125863577876,18.1006136302211,18.1891847557188,18.2777558812165,18.3657091708626,
18.4535548185024,18.5413156253886,18.6295778521952,18.7172460090986,18.804902588628,
18.8925680768335,18.9812794175854,19.0690682889294,19.1582408643853,19.2474134398412,
19.335483835568,19.4234480064783,19.5113285891001,19.5995463902709,19.6873365944086,
19.7751158504035,19.8629045010682,19.9514461254176,20.0393582345022,20.128214616484,
20.2170709984659,20.3051302458619,20.3930833744788,20.480953035497,20.5691749756962,
20.656954632174,20.7447235025596,20.832501943196,20.9210585966697,21.0089610261075,
21.0978447915991,21.1867285570907,21.2735006371787,21.3371564183306),
 .UNSPECIFIED.);
#1299=B_SPLINE_CURVE_WITH_KNOTS('',3,(#25343,#25344,#25345,#25346,#25347,
#25348,#25349,#25350,#25351,#25352,#25353,#25354,#25355,#25356,#25357,#25358,
#25359,#25360,#25361,#25362,#25363,#25364,#25365,#25366,#25367,#25368,#25369,
#25370,#25371,#25372,#25373,#25374,#25375,#25376,#25377,#25378,#25379,#25380,
#25381,#25382,#25383,#25384,#25385,#25386,#25387,#25388,#25389,#25390,#25391,
#25392,#25393,#25394,#25395,#25396,#25397,#25398,#25399,#25400,#25401,#25402,
#25403,#25404,#25405,#25406,#25407,#25408,#25409,#25410,#25411,#25412,#25413,
#25414,#25415,#25416,#25417,#25418,#25419,#25420,#25421,#25422,#25423,#25424,
#25425,#25426,#25427,#25428,#25429,#25430,#25431,#25432,#25433,#25434,#25435,
#25436,#25437,#25438,#25439,#25440,#25441,#25442,#25443,#25444,#25445,#25446,
#25447,#25448,#25449,#25450,#25451,#25452,#25453,#25454,#25455,#25456,#25457,
#25458,#25459,#25460,#25461,#25462,#25463,#25464,#25465,#25466,#25467,#25468,
#25469,#25470,#25471,#25472,#25473,#25474,#25475,#25476,#25477,#25478,#25479,
#25480,#25481,#25482,#25483,#25484,#25485,#25486,#25487,#25488,#25489,#25490,
#25491,#25492,#25493,#25494,#25495,#25496,#25497,#25498,#25499,#25500,#25501,
#25502,#25503,#25504,#25505,#25506,#25507,#25508,#25509,#25510,#25511,#25512,
#25513,#25514,#25515,#25516,#25517,#25518,#25519,#25520,#25521,#25522,#25523,
#25524,#25525,#25526,#25527,#25528,#25529,#25530,#25531,#25532,#25533,#25534,
#25535),.UNSPECIFIED.,.F.,.F.,(4,3,3,3,3,3,3,3,3,3,3,3,3,3,3,3,3,3,3,3,
3,3,3,3,3,3,3,3,3,3,3,3,3,3,3,3,3,3,3,3,3,3,3,3,3,3,3,3,3,3,3,3,3,3,3,3,
3,3,3,3,3,3,3,3,4),(21.9911485751286,22.0812818533853,22.1714775654381,
22.2618222124728,22.3522429655899,22.4428404146287,22.5237709676885,22.6118195054854,
22.6997616830464,22.7876201674516,22.8758462123093,22.9636142132378,23.0513712689732,
23.1391377493465,23.2277104435881,23.3156006621682,23.4045145942407,23.4934285263132,
23.5814764104089,23.6694179282831,23.7572757479402,23.8455020400649,23.9332693683819,
24.0210257498194,24.1087915550198,24.1973651874993,24.285254734994,24.3741704099659,
24.4630860849379,24.5511339011155,24.6390753469046,24.7269330904281,24.8151594095699,
24.902926652306,24.9906829447511,25.0784486576395,25.1670224041203,25.2549118519318,
25.3438277477472,25.4327436435627,25.5207914393718,25.608732868773,25.6965905998733,
25.7848169251625,25.8725841652395,25.9603404587052,26.0481061762938,26.1366799327672,
26.2245693942772,26.3134852982323,26.4024012021874,26.4904491024023,26.5783906332456,
26.6662484627345,26.7544747499942,26.8422420804156,26.9299984610454,27.0177642625259,
27.1063378870974,27.1942274237512,27.2831430922816,27.3720587608121,27.459280535532,
27.5463867365523,27.6203176265813),.UNSPECIFIED.);
#1300=B_SPLINE_CURVE_WITH_KNOTS('',3,(#25536,#25537,#25538,#25539,#25540),
 .UNSPECIFIED.,.F.,.F.,(4,1,4),(21.3359364871903,21.5541134090638,21.9911454985159),
 .UNSPECIFIED.);
#1301=B_SPLINE_CURVE_WITH_KNOTS('',3,(#25542,#25543,#25544,#25545,#25546,
#25547,#25548,#25549,#25550,#25551,#25552,#25553,#25554,#25555,#25556,#25557,
#25558,#25559,#25560,#25561,#25562,#25563,#25564,#25565,#25566),
 .UNSPECIFIED.,.F.,.F.,(4,3,3,3,3,3,3,3,4),(21.3371564183306,21.4237674913069,
21.5103226356218,21.59684350434,21.6833517173297,21.7699037254338,21.8564793827075,
21.9431463484601,21.9911485750058),.UNSPECIFIED.);
#1302=B_SPLINE_CURVE_WITH_KNOTS('',3,(#25567,#25568,#25569,#25570,#25571,
#25572,#25573,#25574,#25575,#25576,#25577,#25578,#25579,#25580,#25581,#25582,
#25583,#25584,#25585,#25586,#25587,#25588,#25589,#25590,#25591,#25592,#25593,
#25594,#25595,#25596,#25597,#25598,#25599,#25600,#25601,#25602,#25603,#25604,
#25605,#25606,#25607,#25608,#25609,#25610,#25611,#25612,#25613,#25614,#25615,
#25616,#25617,#25618,#25619,#25620,#25621,#25622,#25623,#25624,#25625,#25626,
#25627,#25628,#25629,#25630,#25631,#25632,#25633,#25634,#25635,#25636,#25637,
#25638,#25639,#25640,#25641,#25642,#25643,#25644,#25645,#25646,#25647,#25648,
#25649,#25650,#25651,#25652,#25653,#25654,#25655,#25656,#25657,#25658,#25659,
#25660,#25661,#25662,#25663,#25664,#25665,#25666,#25667,#25668,#25669,#25670,
#25671,#25672,#25673,#25674,#25675,#25676,#25677,#25678,#25679,#25680,#25681,
#25682,#25683,#25684,#25685,#25686,#25687,#25688,#25689,#25690,#25691,#25692,
#25693,#25694,#25695,#25696,#25697,#25698,#25699,#25700,#25701,#25702,#25703,
#25704,#25705,#25706,#25707,#25708,#25709,#25710,#25711,#25712,#25713,#25714,
#25715,#25716,#25717,#25718,#25719,#25720,#25721,#25722,#25723,#25724,#25725,
#25726,#25727,#25728,#25729,#25730,#25731,#25732,#25733,#25734,#25735,#25736,
#25737,#25738,#25739,#25740,#25741,#25742,#25743,#25744,#25745,#25746,#25747,
#25748,#25749,#25750,#25751,#25752,#25753,#25754,#25755,#25756,#25757,#25758,
#25759),.UNSPECIFIED.,.F.,.F.,(4,3,3,3,3,3,3,3,3,3,3,3,3,3,3,3,3,3,3,3,
3,3,3,3,3,3,3,3,3,3,3,3,3,3,3,3,3,3,3,3,3,3,3,3,3,3,3,3,3,3,3,3,3,3,3,3,
3,3,3,3,3,3,3,3,4),(21.9911485751286,22.1228194350913,22.1563861157154,
22.2444380999692,22.3323837550216,22.4202457430996,22.5084704845047,22.59624202941,
22.6840026375976,22.7717726746395,22.8603404245647,22.948234177373,23.0371389258566,
23.1260436743401,23.214092344832,23.3020346710917,23.3898933199334,23.4781193090624,
23.5658875121345,23.6536447839157,23.7414114940515,23.8299839287799,23.9178744090476,
24.0067878210062,24.0957012329649,24.1837476390331,24.2716876540278,24.3595439480956,
24.4477708035323,24.5355365607886,24.623291356946,24.7110555644892,24.7996313712643,
24.887519305156,24.9764390483728,25.0653587915896,25.1534073144324,25.241349476856,
25.3292079459619,25.4174339964934,25.5052019818284,25.5929590218885,25.6807254865233,
25.7692982024461,25.8571884052756,25.946102377745,26.0350163502143,26.1230642365196,
26.2110057565983,26.2988635784517,26.3870898697501,26.4748572002282,26.5626135838093,
26.650379391133,26.7389530205595,26.826842570107,26.9157582394731,27.0046739088391,
27.0927089175608,27.1806439750418,27.2684996153284,27.3562982655407,27.4440610465582,
27.531833492624,27.6195744277319),.UNSPECIFIED.);
#1303=B_SPLINE_CURVE_WITH_KNOTS('',3,(#25765,#25766,#25767,#25768,#25769,
#25770,#25771,#25772,#25773,#25774),.UNSPECIFIED.,.F.,.F.,(4,1,1,1,1,1,
1,4),(28.2743338823081,28.3417163194369,29.3113738780616,30.2810314366863,
31.2506889953111,32.2203465539358,33.1900041125605,33.9023219446702),
 .UNSPECIFIED.);
#1304=B_SPLINE_CURVE_WITH_KNOTS('',3,(#25775,#25776,#25777,#25778,#25779,
#25780,#25781,#25782,#25783,#25784,#25785,#25786,#25787,#25788,#25789,#25790,
#25791,#25792,#25793,#25794,#25795,#25796,#25797,#25798,#25799),
 .UNSPECIFIED.,.F.,.F.,(4,3,3,3,3,3,3,3,4),(27.6203176265813,27.7073051292124,
27.794260804199,27.8812059046581,27.9681616709394,28.055194626814,28.1422707001016,
28.2294648389027,28.2743338823081),.UNSPECIFIED.);
#1305=B_SPLINE_CURVE_WITH_KNOTS('',3,(#25801,#25802,#25803,#25804,#25805,
#25806,#25807,#25808,#25809,#25810,#25811,#25812,#25813,#25814,#25815,#25816,
#25817,#25818,#25819,#25820,#25821,#25822),.UNSPECIFIED.,.F.,.F.,(4,3,3,
3,3,3,3,4),(27.6195744277319,27.7082636876649,27.7961529417002,27.885242204582,
27.9743314674638,28.0790230082866,28.1827301957677,28.2743337273969),
 .UNSPECIFIED.);
#1306=B_SPLINE_CURVE_WITH_KNOTS('',3,(#25823,#25824,#25825,#25826,#25827,
#25828,#25829,#25830,#25831,#25832),.UNSPECIFIED.,.F.,.F.,(4,1,1,1,1,1,
1,4),(28.2743338823081,28.9439890260885,29.9136465847132,30.883304143338,
31.8529617019627,32.8226192605874,33.7922768192122,33.9036448620551),
 .UNSPECIFIED.);
#1307=B_SPLINE_CURVE_WITH_KNOTS('',3,(#25838,#25839,#25840,#25841,#25842,
#25843,#25844,#25845,#25846,#25847,#25848,#25849,#25850),.UNSPECIFIED.,
 .F.,.F.,(4,3,3,3,4),(7.592022928411,7.72998057268366,7.75726046899785,
7.85218978178926,7.94711909458068),.UNSPECIFIED.);
#1308=B_SPLINE_CURVE_WITH_KNOTS('',3,(#25852,#25853,#25854,#25855,#25856,
#25857,#25858,#25859,#25860,#25861,#25862,#25863,#25864,#25865,#25866,#25867,
#25868,#25869,#25870,#25871,#25872,#25873,#25874,#25875,#25876,#25877,#25878,
#25879,#25880,#25881,#25882,#25883,#25884,#25885,#25886,#25887,#25888,#25889,
#25890,#25891,#25892,#25893,#25894,#25895,#25896,#25897,#25898,#25899,#25900,
#25901,#25902,#25903,#25904,#25905,#25906,#25907,#25908,#25909,#25910,#25911,
#25912,#25913,#25914,#25915,#25916,#25917,#25918,#25919,#25920,#25921,#25922,
#25923,#25924,#25925,#25926,#25927,#25928,#25929,#25930,#25931,#25932,#25933,
#25934,#25935,#25936,#25937,#25938,#25939,#25940,#25941,#25942,#25943,#25944,
#25945,#25946,#25947,#25948,#25949,#25950,#25951,#25952,#25953,#25954,#25955,
#25956,#25957,#25958,#25959,#25960,#25961,#25962,#25963,#25964,#25965,#25966,
#25967,#25968,#25969,#25970,#25971,#25972,#25973,#25974,#25975,#25976,#25977,
#25978,#25979,#25980,#25981,#25982,#25983,#25984,#25985,#25986,#25987,#25988,
#25989,#25990,#25991,#25992,#25993,#25994,#25995,#25996,#25997,#25998,#25999,
#26000,#26001,#26002,#26003,#26004,#26005,#26006,#26007,#26008,#26009,#26010,
#26011,#26012,#26013,#26014,#26015,#26016,#26017,#26018,#26019,#26020,#26021,
#26022,#26023,#26024,#26025,#26026,#26027,#26028,#26029,#26030,#26031,#26032,
#26033,#26034,#26035,#26036,#26037,#26038,#26039,#26040,#26041),
 .UNSPECIFIED.,.F.,.F.,(4,3,3,3,3,3,3,3,3,3,3,3,3,3,3,3,3,3,3,3,3,3,3,3,
3,3,3,3,3,3,3,3,3,3,3,3,3,3,3,3,3,3,3,3,3,3,3,3,3,3,3,3,3,3,3,3,3,3,3,3,
3,3,3,4),(2.0176935435318,2.10900613700961,2.20020948780471,2.29132757712989,
2.38239979845583,2.47345065763357,2.56450463665772,2.65563952109678,2.7468159737042,
2.83813121660439,2.90897267587419,3.00135448708213,3.09362272558863,3.18580324790417,
3.27792608126715,3.3700199280202,3.46210804549375,3.55421368001692,3.6464128429923,
3.73866410476864,3.8310522924152,3.87863023449892,3.97078296023955,4.06281811462994,
4.15476192079865,4.24664363672281,4.33849375932083,4.43033586316209,4.52219351001169,
4.61414316369226,4.70614373799067,4.79828172793459,4.84828779312365,4.94056321631626,
5.03272261966758,5.12479203689778,5.21680086059312,5.308778956382,5.40074973362021,
5.49273658940472,5.58481549634695,5.67694551413242,5.76921203980279,5.81794535174838,
5.91020909431947,6.00235693384428,6.09441492089814,6.18641256521841,6.27837964339645,
6.37033958024058,6.46231578844065,6.55438440757534,6.64650432910375,6.73876115358093,
6.78760291037311,6.8785392358345,6.96933903752258,7.06006166276081,7.1507320536416,
7.24137509809403,7.33205488312372,7.42275060426606,7.51354992827336,7.5920229281199),
 .UNSPECIFIED.);
#1309=B_SPLINE_CURVE_WITH_KNOTS('',3,(#26044,#26045,#26046,#26047,#26048,
#26049,#26050,#26051,#26052,#26053,#26054,#26055,#26056,#26057,#26058,#26059,
#26060,#26061,#26062,#26063,#26064,#26065,#26066,#26067,#26068,#26069,#26070,
#26071,#26072,#26073,#26074,#26075,#26076,#26077,#26078,#26079,#26080,#26081,
#26082,#26083,#26084,#26085,#26086,#26087,#26088,#26089,#26090,#26091,#26092,
#26093,#26094,#26095,#26096,#26097,#26098,#26099,#26100,#26101,#26102,#26103,
#26104,#26105,#26106,#26107,#26108,#26109,#26110,#26111,#26112,#26113,#26114,
#26115,#26116,#26117,#26118,#26119,#26120,#26121,#26122,#26123,#26124,#26125,
#26126,#26127,#26128,#26129,#26130,#26131),.UNSPECIFIED.,.F.,.F.,(4,2,2,
2,2,2,2,2,2,2,2,2,2,2,2,2,2,2,2,2,2,2,2,2,2,2,2,2,2,2,2,2,2,2,2,2,2,2,2,
2,2,2,2,4),(0.000213322277777609,0.0081712364937981,0.0180651814832395,
0.0898839906907267,0.131793832432466,0.155491307257063,0.181103288449151,
0.27540615577459,0.312356721458623,0.326548888301831,0.33877329588411,0.36164707735747,
0.421445917416244,0.453614416798198,0.48020288102199,0.50005478394176,0.523917830127524,
0.60111797580595,0.630853315953084,0.651562322220697,0.663443723530535,
0.678063909123624,0.717907332690356,0.771430698552995,0.807243642528013,
0.829055144438564,0.852189025253953,0.904418311791255,0.964484903374977,
0.982393494675465,0.994646271915792,1.01304652705384,1.08900583967967,1.13006385373997,
1.15222227131495,1.17427647889075,1.21412238852217,1.27425770059287,1.29572128492808,
1.31261454987213,1.32461516809104,1.34294772153475,1.41903836990406,1.42895520339045),
 .UNSPECIFIED.);
#1310=B_SPLINE_CURVE_WITH_KNOTS('',3,(#26137,#26138,#26139,#26140,#26141,
#26142,#26143,#26144,#26145,#26146,#26147,#26148,#26149),.UNSPECIFIED.,
 .F.,.F.,(4,3,3,3,4),(13.8752082355906,13.9667885610938,14.0583377787896,
14.1499114854528,14.2294808573324),.UNSPECIFIED.);
#1311=B_SPLINE_CURVE_WITH_KNOTS('',3,(#26150,#26151,#26152,#26153,#26154,
#26155,#26156,#26157,#26158,#26159,#26160,#26161,#26162,#26163,#26164,#26165,
#26166,#26167,#26168,#26169,#26170,#26171,#26172,#26173,#26174,#26175,#26176,
#26177,#26178,#26179,#26180,#26181,#26182,#26183,#26184,#26185,#26186,#26187,
#26188,#26189,#26190,#26191,#26192,#26193,#26194,#26195,#26196,#26197,#26198,
#26199,#26200,#26201,#26202,#26203,#26204,#26205,#26206,#26207,#26208,#26209,
#26210,#26211,#26212,#26213,#26214,#26215,#26216,#26217,#26218,#26219,#26220,
#26221,#26222,#26223,#26224,#26225,#26226,#26227,#26228,#26229,#26230,#26231,
#26232,#26233,#26234,#26235,#26236,#26237,#26238,#26239,#26240,#26241,#26242,
#26243,#26244,#26245,#26246,#26247,#26248,#26249,#26250,#26251,#26252,#26253,
#26254,#26255,#26256,#26257,#26258,#26259,#26260,#26261,#26262,#26263,#26264,
#26265,#26266,#26267,#26268,#26269,#26270,#26271,#26272,#26273,#26274,#26275,
#26276,#26277,#26278,#26279,#26280,#26281,#26282,#26283,#26284,#26285,#26286,
#26287,#26288,#26289,#26290,#26291,#26292,#26293,#26294,#26295,#26296,#26297,
#26298,#26299,#26300,#26301,#26302,#26303,#26304,#26305,#26306,#26307,#26308,
#26309,#26310,#26311,#26312,#26313,#26314,#26315,#26316,#26317,#26318,#26319,
#26320,#26321,#26322,#26323,#26324,#26325,#26326,#26327,#26328,#26329,#26330,
#26331,#26332,#26333,#26334,#26335,#26336,#26337,#26338,#26339,#26340,#26341,
#26342,#26343,#26344,#26345,#26346,#26347,#26348,#26349,#26350,#26351),
 .UNSPECIFIED.,.F.,.F.,(4,3,3,3,3,3,3,3,3,3,3,3,3,3,3,3,3,3,3,3,3,3,3,3,
3,3,3,3,3,3,3,3,3,3,3,3,3,3,3,3,3,3,3,3,3,3,3,3,3,3,3,3,3,3,3,3,3,3,3,3,
3,3,3,3,3,3,3,4),(7.94711909458068,8.03916449689059,8.13115131314578,8.22310877742044,
8.31506032401175,8.40702937604215,8.49909140929719,8.59120587840926,8.68345569404661,
8.72691802762258,8.8191706882828,8.9113071987979,9.00335362771794,9.09533942116433,
9.18729447283689,9.2792422229474,9.37120609946293,9.46326223939332,9.55536958219376,
9.6476137888841,9.69657558624731,9.78882587436606,9.8809599610036,9.97300391854113,
10.0649871802198,10.1569396639359,10.2488848131877,10.3408460592029,10.4328995391064,
10.5250042017507,10.6172457216456,10.666233144872,10.7584856508334,10.8506219888867,
10.9426682279119,11.0346538061488,11.1266086269975,11.2185561309138,11.3105197460972,
11.402575603076,11.4946826502856,11.5869265442726,11.6358907034968,11.7281425425284,
11.8202782073,11.9123237677263,12.0043086623816,12.0962627969125,12.1882096126845,
12.2801725388051,12.3722277094847,12.4643340711003,12.5565772870035,12.6055482621215,
12.6978000285144,12.7899356161397,12.8819810950496,12.9739659020025,13.0659199450359,
13.1578666656258,13.2498294929868,13.3418845600313,13.4339908151117,13.5262339209227,
13.5752058207462,13.6848959854304,13.7935319587344,13.8752082353429),
 .UNSPECIFIED.);
#1312=B_SPLINE_CURVE_WITH_KNOTS('',3,(#26352,#26353,#26354,#26355,#26356,
#26357,#26358,#26359,#26360,#26361,#26362,#26363,#26364,#26365,#26366,#26367,
#26368,#26369,#26370,#26371,#26372,#26373,#26374,#26375,#26376,#26377,#26378,
#26379,#26380,#26381,#26382,#26383,#26384,#26385,#26386,#26387,#26388,#26389,
#26390,#26391,#26392,#26393,#26394,#26395,#26396,#26397,#26398,#26399,#26400,
#26401,#26402,#26403,#26404,#26405,#26406,#26407,#26408,#26409,#26410,#26411,
#26412,#26413,#26414,#26415,#26416,#26417,#26418,#26419,#26420,#26421,#26422,
#26423,#26424,#26425,#26426,#26427,#26428,#26429,#26430,#26431,#26432,#26433,
#26434,#26435,#26436,#26437,#26438,#26439,#26440,#26441,#26442,#26443,#26444,
#26445,#26446,#26447,#26448,#26449,#26450,#26451,#26452,#26453,#26454,#26455,
#26456,#26457,#26458,#26459,#26460,#26461,#26462,#26463,#26464,#26465,#26466,
#26467,#26468,#26469,#26470,#26471,#26472,#26473,#26474,#26475,#26476,#26477,
#26478,#26479),.UNSPECIFIED.,.F.,.F.,(4,2,2,2,2,2,2,2,2,2,2,2,2,2,2,2,2,
2,2,2,2,2,2,2,2,2,2,2,2,2,2,2,2,2,2,2,2,2,2,2,2,2,2,2,2,2,2,2,2,2,2,2,2,
2,2,2,2,2,2,2,2,2,2,4),(1.42895520339045,1.46007496358097,1.48208211995382,
1.50383525497819,1.54229239714939,1.61367123091507,1.63723341041766,1.64972479841955,
1.66413554710266,1.70913175895384,1.75932713685332,1.7938919452629,1.81535639125292,
1.83827099184157,1.92496622075754,1.96180891024268,1.97578576406935,1.98865268163704,
2.01479493650323,2.09654907503768,2.12672628323235,2.14771017773909,2.17188820208918,
2.24835130633677,2.27743430706929,2.29799339774998,2.3101772215098,2.32575431093369,
2.40561867459191,2.448146251685,2.4703723153293,2.49216294186807,2.53023103464384,
2.60191563565894,2.62554538117764,2.63808055811796,2.65254485963469,2.69164913274144,
2.75066083212034,2.78343334713444,2.80467240406175,2.82794644366014,2.90446187422405,
2.93517090993916,2.95642742460775,2.96869014449942,2.98398316625685,3.04122032585058,
3.08279506652258,3.11408919989558,3.13517077037761,3.15889354399749,3.23899869863535,
3.26679837079315,3.28678320333307,3.29891650195166,3.31451643957388,3.3588094988828,
3.40732399911904,3.44127988580007,3.4626370436004,3.4855939743301,3.53754491533665,
3.56373237072242),.UNSPECIFIED.);
#1313=B_SPLINE_CURVE_WITH_KNOTS('',3,(#26485,#26486,#26487,#26488,#26489,
#26490,#26491,#26492,#26493,#26494,#26495,#26496,#26497),.UNSPECIFIED.,
 .F.,.F.,(4,3,3,3,4),(20.1583935427702,20.2835108838085,20.3628087311194,
20.4550618538465,20.5134609524394),.UNSPECIFIED.);
#1314=B_SPLINE_CURVE_WITH_KNOTS('',3,(#26498,#26499,#26500,#26501,#26502,
#26503,#26504,#26505,#26506,#26507,#26508,#26509,#26510,#26511,#26512,#26513,
#26514,#26515,#26516,#26517,#26518,#26519,#26520,#26521,#26522,#26523,#26524,
#26525,#26526,#26527,#26528,#26529,#26530,#26531,#26532,#26533,#26534,#26535,
#26536,#26537,#26538,#26539,#26540,#26541,#26542,#26543,#26544,#26545,#26546,
#26547,#26548,#26549,#26550,#26551,#26552,#26553,#26554,#26555,#26556,#26557,
#26558,#26559,#26560,#26561,#26562,#26563,#26564,#26565,#26566,#26567,#26568,
#26569,#26570,#26571,#26572,#26573,#26574,#26575,#26576,#26577,#26578,#26579,
#26580,#26581,#26582,#26583,#26584,#26585,#26586,#26587,#26588,#26589,#26590,
#26591,#26592,#26593,#26594,#26595,#26596,#26597,#26598,#26599,#26600,#26601,
#26602,#26603,#26604,#26605,#26606,#26607,#26608,#26609,#26610,#26611,#26612,
#26613,#26614,#26615,#26616,#26617,#26618,#26619,#26620,#26621,#26622,#26623,
#26624,#26625,#26626,#26627,#26628,#26629,#26630,#26631,#26632,#26633,#26634,
#26635,#26636,#26637,#26638,#26639,#26640,#26641,#26642,#26643,#26644,#26645,
#26646,#26647,#26648,#26649,#26650,#26651,#26652,#26653,#26654,#26655,#26656,
#26657,#26658,#26659,#26660,#26661,#26662,#26663,#26664,#26665,#26666,#26667,
#26668,#26669,#26670,#26671,#26672,#26673,#26674,#26675,#26676,#26677,#26678,
#26679,#26680,#26681,#26682,#26683,#26684,#26685,#26686,#26687,#26688,#26689,
#26690,#26691,#26692,#26693,#26694,#26695,#26696,#26697,#26698,#26699,#26700,
#26701,#26702),.UNSPECIFIED.,.F.,.F.,(4,3,3,3,3,3,3,3,3,3,3,3,3,3,3,3,3,
3,3,3,3,3,3,3,3,3,3,3,3,3,3,3,3,3,3,3,3,3,3,3,3,3,3,3,3,3,3,3,3,3,3,3,3,
3,3,3,3,3,3,3,3,3,3,3,3,3,3,3,4),(14.2294808573324,14.3211458580209,14.4128655316526,
14.5047229612972,14.544863379371,14.6371152350521,14.7292509130644,14.8212964833362,
14.9132813827541,15.0052355188961,15.0971823331305,15.1891452545648,15.2812004158074,
15.3733067652785,15.4655499649325,15.5145209379957,15.6067734688626,15.6989098267224,
15.790956080476,15.882941665837,15.9748964890955,16.0668439907115,16.1588075988842,
16.2508634417462,16.3429704707886,16.4352143404685,16.4841784966204,16.5764286618195,
16.6685626507028,16.7606065355495,16.8525897620659,16.9445422338854,17.0364873944877,
17.1284486751,17.2205022246723,17.3126069769739,17.4048486168314,17.4538360552452,
17.5460888997187,17.6382255564142,17.7302720940337,17.8222579400587,17.9142130095176,
18.0061607426501,18.0981245674236,18.1901806031659,18.282287811887,18.3745318391812,
18.4234936138699,18.515749813376,18.6078898654283,18.6999398333559,18.7919291466729,
18.8838877045188,18.9758389424325,19.0678062836941,19.1598658322997,19.2519765562282,
19.3442240693714,19.3931511724946,19.4888064687512,19.579682221144,19.6704808514327,
19.761227231578,19.8519461796405,19.9426928355591,20.0334557138223,20.1242985696788,
20.1583935425473),.UNSPECIFIED.);
#1315=B_SPLINE_CURVE_WITH_KNOTS('',3,(#26703,#26704,#26705,#26706,#26707,
#26708,#26709,#26710,#26711,#26712,#26713,#26714,#26715,#26716,#26717,#26718,
#26719,#26720,#26721,#26722,#26723,#26724,#26725,#26726,#26727,#26728,#26729,
#26730,#26731,#26732,#26733,#26734,#26735,#26736,#26737,#26738,#26739,#26740,
#26741,#26742,#26743,#26744,#26745,#26746,#26747,#26748,#26749,#26750,#26751,
#26752,#26753,#26754,#26755,#26756,#26757,#26758,#26759,#26760,#26761,#26762,
#26763,#26764,#26765,#26766,#26767,#26768,#26769,#26770,#26771,#26772,#26773,
#26774,#26775,#26776,#26777,#26778,#26779,#26780,#26781,#26782,#26783,#26784,
#26785,#26786,#26787,#26788,#26789,#26790,#26791,#26792,#26793,#26794,#26795,
#26796,#26797,#26798,#26799,#26800,#26801,#26802,#26803,#26804,#26805,#26806,
#26807,#26808,#26809,#26810,#26811,#26812,#26813,#26814,#26815,#26816,#26817,
#26818,#26819,#26820,#26821,#26822,#26823,#26824,#26825,#26826,#26827,#26828,
#26829,#26830,#26831,#26832,#26833,#26834),.UNSPECIFIED.,.F.,.F.,(4,2,2,
2,2,2,2,2,2,2,2,2,2,2,2,2,2,2,2,2,2,2,2,2,2,2,2,2,2,2,2,2,2,2,2,2,2,2,2,
2,2,2,2,2,2,2,2,2,2,2,2,2,2,2,2,2,2,2,2,2,2,2,2,2,2,4),(3.56373237072242,
3.58500893758219,3.61205525450633,3.62502163344836,3.63875725526822,3.66736872694212,
3.72979858715719,3.75742179782564,3.78196586164726,3.80287856553384,3.83225892708286,
3.90236218915142,3.93857485611522,3.95248185392889,3.96373358626966,3.98677654560246,
4.05658521376898,4.09642272798821,4.11840293043193,4.14044784784961,4.18093262120689,
4.23986264155682,4.26974413711665,4.28304819816273,4.29639233501895,4.32663110267408,
4.38726137784765,4.42625069116603,4.44814569393084,4.47028287207744,4.51172757481414,
4.58971329466417,4.60689960761048,4.61892315991081,4.63704975968857,4.70023433345295,
4.75121650123014,4.77412816144496,4.79551264190333,4.82969079281924,4.87882904963454,
4.92211336059089,4.93775152690358,4.94988200866164,4.96980755625938,4.99747302872111,
5.08099981152042,5.10383064968515,5.12525530834568,5.15980585491857,5.21002914245259,
5.25492534924277,5.2693475545555,5.28191143053491,5.30572909525281,5.37862579493191,
5.4157033627135,5.43740185377705,5.45979205044023,5.50404447853088,5.56445557350166,
5.58926589947181,5.60205980227513,5.61605368880105,5.65343827770255,5.69838345838743),
 .UNSPECIFIED.);
#1316=B_SPLINE_CURVE_WITH_KNOTS('',3,(#26840,#26841,#26842,#26843,#26844,
#26845,#26846,#26847,#26848,#26849,#26850,#26851),.UNSPECIFIED.,.F.,.F.,
(4,2,2,2,2,4),(-0.241179247961179,-0.205768877166292,-0.169865978853117,
-0.146695594041589,-0.120665889329961,-0.120342605042655),.UNSPECIFIED.);
#1317=B_SPLINE_CURVE_WITH_KNOTS('',3,(#26852,#26853,#26854,#26855,#26856,
#26857,#26858,#26859,#26860,#26861,#26862,#26863,#26864,#26865,#26866,#26867,
#26868,#26869,#26870,#26871,#26872,#26873,#26874,#26875,#26876,#26877,#26878,
#26879,#26880,#26881,#26882,#26883,#26884,#26885,#26886,#26887,#26888,#26889,
#26890,#26891,#26892,#26893,#26894,#26895,#26896,#26897,#26898,#26899,#26900,
#26901,#26902,#26903,#26904,#26905,#26906,#26907,#26908,#26909,#26910,#26911,
#26912,#26913,#26914,#26915,#26916,#26917,#26918,#26919,#26920,#26921,#26922,
#26923,#26924,#26925,#26926,#26927,#26928,#26929,#26930,#26931,#26932,#26933,
#26934,#26935,#26936,#26937,#26938,#26939,#26940,#26941,#26942,#26943,#26944,
#26945,#26946,#26947,#26948,#26949,#26950,#26951,#26952,#26953,#26954,#26955,
#26956,#26957,#26958,#26959,#26960,#26961,#26962,#26963,#26964,#26965,#26966,
#26967,#26968,#26969,#26970,#26971,#26972,#26973,#26974,#26975,#26976,#26977,
#26978,#26979,#26980,#26981,#26982,#26983,#26984,#26985,#26986,#26987,#26988,
#26989,#26990,#26991,#26992,#26993,#26994,#26995,#26996,#26997,#26998,#26999,
#27000,#27001,#27002,#27003,#27004,#27005,#27006,#27007,#27008,#27009,#27010,
#27011,#27012,#27013,#27014,#27015,#27016,#27017,#27018,#27019,#27020,#27021,
#27022,#27023,#27024,#27025,#27026,#27027,#27028,#27029,#27030,#27031,#27032,
#27033,#27034,#27035,#27036,#27037,#27038,#27039,#27040,#27041,#27042,#27043,
#27044,#27045,#27046,#27047,#27048,#27049,#27050,#27051,#27052,#27053),
 .UNSPECIFIED.,.F.,.F.,(4,3,3,3,3,3,3,3,3,3,3,3,3,3,3,3,3,3,3,3,3,3,3,3,
3,3,3,3,3,3,3,3,3,3,3,3,3,3,3,3,3,3,3,3,3,3,3,3,3,3,3,3,3,3,3,3,3,3,3,3,
3,3,3,3,3,3,3,4),(20.5134609524394,20.6055499763409,20.6975652948072,20.7895411354812,
20.8815009324973,20.9734681009837,21.0655223439608,21.1576198991999,21.2498633183681,
21.3324662897441,21.4247413460989,21.5169004577346,21.6089696580682,21.7009783768828,
21.7929564372439,21.8849272484514,21.976914207601,22.0689933225765,22.1611236080645,
22.2533904918466,22.3021238483688,22.3942708610428,22.486301470765,22.5782418959037,
22.6701219740309,22.7619715389531,22.8538141643628,22.9456734120041,23.0376262965107,
23.1296310296129,23.2217745889557,23.2717814069936,23.3641777908133,23.4564576141058,
23.5486467453446,23.6407737348538,23.7328689752169,23.8249557259828,23.9170572335176,
24.0092481114704,24.1014887148543,24.1938626585338,24.2414389656183,24.3337905638608,
24.4260277122443,24.5181763073473,24.6102660719698,24.7023261537227,24.7943798433827,
24.8864504202011,24.9786137485308,25.0708286878585,25.1631801049782,25.211096524243,
25.3024910772515,25.3937689813926,25.4849573994033,25.5760894638707,25.6671936952272,
25.7582945058579,25.8494162995359,25.9406426849034,26.0319260146508,26.123363113343,
26.1807540828677,26.304510185502,26.4254147545538,26.4415719136207),
 .UNSPECIFIED.);
#1318=B_SPLINE_CURVE_WITH_KNOTS('',3,(#27054,#27055,#27056,#27057,#27058,
#27059,#27060,#27061,#27062,#27063,#27064,#27065,#27066,#27067,#27068,#27069,
#27070,#27071,#27072,#27073,#27074,#27075,#27076,#27077,#27078,#27079,#27080,
#27081,#27082,#27083,#27084,#27085,#27086,#27087,#27088,#27089,#27090,#27091,
#27092,#27093,#27094,#27095,#27096,#27097,#27098,#27099,#27100,#27101,#27102,
#27103,#27104,#27105,#27106,#27107,#27108,#27109,#27110,#27111,#27112,#27113,
#27114,#27115,#27116,#27117,#27118,#27119,#27120,#27121,#27122,#27123,#27124,
#27125,#27126,#27127,#27128,#27129,#27130,#27131,#27132,#27133,#27134,#27135,
#27136,#27137,#27138,#27139,#27140,#27141,#27142,#27143,#27144,#27145,#27146,
#27147,#27148,#27149,#27150,#27151,#27152,#27153,#27154,#27155,#27156,#27157,
#27158,#27159,#27160,#27161,#27162,#27163,#27164,#27165,#27166,#27167,#27168,
#27169,#27170,#27171,#27172,#27173,#27174,#27175,#27176,#27177,#27178,#27179,
#27180,#27181,#27182,#27183),.UNSPECIFIED.,.F.,.F.,(4,2,2,2,2,2,2,2,2,2,
2,2,2,2,2,2,2,2,2,2,2,2,2,2,2,2,2,2,2,2,2,2,2,2,2,2,2,2,2,2,2,2,2,2,2,2,
2,2,2,2,2,2,2,2,2,2,2,2,2,2,2,2,2,2,4),(5.69838345838743,5.74060319572305,
5.7632661986444,5.78477844420156,5.82015647797038,5.872901481636,5.91300242004822,
5.92775728863181,5.94017853306185,5.96284937030756,5.99706344315429,6.06492185284883,
6.08901671388651,6.11001158146563,6.14035782781468,6.22316375865817,6.24842600679028,
6.26117260717653,6.27525839703446,6.31394127226314,6.39916694977668,6.4219244805174,
6.44339981060996,6.47836891746152,6.52983710275213,6.5724178679904,6.58698095509419,
6.59947360921006,6.62275706998295,6.69225512275375,6.73206194066716,6.75403029276206,
6.7760589413377,6.81646931902625,6.88902612054175,6.90993336052652,6.92215094092272,
6.93756675402472,6.95633575549997,7.00008115709449,7.05657043084698,7.07975117479927,
7.10102194001076,7.13411441019393,7.1914134114673,7.23069167280445,7.24554717201633,
7.25798769433682,7.28060404660744,7.31466797652171,7.38255608232399,7.40664697340677,
7.42771054494079,7.45833253357428,7.5427346644408,7.56670106682125,7.57927538580445,
7.59353989701433,7.63629384962888,7.71167534647685,7.7359192222688,7.75672995854454,
7.78615535500089,7.82354158989668,7.83324491651743),.UNSPECIFIED.);
#1319=B_SPLINE_CURVE_WITH_KNOTS('',3,(#27186,#27187,#27188,#27189,#27190,
#27191,#27192,#27193,#27194,#27195,#27196,#27197,#27198,#27199,#27200,#27201,
#27202,#27203,#27204,#27205,#27206,#27207,#27208,#27209,#27210,#27211,#27212,
#27213,#27214,#27215,#27216,#27217,#27218,#27219,#27220,#27221,#27222,#27223,
#27224,#27225,#27226,#27227),.UNSPECIFIED.,.F.,.F.,(4,2,2,2,2,2,2,2,2,2,
2,2,2,2,2,2,2,2,2,2,4),(7.83324491651743,7.88736378546632,7.90302452762842,
7.91511738014786,7.93479602143784,7.96188536926654,8.04728261795144,8.07014143595615,
8.0916925458198,8.12681613428747,8.17876006848774,8.21984831770643,8.23469331810836,
8.24749030579618,8.27182649576923,8.34803095583536,8.38138093447557,8.4029187966207,
8.42667316414753,8.48702841435749,8.53519991959206),.UNSPECIFIED.);
#1320=B_SPLINE_CURVE_WITH_KNOTS('',3,(#27230,#27231,#27232,#27233,#27234,
#27235,#27236,#27237,#27238,#27239),.UNSPECIFIED.,.F.,.F.,(4,2,2,2,4),(-0.120342605042655,
-0.0910596067984688,-0.0177190149419271,-0.0080247817111039,0.),
 .UNSPECIFIED.);
#1321=B_SPLINE_CURVE_WITH_KNOTS('',3,(#27242,#27243,#27244,#27245),
 .UNSPECIFIED.,.F.,.F.,(4,4),(33.9036448620551,34.557517409689),
 .UNSPECIFIED.);
#1322=B_SPLINE_CURVE_WITH_KNOTS('',3,(#27247,#27248,#27249,#27250,#27251,
#27252,#27253,#27254,#27255,#27256,#27257,#27258,#27259,#27260,#27261,#27262,
#27263,#27264,#27265,#27266,#27267,#27268,#27269,#27270,#27271,#27272,#27273,
#27274,#27275,#27276,#27277,#27278,#27279,#27280,#27281,#27282,#27283,#27284,
#27285,#27286,#27287,#27288,#27289,#27290,#27291,#27292,#27293,#27294,#27295,
#27296,#27297,#27298,#27299,#27300,#27301,#27302,#27303,#27304,#27305,#27306,
#27307,#27308,#27309,#27310,#27311,#27312,#27313,#27314,#27315,#27316,#27317,
#27318,#27319,#27320,#27321,#27322,#27323,#27324,#27325,#27326,#27327,#27328,
#27329,#27330,#27331,#27332,#27333,#27334,#27335,#27336,#27337,#27338,#27339,
#27340,#27341,#27342,#27343,#27344,#27345,#27346,#27347,#27348,#27349,#27350,
#27351,#27352,#27353,#27354,#27355,#27356,#27357,#27358,#27359,#27360,#27361,
#27362,#27363,#27364,#27365,#27366,#27367,#27368,#27369,#27370,#27371,#27372,
#27373,#27374,#27375,#27376,#27377,#27378,#27379,#27380,#27381,#27382,#27383,
#27384,#27385,#27386,#27387,#27388,#27389,#27390,#27391,#27392,#27393,#27394,
#27395,#27396,#27397,#27398,#27399,#27400,#27401,#27402,#27403,#27404,#27405,
#27406,#27407,#27408,#27409,#27410,#27411,#27412,#27413,#27414,#27415,#27416,
#27417,#27418),.UNSPECIFIED.,.F.,.F.,(4,3,3,3,3,3,3,3,3,3,3,3,3,3,3,3,3,
3,3,3,3,3,3,3,3,3,3,3,3,3,3,3,3,3,3,3,3,3,3,3,3,3,3,3,3,3,3,3,3,3,3,3,3,
3,3,3,3,4),(34.5575191894877,34.6769348838958,34.7619343778369,34.8499952335888,
34.9379496562291,35.0258202981564,35.1140417529446,35.2018216192856,35.2895904089036,
35.3773684781906,35.4659243427584,35.5538256903796,35.6427088134206,35.7315919364616,
35.8196619820676,35.9076258712916,35.9955062403964,36.0837241472326,36.1715143057049,
36.2592935793087,36.3470823108465,36.4356241069065,36.5235364515172,36.6123929733018,
36.7012494950864,36.7891973320126,36.8770385913154,36.9647960700815,37.0530599430352,
37.1407273852193,37.2283842340686,37.3160509754662,37.4047649950274,37.4925575294465,
37.5817322915788,37.6709070537111,37.7590928978415,37.8471720280796,37.9351669372927,
38.023341646673,38.1112438804587,38.1991340908128,38.2870324896825,38.3754155203458,
38.4634334250405,38.5519990186881,38.6405646123358,38.7277373495786,38.8148055298882,
38.9044381980817,38.9913694404484,39.0782741687425,39.1651736724377,39.2520892322613,
39.3390842030036,39.4261272395307,39.5132811504422,39.5318668754359),
 .UNSPECIFIED.);
#1323=B_SPLINE_CURVE_WITH_KNOTS('',3,(#27422,#27423,#27424,#27425,#27426,
#27427,#27428,#27429),.UNSPECIFIED.,.F.,.F.,(4,1,1,1,1,4),(34.5575191894877,
35.12931922981,36.0989767884347,37.0686343470595,38.0382919056842,39.0079494643089),
 .UNSPECIFIED.);
#1324=B_SPLINE_CURVE_WITH_KNOTS('',3,(#27430,#27431,#27432,#27433,#27434),
 .UNSPECIFIED.,.F.,.F.,(4,1,4),(33.9023219446702,34.1596616711853,34.5575191894877),
 .UNSPECIFIED.);
#1325=B_SPLINE_CURVE_WITH_KNOTS('',3,(#27560,#27561,#27562,#27563,#27564,
#27565,#27566,#27567,#27568,#27569,#27570,#27571,#27572,#27573,#27574,#27575,
#27576,#27577,#27578,#27579,#27580,#27581,#27582,#27583,#27584,#27585,#27586,
#27587,#27588,#27589,#27590,#27591,#27592,#27593,#27594,#27595,#27596,#27597,
#27598,#27599,#27600,#27601,#27602,#27603,#27604,#27605,#27606,#27607,#27608,
#27609,#27610,#27611,#27612,#27613,#27614,#27615,#27616,#27617,#27618,#27619,
#27620,#27621,#27622,#27623,#27624,#27625,#27626,#27627,#27628,#27629,#27630,
#27631,#27632,#27633,#27634,#27635,#27636,#27637,#27638,#27639,#27640,#27641,
#27642,#27643,#27644,#27645,#27646,#27647,#27648,#27649,#27650),
 .UNSPECIFIED.,.F.,.F.,(4,3,3,3,3,3,3,3,3,3,3,3,3,3,3,3,3,3,3,3,3,3,3,3,
3,3,3,3,3,3,4),(0.,0.0371673843853462,0.0748693007053213,0.112706345019989,
0.146754419031169,0.154576061769547,0.159872184166855,0.196816634794726,
0.233577891628905,0.269502801433578,0.298936453110779,0.306086760141218,
0.311219678986263,0.347080703449979,0.382941727913695,0.418958403167855,
0.449351754992565,0.454627452010795,0.489595285086492,0.524700175211502,
0.559247248798574,0.592850943657959,0.598655230831888,0.632673659813041,
0.665941928010469,0.67053803226665,0.677685069465016,0.685585591405337,
0.718097783781032,0.733842861978519,0.7607598169945),.UNSPECIFIED.);
#1326=B_SPLINE_CURVE_WITH_KNOTS('',3,(#27651,#27652,#27653,#27654),
 .UNSPECIFIED.,.F.,.F.,(4,4),(-0.0128693341657787,0.),.UNSPECIFIED.);
#1327=B_SPLINE_CURVE_WITH_KNOTS('',3,(#27655,#27656,#27657,#27658,#27659,
#27660,#27661,#27662,#27663,#27664,#27665,#27666,#27667,#27668,#27669,#27670,
#27671,#27672,#27673,#27674,#27675,#27676,#27677,#27678,#27679,#27680,#27681,
#27682,#27683,#27684,#27685,#27686,#27687,#27688,#27689,#27690,#27691,#27692,
#27693,#27694,#27695,#27696,#27697,#27698,#27699,#27700,#27701,#27702,#27703,
#27704,#27705,#27706,#27707,#27708,#27709,#27710,#27711,#27712,#27713,#27714,
#27715,#27716,#27717,#27718,#27719,#27720,#27721,#27722,#27723,#27724,#27725,
#27726,#27727,#27728,#27729,#27730,#27731,#27732,#27733,#27734,#27735,#27736,
#27737,#27738,#27739,#27740,#27741,#27742),.UNSPECIFIED.,.F.,.F.,(4,3,3,
3,3,3,3,3,3,3,3,3,3,3,3,3,3,3,3,3,3,3,3,3,3,3,3,3,3,4),(2.84112346422651E-15,
0.0321878095080291,0.0648568461842673,0.0983283809336569,0.128751238032108,
0.1340110409187,0.14433350266263,0.178553412701981,0.213220662816023,0.246728237516609,
0.272650549117548,0.278294855644787,0.29438467656025,0.329979550746285,
0.347250961618367,0.382122925792846,0.414901056202246,0.421530557898444,
0.45684142113921,0.49289896799214,0.529433101181703,0.562152125203941,0.568353583238998,
0.605677260428984,0.642991738905437,0.660309197270654,0.666091466789222,
0.703920126902519,0.725827582042816,0.757732684314163),.UNSPECIFIED.);
#1328=B_SPLINE_CURVE_WITH_KNOTS('',3,(#27867,#27868,#27869,#27870,#27871,
#27872,#27873,#27874,#27875,#27876,#27877,#27878,#27879,#27880,#27881,#27882,
#27883,#27884,#27885,#27886,#27887,#27888,#27889,#27890,#27891,#27892,#27893,
#27894,#27895,#27896,#27897,#27898,#27899,#27900,#27901,#27902,#27903,#27904,
#27905,#27906,#27907,#27908,#27909,#27910,#27911,#27912,#27913,#27914,#27915,
#27916,#27917,#27918,#27919,#27920,#27921,#27922,#27923,#27924,#27925,#27926,
#27927,#27928,#27929,#27930,#27931,#27932,#27933,#27934,#27935,#27936,#27937,
#27938,#27939,#27940,#27941,#27942,#27943,#27944,#27945,#27946,#27947,#27948,
#27949,#27950,#27951,#27952,#27953,#27954,#27955,#27956,#27957),
 .UNSPECIFIED.,.F.,.F.,(4,3,3,3,3,3,3,3,3,3,3,3,3,3,3,3,3,3,3,3,3,3,3,3,
3,3,3,3,3,3,4),(0.,0.0321876396051637,0.0648564132377103,0.0983277964673542,
0.128750558420655,0.134005598284691,0.143992997014492,0.178320378143294,
0.212997816940641,0.247571536985515,0.268680605758807,0.273376200123601,
0.2783803293651,0.314015287499765,0.347250961618176,0.382123065927106,0.414901307298664,
0.421530568332327,0.456928426576089,0.492963289038479,0.529560343224023,
0.553903620195441,0.562418678032901,0.567813497614329,0.605133071291381,
0.642450419073943,0.660309272119139,0.666091576557883,0.703920232934646,
0.725827582042572,0.757703647974356),.UNSPECIFIED.);
#1329=B_SPLINE_CURVE_WITH_KNOTS('',3,(#27958,#27959,#27960,#27961,#27962,
#27963,#27964,#27965,#27966,#27967,#27968,#27969,#27970,#27971,#27972,#27973,
#27974,#27975,#27976,#27977,#27978,#27979,#27980,#27981,#27982,#27983,#27984,
#27985,#27986,#27987,#27988,#27989,#27990,#27991,#27992,#27993,#27994,#27995,
#27996,#27997,#27998,#27999,#28000,#28001,#28002,#28003,#28004,#28005,#28006,
#28007,#28008,#28009,#28010,#28011,#28012,#28013,#28014,#28015,#28016,#28017,
#28018,#28019,#28020,#28021,#28022,#28023,#28024,#28025,#28026,#28027,#28028,
#28029,#28030,#28031,#28032,#28033,#28034,#28035,#28036,#28037,#28038,#28039,
#28040,#28041,#28042,#28043,#28044,#28045),.UNSPECIFIED.,.F.,.F.,(4,3,3,
3,3,3,3,3,3,3,3,3,3,3,3,3,3,3,3,3,3,3,3,3,3,3,3,3,3,4),(2.19148179006735E-15,
0.0367103964528547,0.0744331778325135,0.112337565911546,0.149893962136006,
0.154575496994253,0.159872057743945,0.196816523045437,0.233577852742176,
0.269502850644212,0.298936418321743,0.306086670949945,0.311219649844233,
0.347080688878984,0.382941727913735,0.418958395967714,0.449351764007576,
0.454627460526605,0.489595295166872,0.524700180321969,0.559247313820411,
0.59285103833404,0.598655234317479,0.632644611325471,0.665820672120261,
0.677685668474962,0.683715521223274,0.716251000825657,0.733842861978756,
0.760759816994732),.UNSPECIFIED.);
#1667=VERTEX_POINT('',#25102);
#1668=VERTEX_POINT('',#25103);
#1669=VERTEX_POINT('',#25105);
#1670=VERTEX_POINT('',#25111);
#1671=VERTEX_POINT('',#25118);
#1672=VERTEX_POINT('',#25119);
#1673=VERTEX_POINT('',#25121);
#1674=VERTEX_POINT('',#25136);
#1675=VERTEX_POINT('',#25339);
#1676=VERTEX_POINT('',#25340);
#1677=VERTEX_POINT('',#25342);
#1678=VERTEX_POINT('',#25541);
#1679=VERTEX_POINT('',#25761);
#1680=VERTEX_POINT('',#25762);
#1681=VERTEX_POINT('',#25764);
#1682=VERTEX_POINT('',#25800);
#1683=VERTEX_POINT('',#25834);
#1684=VERTEX_POINT('',#25835);
#1685=VERTEX_POINT('',#25837);
#1686=VERTEX_POINT('',#25851);
#1687=VERTEX_POINT('',#26042);
#1688=VERTEX_POINT('',#26133);
#1689=VERTEX_POINT('',#26134);
#1690=VERTEX_POINT('',#26136);
#1691=VERTEX_POINT('',#26481);
#1692=VERTEX_POINT('',#26482);
#1693=VERTEX_POINT('',#26484);
#1694=VERTEX_POINT('',#26836);
#1695=VERTEX_POINT('',#26837);
#1696=VERTEX_POINT('',#26839);
#1697=VERTEX_POINT('',#27185);
#1698=VERTEX_POINT('',#27228);
#1699=VERTEX_POINT('',#27241);
#1700=VERTEX_POINT('',#27246);
#1701=VERTEX_POINT('',#27419);
#1702=VERTEX_POINT('',#27421);
#1703=VERTEX_POINT('',#27559);
#1704=VERTEX_POINT('',#28047);
#1705=VERTEX_POINT('',#28048);
#1706=VERTEX_POINT('',#28050);
#1707=VERTEX_POINT('',#28052);
#1708=VERTEX_POINT('',#28054);
#1709=VERTEX_POINT('',#28056);
#1710=VERTEX_POINT('',#28060);
#1711=VERTEX_POINT('',#28062);
#1712=VERTEX_POINT('',#28066);
#1713=VERTEX_POINT('',#28070);
#1714=VERTEX_POINT('',#28074);
#1715=VERTEX_POINT('',#28078);
#2223=EDGE_CURVE('',#1667,#1668,#798,.T.);
#2224=EDGE_CURVE('',#1669,#1667,#1293,.T.);
#2225=EDGE_CURVE('',#1669,#1670,#635,.T.);
#2226=EDGE_CURVE('',#1670,#1668,#1294,.T.);
#2227=EDGE_CURVE('',#1671,#1672,#799,.T.);
#2228=EDGE_CURVE('',#1673,#1671,#1295,.T.);
#2229=EDGE_CURVE('',#1667,#1673,#1296,.T.);
#2230=EDGE_CURVE('',#1668,#1674,#1297,.T.);
#2231=EDGE_CURVE('',#1674,#1672,#1298,.T.);
#2232=EDGE_CURVE('',#1675,#1676,#800,.T.);
#2233=EDGE_CURVE('',#1677,#1675,#1299,.T.);
#2234=EDGE_CURVE('',#1671,#1677,#1300,.T.);
#2235=EDGE_CURVE('',#1672,#1678,#1301,.T.);
#2236=EDGE_CURVE('',#1678,#1676,#1302,.T.);
#2237=EDGE_CURVE('',#1679,#1680,#801,.T.);
#2238=EDGE_CURVE('',#1681,#1679,#1303,.T.);
#2239=EDGE_CURVE('',#1675,#1681,#1304,.T.);
#2240=EDGE_CURVE('',#1676,#1682,#1305,.T.);
#2241=EDGE_CURVE('',#1682,#1680,#1306,.T.);
#2242=EDGE_CURVE('',#1683,#1684,#802,.T.);
#2243=EDGE_CURVE('',#1685,#1683,#1307,.T.);
#2244=EDGE_CURVE('',#1686,#1685,#1308,.T.);
#2245=EDGE_CURVE('',#1686,#1687,#636,.F.);
#2246=EDGE_CURVE('',#1684,#1687,#1309,.F.);
#2247=EDGE_CURVE('',#1688,#1689,#803,.T.);
#2248=EDGE_CURVE('',#1690,#1688,#1310,.T.);
#2249=EDGE_CURVE('',#1683,#1690,#1311,.T.);
#2250=EDGE_CURVE('',#1689,#1684,#1312,.F.);
#2251=EDGE_CURVE('',#1691,#1692,#804,.T.);
#2252=EDGE_CURVE('',#1693,#1691,#1313,.T.);
#2253=EDGE_CURVE('',#1688,#1693,#1314,.T.);
#2254=EDGE_CURVE('',#1692,#1689,#1315,.F.);
#2255=EDGE_CURVE('',#1694,#1695,#805,.T.);
#2256=EDGE_CURVE('',#1696,#1694,#1316,.T.);
#2257=EDGE_CURVE('',#1691,#1696,#1317,.T.);
#2258=EDGE_CURVE('',#1695,#1692,#1318,.F.);
#2259=EDGE_CURVE('',#1697,#1695,#1319,.F.);
#2260=EDGE_CURVE('',#1697,#1698,#637,.T.);
#2261=EDGE_CURVE('',#1694,#1698,#1320,.T.);
#2262=EDGE_CURVE('',#1680,#1699,#1321,.T.);
#2263=EDGE_CURVE('',#1699,#1700,#1322,.T.);
#2264=EDGE_CURVE('',#1700,#1701,#638,.T.);
#2265=EDGE_CURVE('',#1702,#1701,#1323,.T.);
#2266=EDGE_CURVE('',#1679,#1702,#1324,.T.);
#2267=EDGE_CURVE('',#1701,#1703,#1325,.T.);
#2268=EDGE_CURVE('',#1703,#1697,#1326,.T.);
#2269=EDGE_CURVE('',#1687,#1669,#1327,.T.);
#2270=EDGE_CURVE('',#1698,#1700,#1328,.T.);
#2271=EDGE_CURVE('',#1670,#1686,#1329,.T.);
#2272=EDGE_CURVE('',#1704,#1705,#806,.T.);
#2273=EDGE_CURVE('',#1706,#1704,#807,.T.);
#2274=EDGE_CURVE('',#1707,#1706,#808,.T.);
#2275=EDGE_CURVE('',#1708,#1707,#809,.T.);
#2276=EDGE_CURVE('',#1709,#1708,#810,.T.);
#2277=EDGE_CURVE('',#1705,#1709,#811,.T.);
#2278=EDGE_CURVE('',#1709,#1710,#812,.T.);
#2279=EDGE_CURVE('',#1710,#1711,#813,.T.);
#2280=EDGE_CURVE('',#1705,#1711,#814,.T.);
#2281=EDGE_CURVE('',#1708,#1712,#815,.T.);
#2282=EDGE_CURVE('',#1712,#1710,#816,.T.);
#2283=EDGE_CURVE('',#1707,#1713,#817,.T.);
#2284=EDGE_CURVE('',#1713,#1712,#818,.T.);
#2285=EDGE_CURVE('',#1706,#1714,#819,.T.);
#2286=EDGE_CURVE('',#1714,#1713,#820,.T.);
#2287=EDGE_CURVE('',#1704,#1715,#821,.T.);
#2288=EDGE_CURVE('',#1715,#1714,#822,.T.);
#2289=EDGE_CURVE('',#1711,#1715,#823,.T.);
#3139=ORIENTED_EDGE('',*,*,#2223,.F.);
#3140=ORIENTED_EDGE('',*,*,#2224,.F.);
#3141=ORIENTED_EDGE('',*,*,#2225,.T.);
#3142=ORIENTED_EDGE('',*,*,#2226,.T.);
#3143=ORIENTED_EDGE('',*,*,#2227,.F.);
#3144=ORIENTED_EDGE('',*,*,#2228,.F.);
#3145=ORIENTED_EDGE('',*,*,#2229,.F.);
#3146=ORIENTED_EDGE('',*,*,#2223,.T.);
#3147=ORIENTED_EDGE('',*,*,#2230,.T.);
#3148=ORIENTED_EDGE('',*,*,#2231,.T.);
#3149=ORIENTED_EDGE('',*,*,#2232,.F.);
#3150=ORIENTED_EDGE('',*,*,#2233,.F.);
#3151=ORIENTED_EDGE('',*,*,#2234,.F.);
#3152=ORIENTED_EDGE('',*,*,#2227,.T.);
#3153=ORIENTED_EDGE('',*,*,#2235,.T.);
#3154=ORIENTED_EDGE('',*,*,#2236,.T.);
#3155=ORIENTED_EDGE('',*,*,#2237,.F.);
#3156=ORIENTED_EDGE('',*,*,#2238,.F.);
#3157=ORIENTED_EDGE('',*,*,#2239,.F.);
#3158=ORIENTED_EDGE('',*,*,#2232,.T.);
#3159=ORIENTED_EDGE('',*,*,#2240,.T.);
#3160=ORIENTED_EDGE('',*,*,#2241,.T.);
#3161=ORIENTED_EDGE('',*,*,#2242,.F.);
#3162=ORIENTED_EDGE('',*,*,#2243,.F.);
#3163=ORIENTED_EDGE('',*,*,#2244,.F.);
#3164=ORIENTED_EDGE('',*,*,#2245,.T.);
#3165=ORIENTED_EDGE('',*,*,#2246,.F.);
#3166=ORIENTED_EDGE('',*,*,#2247,.F.);
#3167=ORIENTED_EDGE('',*,*,#2248,.F.);
#3168=ORIENTED_EDGE('',*,*,#2249,.F.);
#3169=ORIENTED_EDGE('',*,*,#2242,.T.);
#3170=ORIENTED_EDGE('',*,*,#2250,.F.);
#3171=ORIENTED_EDGE('',*,*,#2251,.F.);
#3172=ORIENTED_EDGE('',*,*,#2252,.F.);
#3173=ORIENTED_EDGE('',*,*,#2253,.F.);
#3174=ORIENTED_EDGE('',*,*,#2247,.T.);
#3175=ORIENTED_EDGE('',*,*,#2254,.F.);
#3176=ORIENTED_EDGE('',*,*,#2255,.F.);
#3177=ORIENTED_EDGE('',*,*,#2256,.F.);
#3178=ORIENTED_EDGE('',*,*,#2257,.F.);
#3179=ORIENTED_EDGE('',*,*,#2251,.T.);
#3180=ORIENTED_EDGE('',*,*,#2258,.F.);
#3181=ORIENTED_EDGE('',*,*,#2255,.T.);
#3182=ORIENTED_EDGE('',*,*,#2259,.F.);
#3183=ORIENTED_EDGE('',*,*,#2260,.T.);
#3184=ORIENTED_EDGE('',*,*,#2261,.F.);
#3185=ORIENTED_EDGE('',*,*,#2237,.T.);
#3186=ORIENTED_EDGE('',*,*,#2262,.T.);
#3187=ORIENTED_EDGE('',*,*,#2263,.T.);
#3188=ORIENTED_EDGE('',*,*,#2264,.T.);
#3189=ORIENTED_EDGE('',*,*,#2265,.F.);
#3190=ORIENTED_EDGE('',*,*,#2266,.F.);
#3191=ORIENTED_EDGE('',*,*,#2267,.T.);
#3192=ORIENTED_EDGE('',*,*,#2268,.T.);
#3193=ORIENTED_EDGE('',*,*,#2259,.T.);
#3194=ORIENTED_EDGE('',*,*,#2258,.T.);
#3195=ORIENTED_EDGE('',*,*,#2254,.T.);
#3196=ORIENTED_EDGE('',*,*,#2250,.T.);
#3197=ORIENTED_EDGE('',*,*,#2246,.T.);
#3198=ORIENTED_EDGE('',*,*,#2269,.T.);
#3199=ORIENTED_EDGE('',*,*,#2224,.T.);
#3200=ORIENTED_EDGE('',*,*,#2229,.T.);
#3201=ORIENTED_EDGE('',*,*,#2228,.T.);
#3202=ORIENTED_EDGE('',*,*,#2234,.T.);
#3203=ORIENTED_EDGE('',*,*,#2233,.T.);
#3204=ORIENTED_EDGE('',*,*,#2239,.T.);
#3205=ORIENTED_EDGE('',*,*,#2238,.T.);
#3206=ORIENTED_EDGE('',*,*,#2266,.T.);
#3207=ORIENTED_EDGE('',*,*,#2265,.T.);
#3208=ORIENTED_EDGE('',*,*,#2270,.T.);
#3209=ORIENTED_EDGE('',*,*,#2263,.F.);
#3210=ORIENTED_EDGE('',*,*,#2262,.F.);
#3211=ORIENTED_EDGE('',*,*,#2241,.F.);
#3212=ORIENTED_EDGE('',*,*,#2240,.F.);
#3213=ORIENTED_EDGE('',*,*,#2236,.F.);
#3214=ORIENTED_EDGE('',*,*,#2235,.F.);
#3215=ORIENTED_EDGE('',*,*,#2231,.F.);
#3216=ORIENTED_EDGE('',*,*,#2230,.F.);
#3217=ORIENTED_EDGE('',*,*,#2226,.F.);
#3218=ORIENTED_EDGE('',*,*,#2271,.T.);
#3219=ORIENTED_EDGE('',*,*,#2244,.T.);
#3220=ORIENTED_EDGE('',*,*,#2243,.T.);
#3221=ORIENTED_EDGE('',*,*,#2249,.T.);
#3222=ORIENTED_EDGE('',*,*,#2248,.T.);
#3223=ORIENTED_EDGE('',*,*,#2253,.T.);
#3224=ORIENTED_EDGE('',*,*,#2252,.T.);
#3225=ORIENTED_EDGE('',*,*,#2257,.T.);
#3226=ORIENTED_EDGE('',*,*,#2256,.T.);
#3227=ORIENTED_EDGE('',*,*,#2261,.T.);
#3228=ORIENTED_EDGE('',*,*,#2272,.F.);
#3229=ORIENTED_EDGE('',*,*,#2273,.F.);
#3230=ORIENTED_EDGE('',*,*,#2274,.F.);
#3231=ORIENTED_EDGE('',*,*,#2275,.F.);
#3232=ORIENTED_EDGE('',*,*,#2276,.F.);
#3233=ORIENTED_EDGE('',*,*,#2277,.F.);
#3234=ORIENTED_EDGE('',*,*,#2269,.F.);
#3235=ORIENTED_EDGE('',*,*,#2245,.F.);
#3236=ORIENTED_EDGE('',*,*,#2271,.F.);
#3237=ORIENTED_EDGE('',*,*,#2225,.F.);
#3238=ORIENTED_EDGE('',*,*,#2277,.T.);
#3239=ORIENTED_EDGE('',*,*,#2278,.T.);
#3240=ORIENTED_EDGE('',*,*,#2279,.T.);
#3241=ORIENTED_EDGE('',*,*,#2280,.F.);
#3242=ORIENTED_EDGE('',*,*,#2276,.T.);
#3243=ORIENTED_EDGE('',*,*,#2281,.T.);
#3244=ORIENTED_EDGE('',*,*,#2282,.T.);
#3245=ORIENTED_EDGE('',*,*,#2278,.F.);
#3246=ORIENTED_EDGE('',*,*,#2275,.T.);
#3247=ORIENTED_EDGE('',*,*,#2283,.T.);
#3248=ORIENTED_EDGE('',*,*,#2284,.T.);
#3249=ORIENTED_EDGE('',*,*,#2281,.F.);
#3250=ORIENTED_EDGE('',*,*,#2274,.T.);
#3251=ORIENTED_EDGE('',*,*,#2285,.T.);
#3252=ORIENTED_EDGE('',*,*,#2286,.T.);
#3253=ORIENTED_EDGE('',*,*,#2283,.F.);
#3254=ORIENTED_EDGE('',*,*,#2273,.T.);
#3255=ORIENTED_EDGE('',*,*,#2287,.T.);
#3256=ORIENTED_EDGE('',*,*,#2288,.T.);
#3257=ORIENTED_EDGE('',*,*,#2285,.F.);
#3258=ORIENTED_EDGE('',*,*,#2272,.T.);
#3259=ORIENTED_EDGE('',*,*,#2280,.T.);
#3260=ORIENTED_EDGE('',*,*,#2289,.T.);
#3261=ORIENTED_EDGE('',*,*,#2287,.F.);
#3262=ORIENTED_EDGE('',*,*,#2289,.F.);
#3263=ORIENTED_EDGE('',*,*,#2279,.F.);
#3264=ORIENTED_EDGE('',*,*,#2282,.F.);
#3265=ORIENTED_EDGE('',*,*,#2284,.F.);
#3266=ORIENTED_EDGE('',*,*,#2286,.F.);
#3267=ORIENTED_EDGE('',*,*,#2288,.F.);
#3268=ORIENTED_EDGE('',*,*,#2267,.F.);
#3269=ORIENTED_EDGE('',*,*,#2264,.F.);
#3270=ORIENTED_EDGE('',*,*,#2270,.F.);
#3271=ORIENTED_EDGE('',*,*,#2260,.F.);
#3272=ORIENTED_EDGE('',*,*,#2268,.F.);
#3996=CYLINDRICAL_SURFACE('',#4467,4.08499999999997);
#3997=CYLINDRICAL_SURFACE('',#4469,4.08499999999997);
#3998=CYLINDRICAL_SURFACE('',#4470,4.08499999999997);
#3999=CYLINDRICAL_SURFACE('',#4471,4.08499999999997);
#4000=CYLINDRICAL_SURFACE('',#4472,3.38975);
#4001=CYLINDRICAL_SURFACE('',#4474,3.38975);
#4002=CYLINDRICAL_SURFACE('',#4475,3.38975);
#4003=CYLINDRICAL_SURFACE('',#4476,3.38975);
#4004=CYLINDRICAL_SURFACE('',#4477,3.38975);
#4005=CYLINDRICAL_SURFACE('',#4479,4.08499999999997);
#4138=ADVANCED_FACE('',(#255),#3996,.F.);
#4139=ADVANCED_FACE('',(#256),#3997,.F.);
#4140=ADVANCED_FACE('',(#257),#3998,.F.);
#4141=ADVANCED_FACE('',(#258),#3999,.F.);
#4142=ADVANCED_FACE('',(#259),#4000,.F.);
#4143=ADVANCED_FACE('',(#260),#4001,.F.);
#4144=ADVANCED_FACE('',(#261),#4002,.F.);
#4145=ADVANCED_FACE('',(#262),#4003,.F.);
#4146=ADVANCED_FACE('',(#263),#4004,.F.);
#4147=ADVANCED_FACE('',(#264),#4005,.F.);
#4148=ADVANCED_FACE('',(#265),#58,.T.);
#4149=ADVANCED_FACE('',(#266),#59,.T.);
#4150=ADVANCED_FACE('',(#267,#104),#139,.F.);
#4151=ADVANCED_FACE('',(#268),#140,.F.);
#4152=ADVANCED_FACE('',(#269),#141,.F.);
#4153=ADVANCED_FACE('',(#270),#142,.F.);
#4154=ADVANCED_FACE('',(#271),#143,.F.);
#4155=ADVANCED_FACE('',(#272),#144,.F.);
#4156=ADVANCED_FACE('',(#273),#145,.F.);
#4157=ADVANCED_FACE('',(#274,#105),#146,.T.);
#4261=CLOSED_SHELL('',(#4138,#4139,#4140,#4141,#4142,#4143,#4144,#4145,
#4146,#4147,#4148,#4149,#4150,#4151,#4152,#4153,#4154,#4155,#4156,#4157));
#4466=AXIS2_PLACEMENT_3D('',#25100,#4976,#4977);
#4467=AXIS2_PLACEMENT_3D('',#25101,#4978,#4979);
#4468=AXIS2_PLACEMENT_3D('',#25112,#4981,#4982);
#4469=AXIS2_PLACEMENT_3D('',#25117,#4983,#4984);
#4470=AXIS2_PLACEMENT_3D('',#25338,#4986,#4987);
#4471=AXIS2_PLACEMENT_3D('',#25760,#4989,#4990);
#4472=AXIS2_PLACEMENT_3D('',#25833,#4992,#4993);
#4473=AXIS2_PLACEMENT_3D('',#26043,#4995,#4996);
#4474=AXIS2_PLACEMENT_3D('',#26132,#4997,#4998);
#4475=AXIS2_PLACEMENT_3D('',#26480,#5000,#5001);
#4476=AXIS2_PLACEMENT_3D('',#26835,#5003,#5004);
#4477=AXIS2_PLACEMENT_3D('',#27184,#5006,#5007);
#4478=AXIS2_PLACEMENT_3D('',#27229,#5008,#5009);
#4479=AXIS2_PLACEMENT_3D('',#27240,#5010,#5011);
#4480=AXIS2_PLACEMENT_3D('',#27420,#5012,#5013);
#4481=AXIS2_PLACEMENT_3D('',#28046,#5014,#5015);
#4482=AXIS2_PLACEMENT_3D('',#28059,#5022,#5023);
#4483=AXIS2_PLACEMENT_3D('',#28065,#5027,#5028);
#4484=AXIS2_PLACEMENT_3D('',#28069,#5031,#5032);
#4485=AXIS2_PLACEMENT_3D('',#28073,#5035,#5036);
#4486=AXIS2_PLACEMENT_3D('',#28077,#5039,#5040);
#4487=AXIS2_PLACEMENT_3D('',#28081,#5043,#5044);
#4488=AXIS2_PLACEMENT_3D('',#28083,#5046,#5047);
#4976=DIRECTION('axis',(0.,0.,1.));
#4977=DIRECTION('refdir',(1.,0.,0.));
#4978=DIRECTION('center_axis',(0.,-2.22044604925031E-16,-1.));
#4979=DIRECTION('ref_axis',(-0.793396157953295,-0.608705623881487,1.35159799770409E-16));
#4980=DIRECTION('',(0.,-2.22044604925031E-16,-1.));
#4981=DIRECTION('center_axis',(0.,-2.22044604925031E-16,-1.));
#4982=DIRECTION('ref_axis',(-1.,3.91712146416972E-15,-8.69775687954924E-31));
#4983=DIRECTION('center_axis',(0.,-2.22044604925031E-16,-1.));
#4984=DIRECTION('ref_axis',(-0.793396157953295,-0.608705623881487,1.35159799770409E-16));
#4985=DIRECTION('',(0.,-2.22044604925031E-16,-1.));
#4986=DIRECTION('center_axis',(0.,-2.22044604925031E-16,-1.));
#4987=DIRECTION('ref_axis',(-0.793396157953295,-0.608705623881487,1.35159799770409E-16));
#4988=DIRECTION('',(0.,-2.22044604925031E-16,-1.));
#4989=DIRECTION('center_axis',(0.,-2.22044604925031E-16,-1.));
#4990=DIRECTION('ref_axis',(-0.793396157953295,-0.608705623881487,1.35159799770409E-16));
#4991=DIRECTION('',(0.,-2.22044604925031E-16,-1.));
#4992=DIRECTION('center_axis',(0.,-2.22044604925031E-16,-1.));
#4993=DIRECTION('ref_axis',(-0.862028396347557,0.506859984503077,-1.12545525011293E-16));
#4994=DIRECTION('',(0.,-2.22044604925031E-16,-1.));
#4995=DIRECTION('center_axis',(0.,2.22044604925031E-16,1.));
#4996=DIRECTION('ref_axis',(-1.,0.,0.));
#4997=DIRECTION('center_axis',(0.,-2.22044604925031E-16,-1.));
#4998=DIRECTION('ref_axis',(-0.937789548385183,0.34720420927678,-7.70948214771704E-17));
#4999=DIRECTION('',(0.,-2.22044604925031E-16,-1.));
#5000=DIRECTION('center_axis',(0.,-2.22044604925031E-16,-1.));
#5001=DIRECTION('ref_axis',(-0.937789548385183,0.34720420927678,-7.70948214771704E-17));
#5002=DIRECTION('',(0.,-2.22044604925031E-16,-1.));
#5003=DIRECTION('center_axis',(0.,-2.22044604925031E-16,-1.));
#5004=DIRECTION('ref_axis',(-0.937789548385183,0.34720420927678,-7.70948214771704E-17));
#5005=DIRECTION('',(0.,-2.22044604925031E-16,-1.));
#5006=DIRECTION('center_axis',(0.,-2.22044604925031E-16,-1.));
#5007=DIRECTION('ref_axis',(-0.937789548385183,0.34720420927678,-7.70948214771704E-17));
#5008=DIRECTION('center_axis',(0.,2.22044604925031E-16,1.));
#5009=DIRECTION('ref_axis',(-1.,0.,0.));
#5010=DIRECTION('center_axis',(0.,-2.22044604925031E-16,-1.));
#5011=DIRECTION('ref_axis',(-0.793396157953295,-0.608705623881487,1.35159799770409E-16));
#5012=DIRECTION('center_axis',(0.,2.22044604925031E-16,1.));
#5013=DIRECTION('ref_axis',(-1.,3.91712146416972E-15,-8.69775687954924E-31));
#5014=DIRECTION('center_axis',(0.,2.22044604925031E-16,1.));
#5015=DIRECTION('ref_axis',(-1.,0.,0.));
#5016=DIRECTION('',(0.,-1.,2.22044604925031E-16));
#5017=DIRECTION('',(-0.866025403784439,-0.5,1.11022302462516E-16));
#5018=DIRECTION('',(-0.866025403784439,0.5,-1.11022302462516E-16));
#5019=DIRECTION('',(0.,1.,-2.22044604925031E-16));
#5020=DIRECTION('',(0.866025403784439,0.5,-1.11022302462516E-16));
#5021=DIRECTION('',(0.866025403784439,-0.5,1.11022302462516E-16));
#5022=DIRECTION('center_axis',(0.5,0.866025403784439,-1.92296268638356E-16));
#5023=DIRECTION('ref_axis',(-0.866025403784439,0.5,-1.11022302462516E-16));
#5024=DIRECTION('',(0.,2.22044604925031E-16,1.));
#5025=DIRECTION('',(-0.866025403784439,0.5,-1.11022302462516E-16));
#5026=DIRECTION('',(0.,2.22044604925031E-16,1.));
#5027=DIRECTION('center_axis',(-0.5,0.866025403784439,-1.92296268638356E-16));
#5028=DIRECTION('ref_axis',(-0.866025403784439,-0.5,1.11022302462516E-16));
#5029=DIRECTION('',(0.,2.22044604925031E-16,1.));
#5030=DIRECTION('',(-0.866025403784439,-0.5,1.11022302462516E-16));
#5031=DIRECTION('center_axis',(-1.,0.,0.));
#5032=DIRECTION('ref_axis',(0.,-1.,2.22044604925031E-16));
#5033=DIRECTION('',(0.,2.22044604925031E-16,1.));
#5034=DIRECTION('',(0.,-1.,2.22044604925031E-16));
#5035=DIRECTION('center_axis',(-0.5,-0.866025403784439,1.92296268638356E-16));
#5036=DIRECTION('ref_axis',(0.866025403784439,-0.5,1.11022302462516E-16));
#5037=DIRECTION('',(0.,2.22044604925031E-16,1.));
#5038=DIRECTION('',(0.866025403784439,-0.5,1.11022302462516E-16));
#5039=DIRECTION('center_axis',(0.5,-0.866025403784439,1.92296268638356E-16));
#5040=DIRECTION('ref_axis',(0.866025403784439,0.5,-1.11022302462516E-16));
#5041=DIRECTION('',(0.,2.22044604925031E-16,1.));
#5042=DIRECTION('',(0.866025403784439,0.5,-1.11022302462516E-16));
#5043=DIRECTION('center_axis',(1.,0.,0.));
#5044=DIRECTION('ref_axis',(0.,1.,-2.22044604925031E-16));
#5045=DIRECTION('',(0.,1.,-2.22044604925031E-16));
#5046=DIRECTION('center_axis',(0.,2.22044604925031E-16,1.));
#5047=DIRECTION('ref_axis',(-1.,0.,0.));
#25100=CARTESIAN_POINT('',(0.,0.,0.));
#25101=CARTESIAN_POINT('Origin',(4.45646910621825,2.93978508838399E-15,
8.23961502859548));
#25102=CARTESIAN_POINT('',(7.69556181015728,2.48510987823924,11.2345514513157));
#25103=CARTESIAN_POINT('',(7.69439310869886,2.48413784397184,11.129953879674));
#25104=CARTESIAN_POINT('',(7.69749241145744,2.48656247355586,8.23961502859548));
#25105=CARTESIAN_POINT('',(3.39564331816006,3.95074861019264,11.));
#25106=CARTESIAN_POINT('Ctrl Pts',(3.39564331816006,3.95074861019264,11.));
#25107=CARTESIAN_POINT('Ctrl Pts',(4.5655900814632,4.25812260114716,11.0591063170672));
#25108=CARTESIAN_POINT('Ctrl Pts',(6.31389358558768,3.94134188869289,11.1372901341725));
#25109=CARTESIAN_POINT('Ctrl Pts',(7.45937911124849,2.79816356646418,11.2154739512777));
#25110=CARTESIAN_POINT('Ctrl Pts',(7.69556181015739,2.48510987823911,11.2345514513157));
#25111=CARTESIAN_POINT('',(5.51437352919123,3.94563850749837,11.));
#25112=CARTESIAN_POINT('Origin',(4.45646910621825,3.5527136788005E-15,11.));
#25113=CARTESIAN_POINT('Ctrl Pts',(5.5143735291912,3.94563850749838,11.));
#25114=CARTESIAN_POINT('Ctrl Pts',(6.37349612905838,3.71529059383414,11.0433179598914));
#25115=CARTESIAN_POINT('Ctrl Pts',(7.14733598556437,3.18456765028079,11.0866359197827));
#25116=CARTESIAN_POINT('Ctrl Pts',(7.69439310869878,2.48413784397194,11.129953879674));
#25117=CARTESIAN_POINT('Origin',(4.45646910621825,2.93978508838399E-15,
8.23961502859548));
#25118=CARTESIAN_POINT('',(7.69775011106544,2.48676061171584,12.4842647253843));
#25119=CARTESIAN_POINT('',(7.69749241145744,2.48656247355586,12.3802773657823));
#25120=CARTESIAN_POINT('',(7.69749241145744,2.48656247355586,8.23961502859548));
#25121=CARTESIAN_POINT('',(8.54727164081007,-0.00047517376629813,11.3646150285955));
#25122=CARTESIAN_POINT('Ctrl Pts',(8.54727164081007,-0.000475173766298197,
11.3646150285955));
#25123=CARTESIAN_POINT('Ctrl Pts',(8.54735745749987,-0.0387234396568994,
11.3664854167815));
#25124=CARTESIAN_POINT('Ctrl Pts',(8.52991518830434,-1.39184926051541,11.4326582189516));
#25125=CARTESIAN_POINT('Ctrl Pts',(7.04969563431661,-4.0201072215765,11.5631334351056));
#25126=CARTESIAN_POINT('Ctrl Pts',(2.60806863526002,-4.41194201582685,11.7560406770575));
#25127=CARTESIAN_POINT('Ctrl Pts',(-0.227582196371091,-0.971141764274265,
11.9489479190094));
#25128=CARTESIAN_POINT('Ctrl Pts',(1.00642988914386,3.31373500369963,12.1418551609614));
#25129=CARTESIAN_POINT('Ctrl Pts',(4.92059444400304,4.61393675418963,12.3202940964197));
#25130=CARTESIAN_POINT('Ctrl Pts',(7.06770587424214,3.29253755255905,12.434430617894));
#25131=CARTESIAN_POINT('Ctrl Pts',(7.69775011106531,2.486760611716,12.4842647253843));
#25132=CARTESIAN_POINT('Ctrl Pts',(7.69556181015739,2.48510987823911,11.2345514513157));
#25133=CARTESIAN_POINT('Ctrl Pts',(8.23229822129631,1.77368048951597,11.2779059770756));
#25134=CARTESIAN_POINT('Ctrl Pts',(8.54528245914361,0.886097699817623,11.3212605028356));
#25135=CARTESIAN_POINT('Ctrl Pts',(8.54727164081007,-0.000475173766298063,
11.3646150285955));
#25136=CARTESIAN_POINT('',(8.54040281351477,0.00367837158999622,11.2603846386009));
#25137=CARTESIAN_POINT('Ctrl Pts',(7.69439310869878,2.48413784397194,11.129953879674));
#25138=CARTESIAN_POINT('Ctrl Pts',(7.95940316723485,2.14482968743651,11.1509383337667));
#25139=CARTESIAN_POINT('Ctrl Pts',(8.39820086233578,1.3593237731873,11.1944148818445));
#25140=CARTESIAN_POINT('Ctrl Pts',(8.53950282154932,0.466629832326752,11.2378914299223));
#25141=CARTESIAN_POINT('Ctrl Pts',(8.53683689913243,0.00369810825016921,
11.2603835239075));
#25142=CARTESIAN_POINT('Ctrl Pts',(8.54146745540981,0.00367247899891429,
11.2603849714045));
#25143=CARTESIAN_POINT('Ctrl Pts',(8.54157476677189,-0.115692869881448,
11.2661779401166));
#25144=CARTESIAN_POINT('Ctrl Pts',(8.53644591819133,-0.235111513907259,
11.2719709088288));
#25145=CARTESIAN_POINT('Ctrl Pts',(8.52609375567047,-0.354090684105999,
11.2777638775409));
#25146=CARTESIAN_POINT('Ctrl Pts',(8.51574265793688,-0.473057616522975,
11.2835562504085));
#25147=CARTESIAN_POINT('Ctrl Pts',(8.50016935000466,-0.591584757457358,
11.2893486232761));
#25148=CARTESIAN_POINT('Ctrl Pts',(8.47943865605452,-0.709183333905947,
11.2951409961437));
#25149=CARTESIAN_POINT('Ctrl Pts',(8.45870517893015,-0.82679769840907,11.3009341466594));
#25150=CARTESIAN_POINT('Ctrl Pts',(8.43281300991758,-0.943482847585876,
11.306727297175));
#25151=CARTESIAN_POINT('Ctrl Pts',(8.401878187897,-1.0587597358261,11.3125204476906));
#25152=CARTESIAN_POINT('Ctrl Pts',(8.37093187778747,-1.17407943378888,11.3183157495756));
#25153=CARTESIAN_POINT('Ctrl Pts',(8.33493929621817,-1.28798943581637,11.3241110514606));
#25154=CARTESIAN_POINT('Ctrl Pts',(8.29406628598849,-1.40002603040773,11.3299063533456));
#25155=CARTESIAN_POINT('Ctrl Pts',(8.25314563799088,-1.51219320440253,11.3357084096938));
#25156=CARTESIAN_POINT('Ctrl Pts',(8.20733334848537,-1.62248222845368,11.3415104660421));
#25157=CARTESIAN_POINT('Ctrl Pts',(8.15684339460683,-1.73044939996305,11.3473125223903));
#25158=CARTESIAN_POINT('Ctrl Pts',(8.10631811955717,-1.83849210188286,11.3531186376733));
#25159=CARTESIAN_POINT('Ctrl Pts',(8.05110885291911,-1.94420935528272,11.3589247529562));
#25160=CARTESIAN_POINT('Ctrl Pts',(7.99147467780075,-2.04718357967243,11.3647308682392));
#25161=CARTESIAN_POINT('Ctrl Pts',(7.93175327035386,-2.15030843382024,11.3705454766547));
#25162=CARTESIAN_POINT('Ctrl Pts',(7.86759425665247,-2.25068190833779,11.3763600850702));
#25163=CARTESIAN_POINT('Ctrl Pts',(7.79929905286146,-2.34791672506183,11.3821746934858));
#25164=CARTESIAN_POINT('Ctrl Pts',(7.78504872503205,-2.36820552922135,11.3833879569585));
#25165=CARTESIAN_POINT('Ctrl Pts',(7.7706184501971,-2.3883578030232,11.3846012204312));
#25166=CARTESIAN_POINT('Ctrl Pts',(7.75601117534001,-2.40837022363578,11.3858144839039));
#25167=CARTESIAN_POINT('Ctrl Pts',(7.68563116797709,-2.5047930214432,11.3916601664818));
#25168=CARTESIAN_POINT('Ctrl Pts',(7.61091634050207,-2.59827161053316,11.3975058490597));
#25169=CARTESIAN_POINT('Ctrl Pts',(7.53214114961318,-2.68839477783279,11.4033515316375));
#25170=CARTESIAN_POINT('Ctrl Pts',(7.45346095414875,-2.77840926512243,11.4091901648755));
#25171=CARTESIAN_POINT('Ctrl Pts',(7.37073040048886,-2.86507607822447,11.4150287981135));
#25172=CARTESIAN_POINT('Ctrl Pts',(7.28426616769128,-2.94801437905656,11.4208674313514));
#25173=CARTESIAN_POINT('Ctrl Pts',(7.19788420965286,-3.03087376021857,11.426700508857));
#25174=CARTESIAN_POINT('Ctrl Pts',(7.10777593234305,-3.11001141007274,11.4325335863625));
#25175=CARTESIAN_POINT('Ctrl Pts',(7.01429670284446,-3.18508131543562,11.438366663868));
#25176=CARTESIAN_POINT('Ctrl Pts',(6.92057628511734,-3.2603449106437,11.4442147914508));
#25177=CARTESIAN_POINT('Ctrl Pts',(6.82346777502968,-3.33151944144697,11.4500629190336));
#25178=CARTESIAN_POINT('Ctrl Pts',(6.72336512514716,-3.3982947840592,11.4559110466165));
#25179=CARTESIAN_POINT('Ctrl Pts',(6.62362386471074,-3.46482905509033,11.4617380613557));
#25180=CARTESIAN_POINT('Ctrl Pts',(6.52091038708962,-3.52699562482708,11.467565076095));
#25181=CARTESIAN_POINT('Ctrl Pts',(6.41564521302468,-3.58452981331144,11.4733920908342));
#25182=CARTESIAN_POINT('Ctrl Pts',(6.31039381885568,-3.64205647019631,11.4792183427794));
#25183=CARTESIAN_POINT('Ctrl Pts',(6.20259174768293,-3.69495175831188,11.4850445947245));
#25184=CARTESIAN_POINT('Ctrl Pts',(6.09268504542169,-3.7429964467384,11.4908708466696));
#25185=CARTESIAN_POINT('Ctrl Pts',(5.9827674125012,-3.79104591340053,11.4966976780587));
#25186=CARTESIAN_POINT('Ctrl Pts',(5.87074510297772,-3.83424365919276,11.5025245094478));
#25187=CARTESIAN_POINT('Ctrl Pts',(5.75708455421943,-3.87241842475996,11.5083513408369));
#25188=CARTESIAN_POINT('Ctrl Pts',(5.64269510245319,-3.91083800439637,11.5142155395885));
#25189=CARTESIAN_POINT('Ctrl Pts',(5.52664671484859,-3.94416980886718,11.52007973834));
#25190=CARTESIAN_POINT('Ctrl Pts',(5.40942970654366,-3.97229040909991,11.5259439370916));
#25191=CARTESIAN_POINT('Ctrl Pts',(5.29279910486616,-4.00027032918237,11.5317787987609));
#25192=CARTESIAN_POINT('Ctrl Pts',(5.17501195806892,-4.02309104079298,11.5376136604303));
#25193=CARTESIAN_POINT('Ctrl Pts',(5.05655990529035,-4.04068261966573,11.5434485220996));
#25194=CARTESIAN_POINT('Ctrl Pts',(4.93721450546845,-4.05840687150282,11.5493273893923));
#25195=CARTESIAN_POINT('Ctrl Pts',(4.81719454464012,-4.07082274578235,11.555206256685));
#25196=CARTESIAN_POINT('Ctrl Pts',(4.6970054840309,-4.0779121190811,11.5610851239777));
#25197=CARTESIAN_POINT('Ctrl Pts',(4.57681642342169,-4.08500149237984,11.5669639912704));
#25198=CARTESIAN_POINT('Ctrl Pts',(4.45645867845014,-4.08676441141684,11.5728428585631));
#25199=CARTESIAN_POINT('Ctrl Pts',(4.33643407615524,-4.08323604406572,11.5787217258558));
#25200=CARTESIAN_POINT('Ctrl Pts',(4.21705838925101,-4.07972675290261,11.584568808936));
#25201=CARTESIAN_POINT('Ctrl Pts',(4.09766291769109,-4.07097301841782,11.5904158920162));
#25202=CARTESIAN_POINT('Ctrl Pts',(3.9787423507795,-4.05696957680702,11.5962629750963));
#25203=CARTESIAN_POINT('Ctrl Pts',(3.85996204158473,-4.04298265118499,11.6021031619891));
#25204=CARTESIAN_POINT('Ctrl Pts',(3.74165592123341,-4.02375838344357,11.6079433488818));
#25205=CARTESIAN_POINT('Ctrl Pts',(3.62431738646312,-3.99934351054124,11.6137835357745));
#25206=CARTESIAN_POINT('Ctrl Pts',(3.5070874522047,-3.97495123437321,11.6196183173902));
#25207=CARTESIAN_POINT('Ctrl Pts',(3.39082371543823,-3.94537799450139,11.6254530990059));
#25208=CARTESIAN_POINT('Ctrl Pts',(3.27601261611103,-3.91072211681723,11.6312878806216));
#25209=CARTESIAN_POINT('Ctrl Pts',(3.16095036555719,-3.87599042881298,11.637135425921));
#25210=CARTESIAN_POINT('Ctrl Pts',(3.04734751891907,-3.83615390439813,11.6429829712204));
#25211=CARTESIAN_POINT('Ctrl Pts',(2.93568203361168,-3.79136277343549,11.6488305165199));
#25212=CARTESIAN_POINT('Ctrl Pts',(2.82436919903747,-3.74671309732912,11.6546595946884));
#25213=CARTESIAN_POINT('Ctrl Pts',(2.71498188359263,-3.6971402155858,11.6604886728568));
#25214=CARTESIAN_POINT('Ctrl Pts',(2.6079761081951,-3.64284210970763,11.6663177510253));
#25215=CARTESIAN_POINT('Ctrl Pts',(2.5009819057502,-3.58854987631068,11.6721461987639));
#25216=CARTESIAN_POINT('Ctrl Pts',(2.39636909137021,-3.52953361839601,11.6779746465024));
#25217=CARTESIAN_POINT('Ctrl Pts',(2.29457054318916,-3.46603802679262,11.683803094241));
#25218=CARTESIAN_POINT('Ctrl Pts',(2.19275959622875,-3.40253470160319,11.6896322518682));
#25219=CARTESIAN_POINT('Ctrl Pts',(2.09376394011757,-3.33455117173568,11.6954614094954));
#25220=CARTESIAN_POINT('Ctrl Pts',(1.99798833561155,-3.26237602071815,11.7012905671227));
#25221=CARTESIAN_POINT('Ctrl Pts',(1.90168078318288,-3.18980000121383,11.7071521005131));
#25222=CARTESIAN_POINT('Ctrl Pts',(1.8086294954468,-3.11298589896686,11.7130136339035));
#25223=CARTESIAN_POINT('Ctrl Pts',(1.7192122295977,-3.03226809358824,11.7188751672939));
#25224=CARTESIAN_POINT('Ctrl Pts',(1.63016174687966,-2.95188138678558,11.7247126571));
#25225=CARTESIAN_POINT('Ctrl Pts',(1.54471578341265,-2.86762326311697,11.7305501469062));
#25226=CARTESIAN_POINT('Ctrl Pts',(1.46320967827899,-2.77986024775571,11.7363876367123));
#25227=CARTESIAN_POINT('Ctrl Pts',(1.38120000937685,-2.69155501197212,11.7422611918948));
#25228=CARTESIAN_POINT('Ctrl Pts',(1.30317931297184,-2.59970174770958,11.7481347470774));
#25229=CARTESIAN_POINT('Ctrl Pts',(1.22944675547593,-2.50470592042444,11.75400830226));
#25230=CARTESIAN_POINT('Ctrl Pts',(1.15571419798002,-2.40971009313931,11.7598818574426));
#25231=CARTESIAN_POINT('Ctrl Pts',(1.08626997328914,-2.3115720696642,11.7657554126251));
#25232=CARTESIAN_POINT('Ctrl Pts',(1.02136744071989,-2.21072421339481,11.7716289678077));
#25233=CARTESIAN_POINT('Ctrl Pts',(0.956917641603606,-2.11057983041662,
11.7774615514779));
#25234=CARTESIAN_POINT('Ctrl Pts',(0.896751387672808,-2.00746031269782,
11.783294135148));
#25235=CARTESIAN_POINT('Ctrl Pts',(0.841153576985724,-1.90176723709551,
11.7891267188182));
#25236=CARTESIAN_POINT('Ctrl Pts',(0.785623809914929,-1.7962035144118,11.7949521642561));
#25237=CARTESIAN_POINT('Ctrl Pts',(0.734651552095715,-1.68807285619862,
11.800777609694));
#25238=CARTESIAN_POINT('Ctrl Pts',(0.688478265853558,-1.57780544647543,
11.8066030551319));
#25239=CARTESIAN_POINT('Ctrl Pts',(0.642349573470072,-1.46764453229729,
11.8124228743926));
#25240=CARTESIAN_POINT('Ctrl Pts',(0.601010787499888,-1.35535134568636,
11.8182426936533));
#25241=CARTESIAN_POINT('Ctrl Pts',(0.564657024109714,-1.24137976363148,
11.824062512914));
#25242=CARTESIAN_POINT('Ctrl Pts',(0.528095554092989,-1.12675700682539,
11.8299155836159));
#25243=CARTESIAN_POINT('Ctrl Pts',(0.496576444740284,-1.01043698359192,
11.8357686543178));
#25244=CARTESIAN_POINT('Ctrl Pts',(0.470248801469663,-0.892901272263529,
11.8416217250197));
#25245=CARTESIAN_POINT('Ctrl Pts',(0.444098362661862,-0.776156662986079,
11.8474354002376));
#25246=CARTESIAN_POINT('Ctrl Pts',(0.423069797110182,-0.658213085408489,
11.8532490754555));
#25247=CARTESIAN_POINT('Ctrl Pts',(0.407258794977066,-0.539556165137435,
11.8590627506734));
#25248=CARTESIAN_POINT('Ctrl Pts',(0.391449880829969,-0.420914914587281,
11.8648756581428));
#25249=CARTESIAN_POINT('Ctrl Pts',(0.380857213193959,-0.301560911811138,
11.8706885656122));
#25250=CARTESIAN_POINT('Ctrl Pts',(0.375524898252689,-0.181987283819745,
11.8765014730816));
#25251=CARTESIAN_POINT('Ctrl Pts',(0.370192041379855,-0.0624015033722743,
11.882314971326));
#25252=CARTESIAN_POINT('Ctrl Pts',(0.37012061818985,0.0574035403353615,
11.8881284695704));
#25253=CARTESIAN_POINT('Ctrl Pts',(0.375302639045832,0.176932945567398,
11.8939419678147));
#25254=CARTESIAN_POINT('Ctrl Pts',(0.380546481604044,0.297888341065266,
11.8998248213101));
#25255=CARTESIAN_POINT('Ctrl Pts',(0.391169927108912,0.418561051469162,
11.9057076748055));
#25256=CARTESIAN_POINT('Ctrl Pts',(0.407110612018016,0.538442926825278,
11.9115905283009));
#25257=CARTESIAN_POINT('Ctrl Pts',(0.422885536900894,0.65707820437732,11.9174122086438));
#25258=CARTESIAN_POINT('Ctrl Pts',(0.443867509038086,0.774938623117823,
11.9232338889867));
#25259=CARTESIAN_POINT('Ctrl Pts',(0.469944651035495,0.891542353581472,
11.9290555693295));
#25260=CARTESIAN_POINT('Ctrl Pts',(0.496432813792764,1.00998396006323,11.9349690094012));
#25261=CARTESIAN_POINT('Ctrl Pts',(0.528178014589218,1.12712850324347,11.9408824494729));
#25262=CARTESIAN_POINT('Ctrl Pts',(0.565010824631404,1.24248840745856,11.9467958895446));
#25263=CARTESIAN_POINT('Ctrl Pts',(0.60184363467359,1.35784831167365,11.9527093296163));
#25264=CARTESIAN_POINT('Ctrl Pts',(0.643763850064308,1.47142318964377,11.9586227696879));
#25265=CARTESIAN_POINT('Ctrl Pts',(0.690552128350566,1.58274897435054,11.9645362097596));
#25266=CARTESIAN_POINT('Ctrl Pts',(0.736762100003609,1.69269876399826,11.9703765592679));
#25267=CARTESIAN_POINT('Ctrl Pts',(0.78786060021798,1.80078831191609,11.9762169087763));
#25268=CARTESIAN_POINT('Ctrl Pts',(0.843676036575304,1.90655480800833,11.9820572582846));
#25269=CARTESIAN_POINT('Ctrl Pts',(0.899424151962499,2.01219373539217,11.987890563541));
#25270=CARTESIAN_POINT('Ctrl Pts',(0.959877697870534,2.11551482912866,11.9937238687974));
#25271=CARTESIAN_POINT('Ctrl Pts',(1.02481697593313,2.21607505665069,11.9995571740538));
#25272=CARTESIAN_POINT('Ctrl Pts',(1.08969454519933,2.31653972643338,12.0053849361897));
#25273=CARTESIAN_POINT('Ctrl Pts',(1.15904914634169,2.41424841125923,12.0112126983255));
#25274=CARTESIAN_POINT('Ctrl Pts',(1.23261538883901,2.50878301352266,12.0170404604614));
#25275=CARTESIAN_POINT('Ctrl Pts',(1.30646392238179,2.60368036737973,12.0228905850968));
#25276=CARTESIAN_POINT('Ctrl Pts',(1.38455628918227,2.69537886602613,12.0287407097322));
#25277=CARTESIAN_POINT('Ctrl Pts',(1.4665800744481,2.78348496990739,12.0345908343676));
#25278=CARTESIAN_POINT('Ctrl Pts',(1.54820628545173,2.8711640181592,12.0404126030941));
#25279=CARTESIAN_POINT('Ctrl Pts',(1.6337256032797,2.95528512548764,12.0462343718206));
#25280=CARTESIAN_POINT('Ctrl Pts',(1.72279041348928,3.03549432628681,12.0520561405471));
#25281=CARTESIAN_POINT('Ctrl Pts',(1.81184411660245,3.11569352435511,12.0578771832523));
#25282=CARTESIAN_POINT('Ctrl Pts',(1.90444213129456,3.19198151514502,12.0636982259575));
#25283=CARTESIAN_POINT('Ctrl Pts',(2.00020153116519,3.26404267737766,12.0695192686628));
#25284=CARTESIAN_POINT('Ctrl Pts',(2.09597117978909,3.33611155203407,12.0753409343714));
#25285=CARTESIAN_POINT('Ctrl Pts',(2.19490256238751,3.4039524548848,12.08116260008));
#25286=CARTESIAN_POINT('Ctrl Pts',(2.29658186477975,3.46729175355507,12.0869842657886));
#25287=CARTESIAN_POINT('Ctrl Pts',(2.39913328262664,3.53117432091382,12.0928558646155));
#25288=CARTESIAN_POINT('Ctrl Pts',(2.50447963195213,3.59047746520519,12.0987274634424));
#25289=CARTESIAN_POINT('Ctrl Pts',(2.61216996471223,3.64496717085901,12.1045990622693));
#25290=CARTESIAN_POINT('Ctrl Pts',(2.71909463828269,3.69906946435795,12.1104289150687));
#25291=CARTESIAN_POINT('Ctrl Pts',(2.82832967587111,3.74842642925111,12.116258767868));
#25292=CARTESIAN_POINT('Ctrl Pts',(2.93941339388369,3.79285736163026,12.1220886206674));
#25293=CARTESIAN_POINT('Ctrl Pts',(3.05169027339974,3.83776553116915,12.1279810925081));
#25294=CARTESIAN_POINT('Ctrl Pts',(3.16585537848582,3.87764108359278,12.1338735643488));
#25295=CARTESIAN_POINT('Ctrl Pts',(3.28141705662326,3.91234938122126,12.1397660361895));
#25296=CARTESIAN_POINT('Ctrl Pts',(3.39697873476069,3.94705767884974,12.1456585080302));
#25297=CARTESIAN_POINT('Ctrl Pts',(3.51393656328173,3.97659867159665,12.1515509798709));
#25298=CARTESIAN_POINT('Ctrl Pts',(3.63179014717668,4.00089110255627,12.1574434517116));
#25299=CARTESIAN_POINT('Ctrl Pts',(3.74858646128753,4.0249656050288,12.1632830619232));
#25300=CARTESIAN_POINT('Ctrl Pts',(3.86661337411199,4.04395768876275,12.1691226721349));
#25301=CARTESIAN_POINT('Ctrl Pts',(3.9853922655829,4.05774711018526,12.1749622823466));
#25302=CARTESIAN_POINT('Ctrl Pts',(4.10402801852705,4.07151991419836,12.1807948553382));
#25303=CARTESIAN_POINT('Ctrl Pts',(4.22341354767919,4.0801024818754,12.1866274283297));
#25304=CARTESIAN_POINT('Ctrl Pts',(4.34305933324282,4.08342542767631,12.1924600013213));
#25305=CARTESIAN_POINT('Ctrl Pts',(4.46259157484755,4.08674521999865,12.1982870391958));
#25306=CARTESIAN_POINT('Ctrl Pts',(4.58238317807265,4.08481531076132,12.2041140770704));
#25307=CARTESIAN_POINT('Ctrl Pts',(4.70193934339502,4.07761809916772,12.2099411149449));
#25308=CARTESIAN_POINT('Ctrl Pts',(4.82197482259569,4.07039203315751,12.2157915140582));
#25309=CARTESIAN_POINT('Ctrl Pts',(4.941772560987,4.05785629549922,12.2216419131714));
#25310=CARTESIAN_POINT('Ctrl Pts',(5.06083116304306,4.04004597798964,12.2274923122847));
#25311=CARTESIAN_POINT('Ctrl Pts',(5.17929288770721,4.0223249490798,12.2333133815478));
#25312=CARTESIAN_POINT('Ctrl Pts',(5.29702246650312,3.99938217433906,12.2391344508108));
#25313=CARTESIAN_POINT('Ctrl Pts',(5.41353148792556,3.97130414316513,12.2449555200739));
#25314=CARTESIAN_POINT('Ctrl Pts',(5.53002619308032,3.9432295621327,12.250775874062));
#25315=CARTESIAN_POINT('Ctrl Pts',(5.64530024504123,3.91002107494793,12.2565962280501));
#25316=CARTESIAN_POINT('Ctrl Pts',(5.75887688775485,3.87181597839989,12.2624165820382));
#25317=CARTESIAN_POINT('Ctrl Pts',(5.87246591477913,3.8336067159972,12.2682375706733));
#25318=CARTESIAN_POINT('Ctrl Pts',(5.9843567801658,3.79039989023818,12.2740585593084));
#25319=CARTESIAN_POINT('Ctrl Pts',(6.09408989255814,3.74238201686403,12.2798795479434));
#25320=CARTESIAN_POINT('Ctrl Pts',(6.20479586019967,3.69393843388274,12.2857521434201));
#25321=CARTESIAN_POINT('Ctrl Pts',(6.31330523837912,3.64059823779966,12.2916247388968));
#25322=CARTESIAN_POINT('Ctrl Pts',(6.41916973806856,3.58260118206509,12.2974973343735));
#25323=CARTESIAN_POINT('Ctrl Pts',(6.52425214971013,3.52503258728045,12.3033265452713));
#25324=CARTESIAN_POINT('Ctrl Pts',(6.62672831222032,3.46287597121902,12.3091557561691));
#25325=CARTESIAN_POINT('Ctrl Pts',(6.72618822050804,3.3964098901969,12.314984967067));
#25326=CARTESIAN_POINT('Ctrl Pts',(6.82675849166665,3.32920178688851,12.3208792548331));
#25327=CARTESIAN_POINT('Ctrl Pts',(6.92424440711328,3.25758766316226,12.3267735425991));
#25328=CARTESIAN_POINT('Ctrl Pts',(7.01825653981374,3.1818972555807,12.3326678303652));
#25329=CARTESIAN_POINT('Ctrl Pts',(7.11226867251421,3.10620684799914,12.3385621181313));
#25330=CARTESIAN_POINT('Ctrl Pts',(7.20280674160711,3.02644047770949,12.3444564058974));
#25331=CARTESIAN_POINT('Ctrl Pts',(7.28952047817893,2.94296532834342,12.3503506936635));
#25332=CARTESIAN_POINT('Ctrl Pts',(7.37417408452558,2.86147336739775,12.356104945942));
#25333=CARTESIAN_POINT('Ctrl Pts',(7.45545512726984,2.77618466306006,12.3618591982205));
#25334=CARTESIAN_POINT('Ctrl Pts',(7.53299895384682,2.6874130863435,12.3676134504989));
#25335=CARTESIAN_POINT('Ctrl Pts',(7.58988491127993,2.62229047946061,12.3718347555934));
#25336=CARTESIAN_POINT('Ctrl Pts',(7.64476020971441,2.55529442644394,12.3760560606879));
#25337=CARTESIAN_POINT('Ctrl Pts',(7.69749241145744,2.48656247355586,12.3802773657823));
#25338=CARTESIAN_POINT('Origin',(4.45646910621825,2.93978508838399E-15,
8.23961502859548));
#25339=CARTESIAN_POINT('',(7.69749241145743,2.48656247355587,13.7345026286438));
#25340=CARTESIAN_POINT('',(7.69749241145744,2.48656247355586,13.6301247167396));
#25341=CARTESIAN_POINT('',(7.69749241145744,2.48656247355586,8.23961502859548));
#25342=CARTESIAN_POINT('',(8.53966035999323,0.000944551248266404,12.6146148317601));
#25343=CARTESIAN_POINT('Ctrl Pts',(8.54146899785629,0.000940912841063322,
12.6146150285955));
#25344=CARTESIAN_POINT('Ctrl Pts',(8.54149739908273,-0.122363820490929,
12.6205921772503));
#25345=CARTESIAN_POINT('Ctrl Pts',(8.53593857126231,-0.245616423183125,
12.6265693259052));
#25346=CARTESIAN_POINT('Ctrl Pts',(8.52483281598515,-0.368295703275901,
12.63254647456));
#25347=CARTESIAN_POINT('Ctrl Pts',(8.51371936793932,-0.491059961229144,
12.6385277634846));
#25348=CARTESIAN_POINT('Ctrl Pts',(8.497051368911,-0.613249733963977,12.6445090524091));
#25349=CARTESIAN_POINT('Ctrl Pts',(8.47492076633568,-0.734350907468087,
12.6504903413336));
#25350=CARTESIAN_POINT('Ctrl Pts',(8.45275362077154,-0.855652048361935,
12.6564815068159));
#25351=CARTESIAN_POINT('Ctrl Pts',(8.42510591433828,-0.975860630413129,
12.6624726722982));
#25352=CARTESIAN_POINT('Ctrl Pts',(8.39212056454292,-1.09447366281089,12.6684638377805));
#25353=CARTESIAN_POINT('Ctrl Pts',(8.35910742797959,-1.21318661450097,12.6744600502041));
#25354=CARTESIAN_POINT('Ctrl Pts',(8.32074779667736,-1.33030098168081,12.6804562626277));
#25355=CARTESIAN_POINT('Ctrl Pts',(8.27723367032645,-1.44533150026379,12.6864524750513));
#25356=CARTESIAN_POINT('Ctrl Pts',(8.23363451074585,-1.56058680599821,12.6924604049872));
#25357=CARTESIAN_POINT('Ctrl Pts',(8.18486086695445,-1.6737497790333,12.698468334923));
#25358=CARTESIAN_POINT('Ctrl Pts',(8.13115235600658,-1.78435647047467,12.7044762648589));
#25359=CARTESIAN_POINT('Ctrl Pts',(8.08317463101388,-1.88316124704867,12.709843138845));
#25360=CARTESIAN_POINT('Ctrl Pts',(8.03125970788008,-1.97992633993934,12.7152100128311));
#25361=CARTESIAN_POINT('Ctrl Pts',(7.97560775666991,-2.07434041538437,12.7205768868172));
#25362=CARTESIAN_POINT('Ctrl Pts',(7.91506111829492,-2.17705837511755,12.7264157868265));
#25363=CARTESIAN_POINT('Ctrl Pts',(7.84992221231509,-2.27727814488456,12.7322546868358));
#25364=CARTESIAN_POINT('Ctrl Pts',(7.78042299958556,-2.37456427892951,12.7380935868451));
#25365=CARTESIAN_POINT('Ctrl Pts',(7.71100774001232,-2.47173289397395,12.7439254336223));
#25366=CARTESIAN_POINT('Ctrl Pts',(7.63724288563745,-2.56597459541495,12.7497572803994));
#25367=CARTESIAN_POINT('Ctrl Pts',(7.55940542000314,-2.65687998084121,12.7555891271765));
#25368=CARTESIAN_POINT('Ctrl Pts',(7.48164203103285,-2.74769885307438,12.7614154238789));
#25369=CARTESIAN_POINT('Ctrl Pts',(7.39981400514475,-2.83518742029049,12.7672417205812));
#25370=CARTESIAN_POINT('Ctrl Pts',(7.31424026387788,-2.91896711362915,12.7730680172836));
#25371=CARTESIAN_POINT('Ctrl Pts',(7.22830852049806,-3.00309730358971,12.7789186885955));
#25372=CARTESIAN_POINT('Ctrl Pts',(7.13859989320791,-3.08348718220274,12.7847693599074));
#25373=CARTESIAN_POINT('Ctrl Pts',(7.04547699114638,-3.15978846946749,12.7906200312193));
#25374=CARTESIAN_POINT('Ctrl Pts',(6.9528375560705,-3.23569362267136,12.7964403275497));
#25375=CARTESIAN_POINT('Ctrl Pts',(6.85681953659431,-3.30755228477065,12.8022606238802));
#25376=CARTESIAN_POINT('Ctrl Pts',(6.7578147457841,-3.37506048053231,12.8080809202106));
#25377=CARTESIAN_POINT('Ctrl Pts',(6.65882230146167,-3.4425602576194,12.8139004907154));
#25378=CARTESIAN_POINT('Ctrl Pts',(6.55684416186541,-3.50571041914857,12.8197200612202));
#25379=CARTESIAN_POINT('Ctrl Pts',(6.45230198519655,-3.56424972738849,12.8255396317249));
#25380=CARTESIAN_POINT('Ctrl Pts',(6.34774858125766,-3.62279532243668,12.8313598272204));
#25381=CARTESIAN_POINT('Ctrl Pts',(6.24063094669848,-3.6767288814336,12.8371800227159));
#25382=CARTESIAN_POINT('Ctrl Pts',(6.13139570863319,-3.7258349234128,12.8430002182114));
#25383=CARTESIAN_POINT('Ctrl Pts',(6.02115704689783,-3.77539204844669,12.8488738774246));
#25384=CARTESIAN_POINT('Ctrl Pts',(5.9087620595364,-3.82003233393355,12.8547475366377));
#25385=CARTESIAN_POINT('Ctrl Pts',(5.79468971302631,-3.85958425319541,12.8606211958508));
#25386=CARTESIAN_POINT('Ctrl Pts',(5.68149632363534,-3.89883141462531,12.866449596991));
#25387=CARTESIAN_POINT('Ctrl Pts',(5.56665174243832,-3.93306829066049,12.8722779981312));
#25388=CARTESIAN_POINT('Ctrl Pts',(5.45063755135768,-3.96217794939712,12.8781063992714));
#25389=CARTESIAN_POINT('Ctrl Pts',(5.33327206892005,-3.99162666691517,12.884002687521));
#25390=CARTESIAN_POINT('Ctrl Pts',(5.21470997644599,-4.01582788214008,12.8898989757706));
#25391=CARTESIAN_POINT('Ctrl Pts',(5.09545770703646,-4.03471418665859,12.8957952640202));
#25392=CARTESIAN_POINT('Ctrl Pts',(4.97620543762694,-4.0536004911771,12.9016915522699));
#25393=CARTESIAN_POINT('Ctrl Pts',(4.85626341900325,-4.06717189238334,12.9075878405195));
#25394=CARTESIAN_POINT('Ctrl Pts',(4.73613955864215,-4.07541524731416,12.9134841287691));
#25395=CARTESIAN_POINT('Ctrl Pts',(4.6171857401835,-4.08357830953164,12.9193229854285));
#25396=CARTESIAN_POINT('Ctrl Pts',(4.49769483746589,-4.08654131907336,12.9251618420879));
#25397=CARTESIAN_POINT('Ctrl Pts',(4.37815714466965,-4.0842492867941,12.9310006987474));
#25398=CARTESIAN_POINT('Ctrl Pts',(4.25876385934941,-4.08196002340379,12.9368325017776));
#25399=CARTESIAN_POINT('Ctrl Pts',(4.13932429883191,-4.07442835476718,12.9426643048079));
#25400=CARTESIAN_POINT('Ctrl Pts',(4.0203327442935,-4.06165115117076,12.9484961078382));
#25401=CARTESIAN_POINT('Ctrl Pts',(3.90145443980128,-4.04888610826005,12.9543223604581));
#25402=CARTESIAN_POINT('Ctrl Pts',(3.7830236942198,-4.03088550700644,12.960148613078));
#25403=CARTESIAN_POINT('Ctrl Pts',(3.66553308053823,-4.00769824254287,12.9659748656978));
#25404=CARTESIAN_POINT('Ctrl Pts',(3.54754971553969,-3.98441373154409,12.9718255534071));
#25405=CARTESIAN_POINT('Ctrl Pts',(3.43051479968968,-3.95589896446489,12.9776762411164));
#25406=CARTESIAN_POINT('Ctrl Pts',(3.31492065169473,-3.92225599954601,12.9835269288257));
#25407=CARTESIAN_POINT('Ctrl Pts',(3.19992783839306,-3.88878804938646,12.9893471805522));
#25408=CARTESIAN_POINT('Ctrl Pts',(3.08636122927721,-3.85024525281661,12.9951674322787));
#25409=CARTESIAN_POINT('Ctrl Pts',(2.97469310746983,-3.80677880753963,13.0009876840053));
#25410=CARTESIAN_POINT('Ctrl Pts',(2.86303891359544,-3.76331778366427,13.0068072097943));
#25411=CARTESIAN_POINT('Ctrl Pts',(2.75328311394058,-3.7149344798687,13.0126267355833));
#25412=CARTESIAN_POINT('Ctrl Pts',(2.64587962648191,-3.66182887856162,13.0184462613723));
#25413=CARTESIAN_POINT('Ctrl Pts',(2.53846460544612,-3.60871757448302,13.024266412094));
#25414=CARTESIAN_POINT('Ctrl Pts',(2.43340276250765,-3.55088314442774,13.0300865628157));
#25415=CARTESIAN_POINT('Ctrl Pts',(2.33112440253129,-3.48857204175426,13.0359067135374));
#25416=CARTESIAN_POINT('Ctrl Pts',(2.22790463662733,-3.42568740581896,13.0417804349694));
#25417=CARTESIAN_POINT('Ctrl Pts',(2.12752021954158,-3.3582434783766,13.0476541564013));
#25418=CARTESIAN_POINT('Ctrl Pts',(2.03038352020519,-3.28653825922343,13.0535278778333));
#25419=CARTESIAN_POINT('Ctrl Pts',(1.93399704139872,-3.21538684442926,13.0593562344708));
#25420=CARTESIAN_POINT('Ctrl Pts',(1.84080856978275,-3.14004003365009,13.0651845911082));
#25421=CARTESIAN_POINT('Ctrl Pts',(1.75118690683325,-3.06082884554011,13.0710129477457));
#25422=CARTESIAN_POINT('Ctrl Pts',(1.66051889362329,-2.98069285147827,13.0769093515749));
#25423=CARTESIAN_POINT('Ctrl Pts',(1.57350181411223,-2.89660196789241,13.0828057554041));
#25424=CARTESIAN_POINT('Ctrl Pts',(1.49047771052929,-2.80893574876657,13.0887021592333));
#25425=CARTESIAN_POINT('Ctrl Pts',(1.40745360694636,-2.72126952964073,13.0945985630626));
#25426=CARTESIAN_POINT('Ctrl Pts',(1.32842271513739,-2.63002833195273,13.1004949668918));
#25427=CARTESIAN_POINT('Ctrl Pts',(1.25368315383551,-2.53562362018094,13.106391370721));
#25428=CARTESIAN_POINT('Ctrl Pts',(1.17967308579315,-2.44214034278348,13.1122302228765));
#25429=CARTESIAN_POINT('Ctrl Pts',(1.10964768046145,-2.34527308168121,13.1180690750319));
#25430=CARTESIAN_POINT('Ctrl Pts',(1.04392958940042,-2.24539507573978,13.1239079271874));
#25431=CARTESIAN_POINT('Ctrl Pts',(0.978290892232233,-2.14563773221525,
13.1297397254374));
#25432=CARTESIAN_POINT('Ctrl Pts',(0.916949378879206,-2.04287721577925,
13.1355715236874));
#25433=CARTESIAN_POINT('Ctrl Pts',(0.860187187972853,-1.93751938429037,
13.1414033219374));
#25434=CARTESIAN_POINT('Ctrl Pts',(0.803479023060019,-1.8322618319033,13.1472295695085));
#25435=CARTESIAN_POINT('Ctrl Pts',(0.751341699701744,-1.7244122386103,13.1530558170796));
#25436=CARTESIAN_POINT('Ctrl Pts',(0.704013486062314,-1.61440447805371,
13.1588820646507));
#25437=CARTESIAN_POINT('Ctrl Pts',(0.656486723895358,-1.50393521943507,
13.1647327541516));
#25438=CARTESIAN_POINT('Ctrl Pts',(0.61380973751515,-1.39128999224299,13.1705834436526));
#25439=CARTESIAN_POINT('Ctrl Pts',(0.576176808876447,-1.27693253039838,
13.1764341331535));
#25440=CARTESIAN_POINT('Ctrl Pts',(0.538739699238071,-1.16317011562208,
13.1822543792047));
#25441=CARTESIAN_POINT('Ctrl Pts',(0.506294399078778,-1.04771363468968,
13.188074625256));
#25442=CARTESIAN_POINT('Ctrl Pts',(0.478983332969678,-0.931038089234241,
13.1938948713072));
#25443=CARTESIAN_POINT('Ctrl Pts',(0.451675674329161,-0.814377100817839,
13.1997143911948));
#25444=CARTESIAN_POINT('Ctrl Pts',(0.429501067866308,-0.696497745366419,
13.2055339110823));
#25445=CARTESIAN_POINT('Ctrl Pts',(0.412551318847235,-0.577887470866143,
13.2113534309698));
#25446=CARTESIAN_POINT('Ctrl Pts',(0.395599750310187,-0.459264463815885,
13.2171735755699));
#25447=CARTESIAN_POINT('Ctrl Pts',(0.383874211789774,-0.339910783308017,
13.22299372017));
#25448=CARTESIAN_POINT('Ctrl Pts',(0.377414829203158,-0.220320687100959,
13.22881386477));
#25449=CARTESIAN_POINT('Ctrl Pts',(0.37089597694503,-0.0996295593878255,
13.234687593762));
#25450=CARTESIAN_POINT('Ctrl Pts',(0.369740775116918,0.0213019396648289,
13.2405613227539));
#25451=CARTESIAN_POINT('Ctrl Pts',(0.373936695342714,0.141965186403322,
13.2464350517458));
#25452=CARTESIAN_POINT('Ctrl Pts',(0.378100198935577,0.261696218998671,
13.2522634017728));
#25453=CARTESIAN_POINT('Ctrl Pts',(0.387532339693921,0.381162726950705,
13.2580917517998));
#25454=CARTESIAN_POINT('Ctrl Pts',(0.402168717863373,0.499873344943745,
13.2639201018268));
#25455=CARTESIAN_POINT('Ctrl Pts',(0.41697603215237,0.619970366878633,13.2698165203012));
#25456=CARTESIAN_POINT('Ctrl Pts',(0.437109846561945,0.739293308218146,
13.2757129387755));
#25457=CARTESIAN_POINT('Ctrl Pts',(0.462450598692844,0.857345415538152,
13.2816093572499));
#25458=CARTESIAN_POINT('Ctrl Pts',(0.487791350823743,0.975397522858159,
13.2875057757243));
#25459=CARTESIAN_POINT('Ctrl Pts',(0.518338879667798,1.09217839974952,13.2934021941986));
#25460=CARTESIAN_POINT('Ctrl Pts',(0.553922463351789,1.20720946825788,13.299298612673));
#25461=CARTESIAN_POINT('Ctrl Pts',(0.589158638859341,1.32111747018309,13.3051374634777));
#25462=CARTESIAN_POINT('Ctrl Pts',(0.629439213296274,1.43365326605997,13.3109763142825));
#25463=CARTESIAN_POINT('Ctrl Pts',(0.67463886394955,1.54433967075305,13.3168151650872));
#25464=CARTESIAN_POINT('Ctrl Pts',(0.719783911027166,1.65489236039775,13.3226469622504));
#25465=CARTESIAN_POINT('Ctrl Pts',(0.769836060649829,1.76359973066888,13.3284787594137));
#25466=CARTESIAN_POINT('Ctrl Pts',(0.824620176145967,1.86999955859155,13.3343105565769));
#25467=CARTESIAN_POINT('Ctrl Pts',(0.879352150831858,1.97629812042298,13.3401368033242));
#25468=CARTESIAN_POINT('Ctrl Pts',(0.938806945629637,2.08029315087318,13.3459630500714));
#25469=CARTESIAN_POINT('Ctrl Pts',(1.00276150719696,2.18154276154798,13.3517892968187));
#25470=CARTESIAN_POINT('Ctrl Pts',(1.0669843807211,2.28321715007287,13.3576399867273));
#25471=CARTESIAN_POINT('Ctrl Pts',(1.13574470350305,2.38212264872249,13.3634906766359));
#25472=CARTESIAN_POINT('Ctrl Pts',(1.20876991878967,2.47783675571566,13.3693413665445));
#25473=CARTESIAN_POINT('Ctrl Pts',(1.28141514775869,2.57305281486445,13.3751616124194));
#25474=CARTESIAN_POINT('Ctrl Pts',(1.35828073431569,2.66511029600926,13.3809818582943));
#25475=CARTESIAN_POINT('Ctrl Pts',(1.43905549995296,2.75362309126083,13.3868021041692));
#25476=CARTESIAN_POINT('Ctrl Pts',(1.51982019110276,2.8421248469131,13.3926216241244));
#25477=CARTESIAN_POINT('Ctrl Pts',(1.60449281800116,2.92708249657188,13.3984411440796));
#25478=CARTESIAN_POINT('Ctrl Pts',(1.69272330849149,3.00814463840212,13.4042606640348));
#25479=CARTESIAN_POINT('Ctrl Pts',(1.78096327402854,3.0892154854722,13.4100808089466));
#25480=CARTESIAN_POINT('Ctrl Pts',(1.87276156410223,3.16638971847438,13.4159009538584));
#25481=CARTESIAN_POINT('Ctrl Pts',(1.9677332618258,3.23935470376987,13.4217210987701));
#25482=CARTESIAN_POINT('Ctrl Pts',(2.06357934224492,3.31299146099376,13.4275948284247));
#25483=CARTESIAN_POINT('Ctrl Pts',(2.16265723391086,3.38234080424751,13.4334685580792));
#25484=CARTESIAN_POINT('Ctrl Pts',(2.26454039229395,3.44712539851308,13.4393422877338));
#25485=CARTESIAN_POINT('Ctrl Pts',(2.36563643116316,3.51140948593184,13.4451706386692));
#25486=CARTESIAN_POINT('Ctrl Pts',(2.46949415929186,3.57119895695132,13.4509989896046));
#25487=CARTESIAN_POINT('Ctrl Pts',(2.57567192763767,3.62626901553692,13.4568273405401));
#25488=CARTESIAN_POINT('Ctrl Pts',(2.68308972369881,3.68198222569742,13.4627237595542));
#25489=CARTESIAN_POINT('Ctrl Pts',(2.79288170743545,3.7328649066331,13.4686201785683));
#25490=CARTESIAN_POINT('Ctrl Pts',(2.90457058759781,3.7787347072669,13.4745165975825));
#25491=CARTESIAN_POINT('Ctrl Pts',(3.01625946776017,3.8246045079007,13.4804130165966));
#25492=CARTESIAN_POINT('Ctrl Pts',(3.12984482636902,3.86546133681569,13.4863094356108));
#25493=CARTESIAN_POINT('Ctrl Pts',(3.24483542673019,3.90117531350874,13.4922058546249));
#25494=CARTESIAN_POINT('Ctrl Pts',(3.35870348020416,3.93654064767587,13.4980447123533));
#25495=CARTESIAN_POINT('Ctrl Pts',(3.47429291146674,3.96696980476108,13.5038835700816));
#25496=CARTESIAN_POINT('Ctrl Pts',(3.59113930905819,3.99229624929648,13.50972242781));
#25497=CARTESIAN_POINT('Ctrl Pts',(3.70784454623759,4.01759209732723,13.5155542317003));
#25498=CARTESIAN_POINT('Ctrl Pts',(3.82580333555408,4.03779741068712,13.5213860355906));
#25499=CARTESIAN_POINT('Ctrl Pts',(3.94453543076624,4.0527951973839,13.527217839481));
#25500=CARTESIAN_POINT('Ctrl Pts',(4.063154518653,4.06777870942512,13.5330440927528));
#25501=CARTESIAN_POINT('Ctrl Pts',(4.18254504751353,4.07756450613422,13.5388703460247));
#25502=CARTESIAN_POINT('Ctrl Pts',(4.30221643997545,4.08208661286808,13.5446965992966));
#25503=CARTESIAN_POINT('Ctrl Pts',(4.42238970978578,4.08662768439285,13.5505472866832));
#25504=CARTESIAN_POINT('Ctrl Pts',(4.54284579927312,4.08586073163649,13.5563979740699));
#25505=CARTESIAN_POINT('Ctrl Pts',(4.66308212298528,4.07977156974532,13.5622486614566));
#25506=CARTESIAN_POINT('Ctrl Pts',(4.78269297231005,4.07371408392912,13.5680689133226));
#25507=CARTESIAN_POINT('Ctrl Pts',(4.90208592820469,4.06238965990478,13.5738891651887));
#25508=CARTESIAN_POINT('Ctrl Pts',(5.02076657283072,4.04583654751085,13.5797094170548));
#25509=CARTESIAN_POINT('Ctrl Pts',(5.13943241094131,4.02928550027182,13.5855289427902));
#25510=CARTESIAN_POINT('Ctrl Pts',(5.25738571286766,4.00750711838774,13.5913484685257));
#25511=CARTESIAN_POINT('Ctrl Pts',(5.3741386848926,3.98059135611474,13.5971679942611));
#25512=CARTESIAN_POINT('Ctrl Pts',(5.49090419061957,3.95367270437232,13.6029881447361));
#25513=CARTESIAN_POINT('Ctrl Pts',(5.60646871493071,3.92161566681467,13.6088082952112));
#25514=CARTESIAN_POINT('Ctrl Pts',(5.72035672823374,3.88456086049837,13.6146284456862));
#25515=CARTESIAN_POINT('Ctrl Pts',(5.83529300139865,3.84716499049131,13.6205021665937));
#25516=CARTESIAN_POINT('Ctrl Pts',(5.94852134084145,3.80467900203611,13.6263758875013));
#25517=CARTESIAN_POINT('Ctrl Pts',(6.05957178679717,3.75729780500834,13.6322496084088));
#25518=CARTESIAN_POINT('Ctrl Pts',(6.16976454776242,3.7102825510542,13.6380779643274));
#25519=CARTESIAN_POINT('Ctrl Pts',(6.27781259618175,3.6584476694299,13.6439063202459));
#25520=CARTESIAN_POINT('Ctrl Pts',(6.3832807544057,3.60203024312803,13.6497346761645));
#25521=CARTESIAN_POINT('Ctrl Pts',(6.48998027922065,3.54495412954965,13.6556310795665));
#25522=CARTESIAN_POINT('Ctrl Pts',(6.59403892002381,3.48318800327208,13.6615274829686));
#25523=CARTESIAN_POINT('Ctrl Pts',(6.69503634868013,3.41702234423136,13.6674238863706));
#25524=CARTESIAN_POINT('Ctrl Pts',(6.79603377733645,3.35085668519065,13.6733202897727));
#25525=CARTESIAN_POINT('Ctrl Pts',(6.89396968205752,3.28029178637921,13.6792166931748));
#25526=CARTESIAN_POINT('Ctrl Pts',(6.9884591187628,3.20565930447614,13.6851130965768));
#25527=CARTESIAN_POINT('Ctrl Pts',(7.08114847821915,3.13244861359426,13.6908971701568));
#25528=CARTESIAN_POINT('Ctrl Pts',(7.17081330379056,3.05509332019825,13.6966812437367));
#25529=CARTESIAN_POINT('Ctrl Pts',(7.25705769295394,2.97387433625659,13.7024653173167));
#25530=CARTESIAN_POINT('Ctrl Pts',(7.34318780350787,2.89276297198312,13.7082417266777));
#25531=CARTESIAN_POINT('Ctrl Pts',(7.42590619518058,2.80779838380308,13.7140181360387));
#25532=CARTESIAN_POINT('Ctrl Pts',(7.50484862644894,2.7193027232432,13.7197945453996));
#25533=CARTESIAN_POINT('Ctrl Pts',(7.5718505635827,2.64419253737513,13.7246972398143));
#25534=CARTESIAN_POINT('Ctrl Pts',(7.63613282774662,2.56653948717263,13.7295999342291));
#25535=CARTESIAN_POINT('Ctrl Pts',(7.69749241145743,2.48656247355587,13.7345026286438));
#25536=CARTESIAN_POINT('Ctrl Pts',(7.69775011106531,2.486760611716,12.4842647253843));
#25537=CARTESIAN_POINT('Ctrl Pts',(7.88067047589132,2.25281987648989,12.4987330318779));
#25538=CARTESIAN_POINT('Ctrl Pts',(8.35218024080415,1.49234549316982,12.5421829289241));
#25539=CARTESIAN_POINT('Ctrl Pts',(8.53713895924919,0.59800099527881,12.5856328259703));
#25540=CARTESIAN_POINT('Ctrl Pts',(8.53584491900118,0.000952226708496463,
12.6146144165228));
#25541=CARTESIAN_POINT('',(8.54146807353351,-0.00290465713063073,12.5103849713801));
#25542=CARTESIAN_POINT('Ctrl Pts',(7.69749241145744,2.48656247355586,12.3802773657823));
#25543=CARTESIAN_POINT('Ctrl Pts',(7.76924068774468,2.39304468020431,12.3860209409451));
#25544=CARTESIAN_POINT('Ctrl Pts',(7.83701986349459,2.29631207426909,12.3917645161079));
#25545=CARTESIAN_POINT('Ctrl Pts',(7.90052900384754,2.19674222919793,12.3975080912707));
#25546=CARTESIAN_POINT('Ctrl Pts',(7.96399713349499,2.09723668084958,12.4032479575489));
#25547=CARTESIAN_POINT('Ctrl Pts',(8.02320048347776,1.99489788651667,12.4089878238271));
#25548=CARTESIAN_POINT('Ctrl Pts',(8.07788012219632,1.8901341892449,12.4147276901054));
#25549=CARTESIAN_POINT('Ctrl Pts',(8.13253810792986,1.78541197810618,12.4204652834125));
#25550=CARTESIAN_POINT('Ctrl Pts',(8.18267575054377,1.67826714401205,12.4262028767196));
#25551=CARTESIAN_POINT('Ctrl Pts',(8.22807936496054,1.56913385539592,12.4319404700267));
#25552=CARTESIAN_POINT('Ctrl Pts',(8.27347633802212,1.46001653011095,12.4376772240748));
#25553=CARTESIAN_POINT('Ctrl Pts',(8.31414050054795,1.3489117158947,12.4434139781229));
#25554=CARTESIAN_POINT('Ctrl Pts',(8.34990605934031,1.23627411687835,12.4491507321709));
#25555=CARTESIAN_POINT('Ctrl Pts',(8.38568972458393,1.12357949464567,12.4548903904727));
#25556=CARTESIAN_POINT('Ctrl Pts',(8.41656970369862,1.00935093669711,12.4606300487745));
#25557=CARTESIAN_POINT('Ctrl Pts',(8.44242997616946,0.894058691148153,12.4663697070763));
#25558=CARTESIAN_POINT('Ctrl Pts',(8.46829731461118,0.778734943547124,12.4721109336624));
#25559=CARTESIAN_POINT('Ctrl Pts',(8.48914213702818,0.662347341222967,12.4778521602484));
#25560=CARTESIAN_POINT('Ctrl Pts',(8.50489977007518,0.545375246910505,12.4835933868345));
#25561=CARTESIAN_POINT('Ctrl Pts',(8.52067402217595,0.428279786003641,12.4893406685021));
#25562=CARTESIAN_POINT('Ctrl Pts',(8.53135033061166,0.310599019056449,12.4950879501697));
#25563=CARTESIAN_POINT('Ctrl Pts',(8.53691600221979,0.192816308727098,12.5008352318374));
#25564=CARTESIAN_POINT('Ctrl Pts',(8.53999866038249,0.127580006806133,12.5040184783516));
#25565=CARTESIAN_POINT('Ctrl Pts',(8.54151444644693,0.0623124390438113,
12.5072017248658));
#25566=CARTESIAN_POINT('Ctrl Pts',(8.54146807353351,-0.00290465713062882,
12.5103849713801));
#25567=CARTESIAN_POINT('Ctrl Pts',(8.54146807353315,-0.00290465763095525,
12.5103849714045));
#25568=CARTESIAN_POINT('Ctrl Pts',(8.54134087188272,-0.181796174867856,
12.5191166664979));
#25569=CARTESIAN_POINT('Ctrl Pts',(8.52945913442029,-0.360258821209145,
12.5278483615914));
#25570=CARTESIAN_POINT('Ctrl Pts',(8.50601097951343,-0.53706202288814,12.5365800566848));
#25571=CARTESIAN_POINT('Ctrl Pts',(8.50003337196073,-0.582134232530938,
12.5388060163284));
#25572=CARTESIAN_POINT('Ctrl Pts',(8.4933043018107,-0.627098745221606,12.5410319759719));
#25573=CARTESIAN_POINT('Ctrl Pts',(8.48582734134787,-0.671935423231146,
12.5432579356155));
#25574=CARTESIAN_POINT('Ctrl Pts',(8.46621380814478,-0.789550820186742,
12.5490970641751));
#25575=CARTESIAN_POINT('Ctrl Pts',(8.44141674655492,-0.906483969071624,
12.5549361927347));
#25576=CARTESIAN_POINT('Ctrl Pts',(8.41149627214712,-1.02224513535862,12.5607753212943));
#25577=CARTESIAN_POINT('Ctrl Pts',(8.38161192889726,-1.13786651158331,12.5666073986797));
#25578=CARTESIAN_POINT('Ctrl Pts',(8.34661658124467,-1.25231833093802,12.5724394760652));
#25579=CARTESIAN_POINT('Ctrl Pts',(8.30662171669774,-1.36511899701738,12.5782715534506));
#25580=CARTESIAN_POINT('Ctrl Pts',(8.26666490120857,-1.47781235034275,12.5840980824975));
#25581=CARTESIAN_POINT('Ctrl Pts',(8.22171816737487,-1.58885729550491,12.5899246115443));
#25582=CARTESIAN_POINT('Ctrl Pts',(8.17194321602948,-1.69778595215126,12.5957511405912));
#25583=CARTESIAN_POINT('Ctrl Pts',(8.12196276023786,-1.80716433948863,12.6016017254652));
#25584=CARTESIAN_POINT('Ctrl Pts',(8.06711423663364,-1.91440852484665,12.6074523103392));
#25585=CARTESIAN_POINT('Ctrl Pts',(8.00761096041533,-2.01906328067485,12.6133028952132));
#25586=CARTESIAN_POINT('Ctrl Pts',(7.94841334308679,-2.12318044162577,12.6191234265609));
#25587=CARTESIAN_POINT('Ctrl Pts',(7.88460889250782,-2.22473436194133,12.6249439579086));
#25588=CARTESIAN_POINT('Ctrl Pts',(7.81645412473464,-2.32330059943718,12.6307644892563));
#25589=CARTESIAN_POINT('Ctrl Pts',(7.74830784934303,-2.42185455514957,12.6365842953404));
#25590=CARTESIAN_POINT('Ctrl Pts',(7.67581256576471,-2.51742123506149,12.6424041014245));
#25591=CARTESIAN_POINT('Ctrl Pts',(7.59926799309304,-2.60960536416108,12.6482239075086));
#25592=CARTESIAN_POINT('Ctrl Pts',(7.5227151965993,-2.70179939737079,12.654044338863));
#25593=CARTESIAN_POINT('Ctrl Pts',(7.44211250513552,-2.79060984511978,12.6598647702174));
#25594=CARTESIAN_POINT('Ctrl Pts',(7.35779937464784,-2.87567516828553,12.6656852015718));
#25595=CARTESIAN_POINT('Ctrl Pts',(7.27271994995913,-2.96151362208319,12.6715585329048));
#25596=CARTESIAN_POINT('Ctrl Pts',(7.1838625901503,-3.04353822672158,12.6774318642378));
#25597=CARTESIAN_POINT('Ctrl Pts',(7.09161260727117,-3.12141694248914,12.6833051955707));
#25598=CARTESIAN_POINT('Ctrl Pts',(7.00006464315778,-3.19870300427225,12.6891338310817));
#25599=CARTESIAN_POINT('Ctrl Pts',(6.90517587314553,-3.27190585709956,12.6949624665927));
#25600=CARTESIAN_POINT('Ctrl Pts',(6.80735376868783,-3.34074337592175,12.7007911021037));
#25601=CARTESIAN_POINT('Ctrl Pts',(6.70840646794043,-3.41037269656827,12.7066867813476));
#25602=CARTESIAN_POINT('Ctrl Pts',(6.60645828806868,-3.47553539771189,12.7125824605916));
#25603=CARTESIAN_POINT('Ctrl Pts',(6.50195748839191,-3.53598674748539,12.7184781398355));
#25604=CARTESIAN_POINT('Ctrl Pts',(6.39745668871515,-3.59643809725888,12.7243738190795));
#25605=CARTESIAN_POINT('Ctrl Pts',(6.29040367073468,-3.6521779490307,12.7302694983234));
#25606=CARTESIAN_POINT('Ctrl Pts',(6.1812675513243,-3.70301165590381,12.7361651775674));
#25607=CARTESIAN_POINT('Ctrl Pts',(6.07318232100037,-3.75335587691225,12.7420040863763));
#25608=CARTESIAN_POINT('Ctrl Pts',(5.96272810830869,-3.79903982898839,12.7478429951853));
#25609=CARTESIAN_POINT('Ctrl Pts',(5.85034275302209,-3.83983609764082,12.7536819039942));
#25610=CARTESIAN_POINT('Ctrl Pts',(5.73809313555261,-3.88058309300103,12.7595137606322));
#25611=CARTESIAN_POINT('Ctrl Pts',(5.62391739373644,-3.91645401109673,12.7653456172702));
#25612=CARTESIAN_POINT('Ctrl Pts',(5.50827571355101,-3.94726840495689,12.7711774739082));
#25613=CARTESIAN_POINT('Ctrl Pts',(5.3927440668114,-3.97805347881813,12.7770037815151));
#25614=CARTESIAN_POINT('Ctrl Pts',(5.2757496470666,-4.00379149764778,12.782830089122));
#25615=CARTESIAN_POINT('Ctrl Pts',(5.15776973081019,-4.02435118173684,12.7886563967289));
#25616=CARTESIAN_POINT('Ctrl Pts',(5.03929653612431,-4.04499682663176,12.7945070643452));
#25617=CARTESIAN_POINT('Ctrl Pts',(4.91982997550732,-4.06042059919596,12.8003577319614));
#25618=CARTESIAN_POINT('Ctrl Pts',(4.79986616233747,-4.07054092988246,12.8062083995777));
#25619=CARTESIAN_POINT('Ctrl Pts',(4.680524816102,-4.08060874830672,12.8120287093132));
#25620=CARTESIAN_POINT('Ctrl Pts',(4.56069177431652,-4.085428005872,12.8178490190487));
#25621=CARTESIAN_POINT('Ctrl Pts',(4.44086211976386,-4.08497018617927,12.8236693287843));
#25622=CARTESIAN_POINT('Ctrl Pts',(4.32104738966884,-4.08451242350675,12.829488913616));
#25623=CARTESIAN_POINT('Ctrl Pts',(4.20123645154675,-4.07877889260651,12.8353084984478));
#25624=CARTESIAN_POINT('Ctrl Pts',(4.08192476980127,-4.06779320271541,12.8411280832795));
#25625=CARTESIAN_POINT('Ctrl Pts',(3.96260025600268,-4.05680633130584,12.8469482940116));
#25626=CARTESIAN_POINT('Ctrl Pts',(3.84377550930107,-4.04056621496815,12.8527685047437));
#25627=CARTESIAN_POINT('Ctrl Pts',(3.72594064703243,-4.01914831404855,12.8585887154758));
#25628=CARTESIAN_POINT('Ctrl Pts',(3.60702402556105,-3.99753379040646,12.8644623574794));
#25629=CARTESIAN_POINT('Ctrl Pts',(3.48911597154714,-3.97064599758179,12.8703359994831));
#25630=CARTESIAN_POINT('Ctrl Pts',(3.37270834167444,-3.93861493487687,12.8762096414867));
#25631=CARTESIAN_POINT('Ctrl Pts',(3.25719698051881,-3.90683049208431,12.8820380599806));
#25632=CARTESIAN_POINT('Ctrl Pts',(3.14316338995698,-3.86998188550789,12.8878664784745));
#25633=CARTESIAN_POINT('Ctrl Pts',(3.03107066098493,-3.8282455867311,12.8936948969684));
#25634=CARTESIAN_POINT('Ctrl Pts',(2.91767331740115,-3.78602353133368,12.8995911507269));
#25635=CARTESIAN_POINT('Ctrl Pts',(2.806262694842,-3.73879945511024,12.9054874044853));
#25636=CARTESIAN_POINT('Ctrl Pts',(2.69729429427881,-3.68680471154055,12.9113836582438));
#25637=CARTESIAN_POINT('Ctrl Pts',(2.58832589371562,-3.63480996797085,12.9172799120023));
#25638=CARTESIAN_POINT('Ctrl Pts',(2.4818000634012,-3.57804480545435,12.9231761657608));
#25639=CARTESIAN_POINT('Ctrl Pts',(2.37814277736662,-3.51678612810075,12.9290724195193));
#25640=CARTESIAN_POINT('Ctrl Pts',(2.2754962665976,-3.4561247918337,12.934911178164));
#25641=CARTESIAN_POINT('Ctrl Pts',(2.17535292698837,-3.39087421999619,12.9407499368087));
#25642=CARTESIAN_POINT('Ctrl Pts',(2.07814793218568,-3.32126683558369,12.9465886954534));
#25643=CARTESIAN_POINT('Ctrl Pts',(1.98106039525784,-3.25174356141123,12.9524203988209));
#25644=CARTESIAN_POINT('Ctrl Pts',(1.88690446724543,-3.17787418187297,12.9582521021883));
#25645=CARTESIAN_POINT('Ctrl Pts',(1.79608922994093,-3.09993611448662,12.9640838055558));
#25646=CARTESIAN_POINT('Ctrl Pts',(1.70536045084141,-3.02207224594185,12.9699099570069));
#25647=CARTESIAN_POINT('Ctrl Pts',(1.61796634064222,-2.94014765955751,12.975736108458));
#25648=CARTESIAN_POINT('Ctrl Pts',(1.53428510214239,-2.85448167734931,12.9815622599091));
#25649=CARTESIAN_POINT('Ctrl Pts',(1.45025091187488,-2.76845437209674,12.9874129849742));
#25650=CARTESIAN_POINT('Ctrl Pts',(1.3699613197849,-2.67865428144424,12.9932637100393));
#25651=CARTESIAN_POINT('Ctrl Pts',(1.29376422719912,-2.58544441986834,12.9991144351044));
#25652=CARTESIAN_POINT('Ctrl Pts',(1.2179653618943,-2.4927216990543,13.0049345826467));
#25653=CARTESIAN_POINT('Ctrl Pts',(1.14621657333452,-2.39662508607003,13.010754730189));
#25654=CARTESIAN_POINT('Ctrl Pts',(1.07882138956362,-2.29754671381835,13.0165748777313));
#25655=CARTESIAN_POINT('Ctrl Pts',(1.01143462280293,-2.19848071550238,13.0223942983932));
#25656=CARTESIAN_POINT('Ctrl Pts',(0.948400607313289,-2.09643403410519,
13.0282137190551));
#25657=CARTESIAN_POINT('Ctrl Pts',(0.889980100662972,-1.99182860037029,
13.0340331397169));
#25658=CARTESIAN_POINT('Ctrl Pts',(0.83155332862376,-1.88721194807943,13.0398531844907));
#25659=CARTESIAN_POINT('Ctrl Pts',(0.777741247004828,-1.78003635203042,
13.0456732292645));
#25660=CARTESIAN_POINT('Ctrl Pts',(0.728758828868994,-1.67074866097342,
13.0514932740382));
#25661=CARTESIAN_POINT('Ctrl Pts',(0.679323445976223,-1.56045033233869,
13.0573671396576));
#25662=CARTESIAN_POINT('Ctrl Pts',(0.634807689365803,-1.44800102578564,
13.0632410052771));
#25663=CARTESIAN_POINT('Ctrl Pts',(0.595382571242502,-1.33387996814883,
13.0691148708965));
#25664=CARTESIAN_POINT('Ctrl Pts',(0.556263625545629,-1.22064516584329,
13.0749431205286));
#25665=CARTESIAN_POINT('Ctrl Pts',(0.522156588801595,-1.10576489519778,
13.0807713701606));
#25666=CARTESIAN_POINT('Ctrl Pts',(0.49317784274618,-0.989720849980289,
13.0865996197927));
#25667=CARTESIAN_POINT('Ctrl Pts',(0.463858884569635,-0.872314441094877,
13.0924962934058));
#25668=CARTESIAN_POINT('Ctrl Pts',(0.439789486603947,-0.753717176795685,
13.0983929670189));
#25669=CARTESIAN_POINT('Ctrl Pts',(0.421036494612281,-0.634435684042738,
13.104289640632));
#25670=CARTESIAN_POINT('Ctrl Pts',(0.402283502620615,-0.515154191289791,
13.1101863142451));
#25671=CARTESIAN_POINT('Ctrl Pts',(0.388846908711802,-0.395188898015737,
13.1160829878582));
#25672=CARTESIAN_POINT('Ctrl Pts',(0.380739271722795,-0.275047843480715,
13.1219796614713));
#25673=CARTESIAN_POINT('Ctrl Pts',(0.372711071968696,-0.156083910366433,
13.1278185604889));
#25674=CARTESIAN_POINT('Ctrl Pts',(0.369883613835015,-0.0365888074691707,
13.1336574595066));
#25675=CARTESIAN_POINT('Ctrl Pts',(0.372311325438709,0.0829471018040055,
13.1394963585243));
#25676=CARTESIAN_POINT('Ctrl Pts',(0.374736104427346,0.202338614680651,
13.1453282042975));
#25677=CARTESIAN_POINT('Ctrl Pts',(0.382403416590484,0.32177043345333,13.1511600500708));
#25678=CARTESIAN_POINT('Ctrl Pts',(0.395315826060202,0.440748267224361,
13.1569918958441));
#25679=CARTESIAN_POINT('Ctrl Pts',(0.408215946971634,0.559612871466202,
13.1628181915319));
#25680=CARTESIAN_POINT('Ctrl Pts',(0.42635118959713,0.678023949096839,13.1686444872197));
#25681=CARTESIAN_POINT('Ctrl Pts',(0.449672095205043,0.795488977004324,
13.1744707829075));
#25682=CARTESIAN_POINT('Ctrl Pts',(0.473090570595575,0.913445453976044,
13.1803214545956));
#25683=CARTESIAN_POINT('Ctrl Pts',(0.501738186921314,1.03044753359977,13.1861721262838));
#25684=CARTESIAN_POINT('Ctrl Pts',(0.535512326060149,1.1460030227412,13.192022797972));
#25685=CARTESIAN_POINT('Ctrl Pts',(0.569111111575057,1.2609585536216,13.1978430932683));
#25686=CARTESIAN_POINT('Ctrl Pts',(0.60778318924555,1.37448208898405,13.2036633885647));
#25687=CARTESIAN_POINT('Ctrl Pts',(0.651376821521075,1.48610151232606,13.209483683861));
#25688=CARTESIAN_POINT('Ctrl Pts',(0.694965017369136,1.59770701595395,13.2153032533263));
#25689=CARTESIAN_POINT('Ctrl Pts',(0.743473399315608,1.70740850214749,13.2211228227916));
#25690=CARTESIAN_POINT('Ctrl Pts',(0.796701466056448,1.81475227511203,13.2269423922569));
#25691=CARTESIAN_POINT('Ctrl Pts',(0.849935249169389,1.92210757614787,13.2327625867087));
#25692=CARTESIAN_POINT('Ctrl Pts',(0.907889544653471,2.0271042970717,13.2385827811605));
#25693=CARTESIAN_POINT('Ctrl Pts',(0.970317407141414,2.12931240803774,13.2444029756123));
#25694=CARTESIAN_POINT('Ctrl Pts',(1.03331875227718,2.23245943595158,13.2502766362632));
#25695=CARTESIAN_POINT('Ctrl Pts',(1.10087606255093,2.33276599500634,13.2561502969141));
#25696=CARTESIAN_POINT('Ctrl Pts',(1.17269088283348,2.42982007145051,13.262023957565));
#25697=CARTESIAN_POINT('Ctrl Pts',(1.24395232102069,2.52612628014296,13.2678523576607));
#25698=CARTESIAN_POINT('Ctrl Pts',(1.31940558078958,2.6192296763458,13.2736807577564));
#25699=CARTESIAN_POINT('Ctrl Pts',(1.39871922202046,2.70876182889677,13.2795091578521));
#25700=CARTESIAN_POINT('Ctrl Pts',(1.47895673070527,2.79933687697666,13.2854054487806));
#25701=CARTESIAN_POINT('Ctrl Pts',(1.56314482844506,2.88625664717841,13.2913017397091));
#25702=CARTESIAN_POINT('Ctrl Pts',(1.65090360063393,2.96917954894533,13.2971980306377));
#25703=CARTESIAN_POINT('Ctrl Pts',(1.7386623728228,3.05210245071224,13.3030943215662));
#25704=CARTESIAN_POINT('Ctrl Pts',(1.82999146227194,3.13102824863487,13.3089906124947));
#25705=CARTESIAN_POINT('Ctrl Pts',(1.92447909665735,3.20565930683277,13.3148869034232));
#25706=CARTESIAN_POINT('Ctrl Pts',(2.01804635339524,3.27956340474405,13.3207257602291));
#25707=CARTESIAN_POINT('Ctrl Pts',(2.11499307489557,3.34947899065648,13.3265646170351));
#25708=CARTESIAN_POINT('Ctrl Pts',(2.2149456546496,3.41508383734098,13.332403473841));
#25709=CARTESIAN_POINT('Ctrl Pts',(2.31477748671508,3.48060943010711,13.3382352770175));
#25710=CARTESIAN_POINT('Ctrl Pts',(2.41760761688817,3.54183442230089,13.344067080194));
#25711=CARTESIAN_POINT('Ctrl Pts',(2.52302986581768,3.59847713674535,13.3498988833705));
#25712=CARTESIAN_POINT('Ctrl Pts',(2.62835177926144,3.65506594156139,13.355725136136));
#25713=CARTESIAN_POINT('Ctrl Pts',(2.73626054717992,3.70708095509481,13.3615513889015));
#25714=CARTESIAN_POINT('Ctrl Pts',(2.84632202440033,3.75428440250776,13.367377641667));
#25715=CARTESIAN_POINT('Ctrl Pts',(2.95684509161434,3.80168581781591,13.3732283293215));
#25716=CARTESIAN_POINT('Ctrl Pts',(3.06953861804267,3.84423499240065,13.379079016976));
#25717=CARTESIAN_POINT('Ctrl Pts',(3.18393865006805,3.88173817228442,13.3849297046305));
#25718=CARTESIAN_POINT('Ctrl Pts',(3.29774356320336,3.91904625737326,13.3907499565004));
#25719=CARTESIAN_POINT('Ctrl Pts',(3.4132368772308,3.95136060343397,13.3965702083702));
#25720=CARTESIAN_POINT('Ctrl Pts',(3.52994342808911,3.97853932590431,13.40239046024));
#25721=CARTESIAN_POINT('Ctrl Pts',(3.64663542256786,4.0057146584724,13.4082099861712));
#25722=CARTESIAN_POINT('Ctrl Pts',(3.76453995782569,4.02775554971939,13.4140295121023));
#25723=CARTESIAN_POINT('Ctrl Pts',(3.88316948104885,4.0445707485196,13.4198490380335));
#25724=CARTESIAN_POINT('Ctrl Pts',(4.00181174333475,4.06138775302438,13.425669188896));
#25725=CARTESIAN_POINT('Ctrl Pts',(4.12117874671891,4.07297789239719,13.4314893397585));
#25726=CARTESIAN_POINT('Ctrl Pts',(4.24077618740749,4.07930160257546,13.437309490621));
#25727=CARTESIAN_POINT('Ctrl Pts',(4.36147443784173,4.08568351802762,13.4431832118505));
#25728=CARTESIAN_POINT('Ctrl Pts',(4.48240696941911,4.08670153095217,13.44905693308));
#25729=CARTESIAN_POINT('Ctrl Pts',(4.60306517603562,4.08236874771423,13.4549306543095));
#25730=CARTESIAN_POINT('Ctrl Pts',(4.7227915042599,4.07806942782032,13.4607590110831));
#25731=CARTESIAN_POINT('Ctrl Pts',(4.84224732746244,4.06850176594928,13.4665873678567));
#25732=CARTESIAN_POINT('Ctrl Pts',(4.96094135312177,4.05373072022599,13.4724157246303));
#25733=CARTESIAN_POINT('Ctrl Pts',(5.08102114412744,4.03878722097625,13.4783121280878));
#25734=CARTESIAN_POINT('Ctrl Pts',(5.20032081395789,4.01851813519756,13.4842085315452));
#25735=CARTESIAN_POINT('Ctrl Pts',(5.31834375020069,3.99304358829952,13.4901049350027));
#25736=CARTESIAN_POINT('Ctrl Pts',(5.4363666864435,3.96756904140149,13.4960013384602));
#25737=CARTESIAN_POINT('Ctrl Pts',(5.55311249288124,3.93688919484002,13.5018977419176));
#25738=CARTESIAN_POINT('Ctrl Pts',(5.66810279045029,3.90117531203535,13.5077941453751));
#25739=CARTESIAN_POINT('Ctrl Pts',(5.7819541725698,3.8658151555341,13.5136321482098));
#25740=CARTESIAN_POINT('Ctrl Pts',(5.89442803691065,3.82541362846627,13.5194701510445));
#25741=CARTESIAN_POINT('Ctrl Pts',(6.00504754787872,3.78009653448483,13.5253081538791));
#25742=CARTESIAN_POINT('Ctrl Pts',(6.11554146611341,3.7348308916231,13.5311395284913));
#25743=CARTESIAN_POINT('Ctrl Pts',(6.22418484561038,3.68466093299057,13.5369709031034));
#25744=CARTESIAN_POINT('Ctrl Pts',(6.33051575959186,3.62976227058728,13.5428022777156));
#25745=CARTESIAN_POINT('Ctrl Pts',(6.4367506424443,3.57491318906632,13.5486283858115));
#25746=CARTESIAN_POINT('Ctrl Pts',(6.54067685555499,3.5153440839737,13.5544544939073));
#25747=CARTESIAN_POINT('Ctrl Pts',(6.64185278983194,3.45127848128702,13.5602806020032));
#25748=CARTESIAN_POINT('Ctrl Pts',(6.74296309344481,3.38725443658623,13.5661029308274));
#25749=CARTESIAN_POINT('Ctrl Pts',(6.84132632583219,3.31873991355129,13.5719252596516));
#25750=CARTESIAN_POINT('Ctrl Pts',(6.93652632958691,3.2460038768949,13.5777475884758));
#25751=CARTESIAN_POINT('Ctrl Pts',(7.03168744040331,3.17329755576451,13.5835675386502));
#25752=CARTESIAN_POINT('Ctrl Pts',(7.12368757265028,3.09637339939824,13.5893874888245));
#25753=CARTESIAN_POINT('Ctrl Pts',(7.21214086356068,3.01554276470838,13.5952074389989));
#25754=CARTESIAN_POINT('Ctrl Pts',(7.30060389556322,2.93470322838635,13.6010280301066));
#25755=CARTESIAN_POINT('Ctrl Pts',(7.38551899932978,2.84995662030946,13.6068486212144));
#25756=CARTESIAN_POINT('Ctrl Pts',(7.46653478833146,2.76165341586596,13.6126692123222));
#25757=CARTESIAN_POINT('Ctrl Pts',(7.54752149206514,2.67338191292656,13.6184877137946));
#25758=CARTESIAN_POINT('Ctrl Pts',(7.62461141413523,2.58155667271329,13.6243062152671));
#25759=CARTESIAN_POINT('Ctrl Pts',(7.69749241145744,2.48656247355586,13.6301247167396));
#25760=CARTESIAN_POINT('Origin',(4.45646910621825,2.93978508838399E-15,
8.23961502859548));
#25761=CARTESIAN_POINT('',(7.69668968132766,2.48593167737218,14.9842676783293));
#25762=CARTESIAN_POINT('',(7.70074909849077,2.48902547716684,14.8803008071898));
#25763=CARTESIAN_POINT('',(7.69749241145744,2.48656247355586,8.23961502859548));
#25764=CARTESIAN_POINT('',(8.54454168082834,-0.00144745710864128,13.8646150285955));
#25765=CARTESIAN_POINT('Ctrl Pts',(8.54666930739189,-0.00144821043386754,
13.8646150285955));
#25766=CARTESIAN_POINT('Ctrl Pts',(8.54710349746243,-0.0928747809970434,
13.8690834652399));
#25767=CARTESIAN_POINT('Ctrl Pts',(8.5037729238356,-1.49954483890456,13.9378543158683));
#25768=CARTESIAN_POINT('Ctrl Pts',(6.8902438015866,-4.1182632906804,14.0709275804807));
#25769=CARTESIAN_POINT('Ctrl Pts',(2.43669343542057,-4.33631261202236,14.2638348224326));
#25770=CARTESIAN_POINT('Ctrl Pts',(-0.262050461583375,-0.786882051116074,
14.4567420643845));
#25771=CARTESIAN_POINT('Ctrl Pts',(1.13891927667451,3.44634822095808,14.6496493063365));
#25772=CARTESIAN_POINT('Ctrl Pts',(5.04320204593008,4.57543617360612,14.8254911776514));
#25773=CARTESIAN_POINT('Ctrl Pts',(7.0992059979852,3.25061891740341,14.9370306349823));
#25774=CARTESIAN_POINT('Ctrl Pts',(7.69668968132748,2.48593167737241,14.9842676783293));
#25775=CARTESIAN_POINT('Ctrl Pts',(7.69749241145743,2.48656247355587,13.7345026286438));
#25776=CARTESIAN_POINT('Ctrl Pts',(7.76968844409539,2.39246106777425,13.7402711665733));
#25777=CARTESIAN_POINT('Ctrl Pts',(7.83783719235359,2.29514180401789,13.7460397045029));
#25778=CARTESIAN_POINT('Ctrl Pts',(7.90164394098947,2.19499324779346,13.7518082424324));
#25779=CARTESIAN_POINT('Ctrl Pts',(7.96542734353023,2.09488133467919,13.7575746697258));
#25780=CARTESIAN_POINT('Ctrl Pts',(8.02487168246655,1.9919425361957,13.7633410970191));
#25781=CARTESIAN_POINT('Ctrl Pts',(8.07972515864914,1.88659496938868,13.7691075243125));
#25782=CARTESIAN_POINT('Ctrl Pts',(8.13457196419649,1.7812602137149,13.7748732503607));
#25783=CARTESIAN_POINT('Ctrl Pts',(8.18482882630859,1.67351763997037,13.7806389764089));
#25784=CARTESIAN_POINT('Ctrl Pts',(8.23028991805605,1.56380992455593,13.7864047024571));
#25785=CARTESIAN_POINT('Ctrl Pts',(8.27575658665505,1.45408875095962,13.7921711358046));
#25786=CARTESIAN_POINT('Ctrl Pts',(8.31642615768105,1.3424023396563,13.7979375691521));
#25787=CARTESIAN_POINT('Ctrl Pts',(8.35214123659239,1.22921261489865,13.8037040024996));
#25788=CARTESIAN_POINT('Ctrl Pts',(8.38788801935198,1.11592241297654,13.809475554641));
#25789=CARTESIAN_POINT('Ctrl Pts',(8.41867140396666,1.00112662887301,13.8152471067824));
#25790=CARTESIAN_POINT('Ctrl Pts',(8.44438410516932,0.88530162156231,13.8210186589238));
#25791=CARTESIAN_POINT('Ctrl Pts',(8.47010954482429,0.769419232830652,13.8267930703774));
#25792=CARTESIAN_POINT('Ctrl Pts',(8.49075922567521,0.652507013129004,13.8325674818311));
#25793=CARTESIAN_POINT('Ctrl Pts',(8.50627742689127,0.535049124667352,13.8383418932847));
#25794=CARTESIAN_POINT('Ctrl Pts',(8.52181666906985,0.417431976315101,13.8441241342009));
#25795=CARTESIAN_POINT('Ctrl Pts',(8.53221050295707,0.29926809418751,13.8499063751171));
#25796=CARTESIAN_POINT('Ctrl Pts',(8.53745524789854,0.181044501195737,13.8556886160333));
#25797=CARTESIAN_POINT('Ctrl Pts',(8.54015412986084,0.120208078032049,13.8586640868873));
#25798=CARTESIAN_POINT('Ctrl Pts',(8.54149037829185,0.059355818985477,13.8616395577414));
#25799=CARTESIAN_POINT('Ctrl Pts',(8.54146885016146,-0.00144636911655798,
13.8646150285955));
#25800=CARTESIAN_POINT('',(8.53888143287343,0.00293751736108398,13.7603849714045));
#25801=CARTESIAN_POINT('Ctrl Pts',(7.69749241145744,2.48656247355586,13.6301247167396));
#25802=CARTESIAN_POINT('Ctrl Pts',(7.77116112387467,2.39054155457618,13.6360061059552));
#25803=CARTESIAN_POINT('Ctrl Pts',(7.84052912275375,2.29128309709694,13.6418874951708));
#25804=CARTESIAN_POINT('Ctrl Pts',(7.90531826065341,2.18921550103037,13.6477688843864));
#25805=CARTESIAN_POINT('Ctrl Pts',(7.96952297950996,2.08806858779367,13.6535972215633));
#25806=CARTESIAN_POINT('Ctrl Pts',(8.0292309536961,1.98416339191401,13.6594255587401));
#25807=CARTESIAN_POINT('Ctrl Pts',(8.0842177015797,1.87794172669251,13.6652538959169));
#25808=CARTESIAN_POINT('Ctrl Pts',(8.13995521910658,1.77026974835418,13.6711618111519));
#25809=CARTESIAN_POINT('Ctrl Pts',(8.1908414495447,1.66021796802013,13.677069726387));
#25810=CARTESIAN_POINT('Ctrl Pts',(8.23669336405316,1.54826663093806,13.682977641622));
#25811=CARTESIAN_POINT('Ctrl Pts',(8.28254527856162,1.43631529385599,13.688885556857));
#25812=CARTESIAN_POINT('Ctrl Pts',(8.32336278519854,1.32246482218004,13.694793472092));
#25813=CARTESIAN_POINT('Ctrl Pts',(8.35901574908476,1.20720946825774,13.7007013873271));
#25814=CARTESIAN_POINT('Ctrl Pts',(8.40091264668397,1.07176934674485,13.7076439607528));
#25815=CARTESIAN_POINT('Ctrl Pts',(8.43578063747411,0.934062884985015,13.7145865341786));
#25816=CARTESIAN_POINT('Ctrl Pts',(8.46341078772054,0.794759939251718,13.7215291076044));
#25817=CARTESIAN_POINT('Ctrl Pts',(8.49078114782047,0.656766777662076,13.7284064040718));
#25818=CARTESIAN_POINT('Ctrl Pts',(8.51104909580129,0.517207073291735,13.7352837005392));
#25819=CARTESIAN_POINT('Ctrl Pts',(8.52405849112768,0.376751371293978,13.7421609970066));
#25820=CARTESIAN_POINT('Ctrl Pts',(8.53554956117983,0.252688240734315,13.7482356448664));
#25821=CARTESIAN_POINT('Ctrl Pts',(8.54137809438647,0.127926344822457,13.7543102927261));
#25822=CARTESIAN_POINT('Ctrl Pts',(8.54146804824079,0.00294001266690675,
13.7603849405859));
#25823=CARTESIAN_POINT('Ctrl Pts',(8.53888143287343,0.00293751736108398,
13.7603849714045));
#25824=CARTESIAN_POINT('Ctrl Pts',(8.53231291773911,-0.910184697636579,
13.8047928573627));
#25825=CARTESIAN_POINT('Ctrl Pts',(7.78645395877844,-3.15524707040652,13.9135031573048));
#25826=CARTESIAN_POINT('Ctrl Pts',(4.12896712280502,-4.77242649979729,14.0865158712309));
#25827=CARTESIAN_POINT('Ctrl Pts',(0.335454948527761,-2.42911695903736,
14.2794231131828));
#25828=CARTESIAN_POINT('Ctrl Pts',(0.122429391055361,2.02471691783314,14.4723303551348));
#25829=CARTESIAN_POINT('Ctrl Pts',(3.67497223820188,4.71936388741884,14.6652375970867));
#25830=CARTESIAN_POINT('Ctrl Pts',(6.65799943773292,3.7284653965522,14.8012277477717));
#25831=CARTESIAN_POINT('Ctrl Pts',(7.60957770066985,2.60967412627678,14.8729154844728));
#25832=CARTESIAN_POINT('Ctrl Pts',(7.70074909849077,2.48902547716684,14.8803008071898));
#25833=CARTESIAN_POINT('Origin',(4.45646910621825,3.5527136788005E-15,11.));
#25834=CARTESIAN_POINT('',(7.63534122785693,-1.17693546839596,12.1796263343991));
#25835=CARTESIAN_POINT('',(7.6353412143218,-1.17693550495398,11.8350241089739));
#25836=CARTESIAN_POINT('',(7.63534122785693,-1.17693546839596,11.));
#25837=CARTESIAN_POINT('',(7.84621824929258,-0.00241029600555726,12.1089821966925));
#25838=CARTESIAN_POINT('Ctrl Pts',(7.84621824929188,-0.00241029699009288,
12.1089821967504));
#25839=CARTESIAN_POINT('Ctrl Pts',(7.84610765710331,-0.157942904798472,
12.1181307971768));
#25840=CARTESIAN_POINT('Ctrl Pts',(7.83528910987164,-0.313084630689196,
12.1272793976032));
#25841=CARTESIAN_POINT('Ctrl Pts',(7.81394315636294,-0.466661617347083,
12.1364279980296));
#25842=CARTESIAN_POINT('Ctrl Pts',(7.80972218403832,-0.497030099603801,
12.1382370523402));
#25843=CARTESIAN_POINT('Ctrl Pts',(7.80508971167061,-0.527337486378948,
12.1400461066508));
#25844=CARTESIAN_POINT('Ctrl Pts',(7.80004733817191,-0.557574810501385,
12.1418551609614));
#25845=CARTESIAN_POINT('Ctrl Pts',(7.7825007520135,-0.662795459675959,12.1481503565343));
#25846=CARTESIAN_POINT('Ctrl Pts',(7.759954023632,-0.767358033495362,12.1544455521073));
#25847=CARTESIAN_POINT('Ctrl Pts',(7.73247177283944,-0.870753461543981,
12.1607407476803));
#25848=CARTESIAN_POINT('Ctrl Pts',(7.70498952204689,-0.974148889592601,
12.1670359432532));
#25849=CARTESIAN_POINT('Ctrl Pts',(7.67257179221753,-1.07637668136229,12.1733311388262));
#25850=CARTESIAN_POINT('Ctrl Pts',(7.63534122785693,-1.17693546839596,12.1796263343991));
#25851=CARTESIAN_POINT('',(7.03046338747139,-2.20566509302208,11.000004601718));
#25852=CARTESIAN_POINT('Ctrl Pts',(7.03046338747139,-2.20566509302208,11.000004601718));
#25853=CARTESIAN_POINT('Ctrl Pts',(6.96364411350853,-2.28364267429769,11.0060599561424));
#25854=CARTESIAN_POINT('Ctrl Pts',(6.89316717227375,-2.35871057473643,11.0121153105668));
#25855=CARTESIAN_POINT('Ctrl Pts',(6.81931811192614,-2.43050398862565,11.0181706649912));
#25856=CARTESIAN_POINT('Ctrl Pts',(6.74555740159863,-2.50221151178682,11.0242187750352));
#25857=CARTESIAN_POINT('Ctrl Pts',(6.66843290009554,-2.57065203402839,11.0302668850792));
#25858=CARTESIAN_POINT('Ctrl Pts',(6.58826985773396,-2.63549437835429,11.0363149951232));
#25859=CARTESIAN_POINT('Ctrl Pts',(6.50818175580784,-2.7002761048022,11.0423574510903));
#25860=CARTESIAN_POINT('Ctrl Pts',(6.42506109837629,-2.76146607043511,11.0483999070575));
#25861=CARTESIAN_POINT('Ctrl Pts',(6.3392686178572,-2.81877119707722,11.0544423630247));
#25862=CARTESIAN_POINT('Ctrl Pts',(6.25351932447536,-2.87604747685122,11.0604817772756));
#25863=CARTESIAN_POINT('Ctrl Pts',(6.16510124073695,-2.9294425618507,11.0665211915266));
#25864=CARTESIAN_POINT('Ctrl Pts',(6.07440605265532,-2.97870527240509,11.0725606057776));
#25865=CARTESIAN_POINT('Ctrl Pts',(5.98373213828396,-3.02795642776396,11.0785986034072));
#25866=CARTESIAN_POINT('Ctrl Pts',(5.89078256297615,-3.07307692789121,11.0846366010367));
#25867=CARTESIAN_POINT('Ctrl Pts',(5.79597483524122,-3.11386086144108,11.0906745986663));
#25868=CARTESIAN_POINT('Ctrl Pts',(5.70116385893125,-3.15464619244739,11.0967128031871));
#25869=CARTESIAN_POINT('Ctrl Pts',(5.60449500353731,-3.19109449113594,11.1027510077078));
#25870=CARTESIAN_POINT('Ctrl Pts',(5.50640609840839,-3.22304783937979,11.1087892122286));
#25871=CARTESIAN_POINT('Ctrl Pts',(5.40823003702718,-3.25502957956131,11.1148327819564));
#25872=CARTESIAN_POINT('Ctrl Pts',(5.30863181993906,-3.28250825767039,11.1208763516841));
#25873=CARTESIAN_POINT('Ctrl Pts',(5.20806460500747,-3.30537581353464,11.1269199214119));
#25874=CARTESIAN_POINT('Ctrl Pts',(5.1074515196614,-3.32825379967944,11.1329662477144));
#25875=CARTESIAN_POINT('Ctrl Pts',(5.00586898412057,-3.34651639752689,11.1390125740169));
#25876=CARTESIAN_POINT('Ctrl Pts',(4.90377855029586,-3.36010704051805,11.1450589003194));
#25877=CARTESIAN_POINT('Ctrl Pts',(4.80153271273702,-3.37371837140906,11.1511144304391));
#25878=CARTESIAN_POINT('Ctrl Pts',(4.69877786588522,-3.38264350423802,11.1571699605588));
#25879=CARTESIAN_POINT('Ctrl Pts',(4.59597894094542,-3.38687792347383,11.1632254906785));
#25880=CARTESIAN_POINT('Ctrl Pts',(4.5162285551083,-3.39016294389646,11.1679233108529));
#25881=CARTESIAN_POINT('Ctrl Pts',(4.43645172653599,-3.39062591871191,11.1726211310273));
#25882=CARTESIAN_POINT('Ctrl Pts',(4.35686353873807,-3.38828626202494,11.1773189512018));
#25883=CARTESIAN_POINT('Ctrl Pts',(4.25307543195265,-3.38523519948931,11.1834452103291));
#25884=CARTESIAN_POINT('Ctrl Pts',(4.14926928185013,-3.37740639907282,11.1895714694564));
#25885=CARTESIAN_POINT('Ctrl Pts',(4.04591729830903,-3.3647960228701,11.1956977285837));
#25886=CARTESIAN_POINT('Ctrl Pts',(3.94269237402144,-3.35220114965951,11.2018164561873));
#25887=CARTESIAN_POINT('Ctrl Pts',(3.83992092339695,-3.33483644124615,11.2079351837909));
#25888=CARTESIAN_POINT('Ctrl Pts',(3.73807358322337,-3.31275005622834,11.2140539113945));
#25889=CARTESIAN_POINT('Ctrl Pts',(3.63632306575806,-3.29068466796518,11.2201668221376));
#25890=CARTESIAN_POINT('Ctrl Pts',(3.53549532339145,-3.26390662077776,11.2262797328806));
#25891=CARTESIAN_POINT('Ctrl Pts',(3.43605348907385,-3.23251558863802,11.2323926436237));
#25892=CARTESIAN_POINT('Ctrl Pts',(3.33667388802547,-3.20114420181724,11.2385017287492));
#25893=CARTESIAN_POINT('Ctrl Pts',(3.23867887293101,-3.16516569891973,11.2446108138748));
#25894=CARTESIAN_POINT('Ctrl Pts',(3.14251830080288,-3.12473012329838,11.2507198990004));
#25895=CARTESIAN_POINT('Ctrl Pts',(3.04638798576622,-3.0843072708013,11.2568270618916));
#25896=CARTESIAN_POINT('Ctrl Pts',(2.9520913562225,-3.03943029779103,11.2629342247829));
#25897=CARTESIAN_POINT('Ctrl Pts',(2.86005937057485,-2.99029781433939,11.2690413876742));
#25898=CARTESIAN_POINT('Ctrl Pts',(2.76803311035823,-2.94116838748426,11.2751481706309));
#25899=CARTESIAN_POINT('Ctrl Pts',(2.67827158723843,-2.88778417655825,11.2812549535875));
#25900=CARTESIAN_POINT('Ctrl Pts',(2.59118140944753,-2.83038987964128,11.2873617365441));
#25901=CARTESIAN_POINT('Ctrl Pts',(2.5040746653177,-2.77298466515128,11.2934696811362));
#25902=CARTESIAN_POINT('Ctrl Pts',(2.41964062997498,-2.71156808176117,11.2995776257283));
#25903=CARTESIAN_POINT('Ctrl Pts',(2.33825643994187,-2.64642781177312,11.3056855703204));
#25904=CARTESIAN_POINT('Ctrl Pts',(2.2567896085224,-2.58122139524953,11.3117997172106));
#25905=CARTESIAN_POINT('Ctrl Pts',(2.17837913695186,-2.51228400757457,11.3179138641007));
#25906=CARTESIAN_POINT('Ctrl Pts',(2.10336854946749,-2.43994320268305,11.3240280109909));
#25907=CARTESIAN_POINT('Ctrl Pts',(2.02831557589694,-2.3675615203142,11.3301456127902));
#25908=CARTESIAN_POINT('Ctrl Pts',(1.95666660454135,-2.29177289708959,11.3362632145894));
#25909=CARTESIAN_POINT('Ctrl Pts',(1.88872651126045,-2.21293990621964,11.3423808163886));
#25910=CARTESIAN_POINT('Ctrl Pts',(1.82068557647108,-2.13398990582949,11.3485074983667));
#25911=CARTESIAN_POINT('Ctrl Pts',(1.75636477447799,-2.05198684699319,11.3546341803447));
#25912=CARTESIAN_POINT('Ctrl Pts',(1.69602714989169,-1.96732439324378,11.3607608623227));
#25913=CARTESIAN_POINT('Ctrl Pts',(1.66495456278761,-1.92372503899987,11.3639159725997));
#25914=CARTESIAN_POINT('Ctrl Pts',(1.63493760256666,-1.87942085103863,11.3670710828767));
#25915=CARTESIAN_POINT('Ctrl Pts',(1.60600744878302,-1.83446815235141,11.3702261931537));
#25916=CARTESIAN_POINT('Ctrl Pts',(1.54997323606809,-1.74740020590397,11.3763372605791));
#25917=CARTESIAN_POINT('Ctrl Pts',(1.49784136340171,-1.6576218645813,11.3824483280045));
#25918=CARTESIAN_POINT('Ctrl Pts',(1.44988280934613,-1.56551713563308,11.3885593954299));
#25919=CARTESIAN_POINT('Ctrl Pts',(1.40198544232448,-1.47352991679927,11.394662666163));
#25920=CARTESIAN_POINT('Ctrl Pts',(1.35825100267684,-1.37922258670873,11.4007659368961));
#25921=CARTESIAN_POINT('Ctrl Pts',(1.31890687553446,-1.28300752573264,11.4068692076292));
#25922=CARTESIAN_POINT('Ctrl Pts',(1.27960179886222,-1.18688796168679,11.4129664206453));
#25923=CARTESIAN_POINT('Ctrl Pts',(1.24467852910567,-1.08886482493238,11.4190636336613));
#25924=CARTESIAN_POINT('Ctrl Pts',(1.21431785207666,-0.989373694701926,
11.4251608466773));
#25925=CARTESIAN_POINT('Ctrl Pts',(1.18397767780842,-0.889949751472577,
11.4312539422061));
#25926=CARTESIAN_POINT('Ctrl Pts',(1.15819409251278,-0.78906019282724,11.4373470377349));
#25927=CARTESIAN_POINT('Ctrl Pts',(1.137098915894,-0.687158352992052,11.4434401332636));
#25928=CARTESIAN_POINT('Ctrl Pts',(1.11601099280535,-0.585291551880595,
11.4495311336949));
#25929=CARTESIAN_POINT('Ctrl Pts',(1.09960836013549,-0.482413578327243,
11.4556221341262));
#25930=CARTESIAN_POINT('Ctrl Pts',(1.08797214948141,-0.378989861282093,
11.4617131345575));
#25931=CARTESIAN_POINT('Ctrl Pts',(1.07633695469905,-0.275575173398873,
11.4678036032284));
#25932=CARTESIAN_POINT('Ctrl Pts',(1.06946740168239,-0.171615260226652,
11.4738940718994));
#25933=CARTESIAN_POINT('Ctrl Pts',(1.06739286425132,-0.0675817182033117,
11.4799845405704));
#25934=CARTESIAN_POINT('Ctrl Pts',(1.06531797573343,0.0364694300609991,
11.4860760399691));
#25935=CARTESIAN_POINT('Ctrl Pts',(1.06803972356699,0.14059380593717,11.4921675393678));
#25936=CARTESIAN_POINT('Ctrl Pts',(1.07553536429218,0.244319657837441,11.4982590387665));
#25937=CARTESIAN_POINT('Ctrl Pts',(1.08303851283162,0.348149404048647,11.5043566395577));
#25938=CARTESIAN_POINT('Ctrl Pts',(1.09532507055292,0.451579403665733,11.5104542403489));
#25939=CARTESIAN_POINT('Ctrl Pts',(1.11232038896645,0.554142959355393,11.51655184114));
#25940=CARTESIAN_POINT('Ctrl Pts',(1.12932511918393,0.656763313514801,11.5226528187096));
#25941=CARTESIAN_POINT('Ctrl Pts',(1.15104371547761,0.75851585140497,11.5287537962791));
#25942=CARTESIAN_POINT('Ctrl Pts',(1.17735076910878,0.858945861933337,11.5348547738486));
#25943=CARTESIAN_POINT('Ctrl Pts',(1.20369711598113,0.959525878641883,11.5409648640762));
#25944=CARTESIAN_POINT('Ctrl Pts',(1.23464547965846,1.05877901668213,11.5470749543038));
#25945=CARTESIAN_POINT('Ctrl Pts',(1.27002112670429,1.15626741558838,11.5531850445313));
#25946=CARTESIAN_POINT('Ctrl Pts',(1.28922055696488,1.20917730904112,11.5565011747227));
#25947=CARTESIAN_POINT('Ctrl Pts',(1.30972323911573,1.26156775104713,11.5598173049141));
#25948=CARTESIAN_POINT('Ctrl Pts',(1.33149552586891,1.31337168563153,11.5631334351056));
#25949=CARTESIAN_POINT('Ctrl Pts',(1.37167159184059,1.40896468957506,11.5692526391585));
#25950=CARTESIAN_POINT('Ctrl Pts',(1.41630116220111,1.5028630143177,11.5753718432114));
#25951=CARTESIAN_POINT('Ctrl Pts',(1.46521933320156,1.59462530330093,11.5814910472643));
#25952=CARTESIAN_POINT('Ctrl Pts',(1.51407599835094,1.68627221761737,11.5876025575126));
#25953=CARTESIAN_POINT('Ctrl Pts',(1.56721034389962,1.77578806447175,11.5937140677608));
#25954=CARTESIAN_POINT('Ctrl Pts',(1.6244094644662,1.86275152611917,11.599825578009));
#25955=CARTESIAN_POINT('Ctrl Pts',(1.68155273476896,1.94963007505764,11.6059311208673));
#25956=CARTESIAN_POINT('Ctrl Pts',(1.74275265396909,2.03396084232813,11.6120366637255));
#25957=CARTESIAN_POINT('Ctrl Pts',(1.80775088932139,2.11534793118738,11.6181422065837));
#25958=CARTESIAN_POINT('Ctrl Pts',(1.87270634746321,2.19668145685971,11.6242437312084));
#25959=CARTESIAN_POINT('Ctrl Pts',(1.94145488559652,2.27507482618555,11.6303452558331));
#25960=CARTESIAN_POINT('Ctrl Pts',(2.01369589367489,2.35016256769199,11.6364467804577));
#25961=CARTESIAN_POINT('Ctrl Pts',(2.08591277564395,2.42522523237423,11.6425462673748));
#25962=CARTESIAN_POINT('Ctrl Pts',(2.16161951463887,2.49698415810805,11.6486457542919));
#25963=CARTESIAN_POINT('Ctrl Pts',(2.24047691939051,2.5651089042024,11.6547452412089));
#25964=CARTESIAN_POINT('Ctrl Pts',(2.31932804958399,2.63322822971915,11.6608442427995));
#25965=CARTESIAN_POINT('Ctrl Pts',(2.40132902530304,2.69771367333297,11.6669432443902));
#25966=CARTESIAN_POINT('Ctrl Pts',(2.48610635141016,2.75827403949736,11.6730422459808));
#25967=CARTESIAN_POINT('Ctrl Pts',(2.57089849848763,2.81884499296655,11.6791423138131));
#25968=CARTESIAN_POINT('Ctrl Pts',(2.6584676148026,2.87548925863655,11.6852423816454));
#25969=CARTESIAN_POINT('Ctrl Pts',(2.74841064676608,2.92795856555278,11.6913424494777));
#25970=CARTESIAN_POINT('Ctrl Pts',(2.83844368463475,2.98048037845375,11.6974486216421));
#25971=CARTESIAN_POINT('Ctrl Pts',(2.93085501384979,3.02881867664673,11.7035547938064));
#25972=CARTESIAN_POINT('Ctrl Pts',(3.02521642954576,3.07277087300987,11.7096609659707));
#25973=CARTESIAN_POINT('Ctrl Pts',(3.11963022305209,3.11674746620713,11.7157705275281));
#25974=CARTESIAN_POINT('Ctrl Pts',(3.21599586664937,3.15633294622868,11.7218800890854));
#25975=CARTESIAN_POINT('Ctrl Pts',(3.31386635016529,3.19137337275979,11.7279896506428));
#25976=CARTESIAN_POINT('Ctrl Pts',(3.41188184714174,3.22646571824877,11.7341082646605));
#25977=CARTESIAN_POINT('Ctrl Pts',(3.51140623094587,3.25699943722907,11.7402268786781));
#25978=CARTESIAN_POINT('Ctrl Pts',(3.61197850559916,3.28287079976749,11.7463454926958));
#25979=CARTESIAN_POINT('Ctrl Pts',(3.66509874609967,3.29653552998121,11.7495772208163));
#25980=CARTESIAN_POINT('Ctrl Pts',(3.71851115781609,3.30890044691213,11.7528089489369));
#25981=CARTESIAN_POINT('Ctrl Pts',(3.77214707404916,3.31995608687645,11.7560406770575));
#25982=CARTESIAN_POINT('Ctrl Pts',(3.87369261179996,3.34088704106166,11.7621591065151));
#25983=CARTESIAN_POINT('Ctrl Pts',(3.97635925686529,3.35718786702286,11.7682775359728));
#25984=CARTESIAN_POINT('Ctrl Pts',(4.07968985990864,3.36874493870498,11.7743959654304));
#25985=CARTESIAN_POINT('Ctrl Pts',(4.18289065755572,3.38028749222669,11.7805067088286));
#25986=CARTESIAN_POINT('Ctrl Pts',(4.2867533356158,3.38709809394802,11.7866174522268));
#25987=CARTESIAN_POINT('Ctrl Pts',(4.39081011957819,3.38911403761712,11.7927281956249));
#25988=CARTESIAN_POINT('Ctrl Pts',(4.49476543877261,3.39112801555896,11.7988329804961));
#25989=CARTESIAN_POINT('Ctrl Pts',(4.5989140646279,3.38835662578775,11.8049377653672));
#25990=CARTESIAN_POINT('Ctrl Pts',(4.70278349365506,3.38078900333068,11.8110425502383));
#25991=CARTESIAN_POINT('Ctrl Pts',(4.80658483771223,3.37322634134516,11.8171433335077));
#25992=CARTESIAN_POINT('Ctrl Pts',(4.91010692625367,3.36087373015861,11.823244116777));
#25993=CARTESIAN_POINT('Ctrl Pts',(5.01287843551619,3.34377237873188,11.8293449000463));
#25994=CARTESIAN_POINT('Ctrl Pts',(5.11561579902865,3.3266767092152,11.8354436563354));
#25995=CARTESIAN_POINT('Ctrl Pts',(5.21760266030219,3.30483550566695,11.8415424126245));
#25996=CARTESIAN_POINT('Ctrl Pts',(5.31837476715059,3.27834160729977,11.8476411689135));
#25997=CARTESIAN_POINT('Ctrl Pts',(5.41913904894595,3.2518497662098,11.8537394516282));
#25998=CARTESIAN_POINT('Ctrl Pts',(5.51868835312645,3.22070605722529,11.8598377343428));
#25999=CARTESIAN_POINT('Ctrl Pts',(5.61657139540344,3.18505380506002,11.8659360170575));
#26000=CARTESIAN_POINT('Ctrl Pts',(5.71447175706836,3.14939524459894,11.8720353787999));
#26001=CARTESIAN_POINT('Ctrl Pts',(5.81070487181571,3.10922670121194,11.8781347405424));
#26002=CARTESIAN_POINT('Ctrl Pts',(5.90483814298822,3.06474015143634,11.8842341022849));
#26003=CARTESIAN_POINT('Ctrl Pts',(5.99906599235371,3.02020890484487,11.8903395922177));
#26004=CARTESIAN_POINT('Ctrl Pts',(6.09118940106688,2.97135117154634,11.8964450821506));
#26005=CARTESIAN_POINT('Ctrl Pts',(6.18079922753286,2.91840550561898,11.9025505720835));
#26006=CARTESIAN_POINT('Ctrl Pts',(6.27045898630629,2.86543033735495,11.9086594641121));
#26007=CARTESIAN_POINT('Ctrl Pts',(6.35760201741397,2.80836293144945,11.9147683561406));
#26008=CARTESIAN_POINT('Ctrl Pts',(6.4418486703467,2.74748485871008,11.9208772481691));
#26009=CARTESIAN_POINT('Ctrl Pts',(6.52622052546176,2.68651631273175,11.9269952188564));
#26010=CARTESIAN_POINT('Ctrl Pts',(6.60768707418294,2.62172605487704,11.9331131895437));
#26011=CARTESIAN_POINT('Ctrl Pts',(6.68590217092384,2.55343558221026,11.939231160231));
#26012=CARTESIAN_POINT('Ctrl Pts',(6.72731008577615,2.51728187026412,11.9424700798238));
#26013=CARTESIAN_POINT('Ctrl Pts',(6.76780731826133,2.48014775675753,11.9457089994166));
#26014=CARTESIAN_POINT('Ctrl Pts',(6.80734692460347,2.44208487680596,11.9489479190095));
#26015=CARTESIAN_POINT('Ctrl Pts',(6.88096398400294,2.37121726952471,11.954978321386));
#26016=CARTESIAN_POINT('Ctrl Pts',(6.95150718080944,2.29688915272491,11.9610087237626));
#26017=CARTESIAN_POINT('Ctrl Pts',(7.01862897299606,2.21940124348283,11.9670391261392));
#26018=CARTESIAN_POINT('Ctrl Pts',(7.08564999444784,2.14202966774886,11.9730604750019));
#26019=CARTESIAN_POINT('Ctrl Pts',(7.14925954296759,2.06150806386155,11.9790818238645));
#26020=CARTESIAN_POINT('Ctrl Pts',(7.20914579240184,1.97817494773373,11.9851031727272));
#26021=CARTESIAN_POINT('Ctrl Pts',(7.26898114075436,1.89491266165112,11.9911194036676));
#26022=CARTESIAN_POINT('Ctrl Pts',(7.32509922049556,1.80884396368172,11.997135634608));
#26023=CARTESIAN_POINT('Ctrl Pts',(7.37722785029553,1.72034107705307,12.0031518655484));
#26024=CARTESIAN_POINT('Ctrl Pts',(7.42932646657381,1.63188914674762,12.0091646325904));
#26025=CARTESIAN_POINT('Ctrl Pts',(7.47743997416593,1.54100618929599,12.0151773996323));
#26026=CARTESIAN_POINT('Ctrl Pts',(7.52133959459298,1.44809321246585,12.0211901666743));
#26027=CARTESIAN_POINT('Ctrl Pts',(7.56522597477905,1.35520825843389,12.0272011202499));
#26028=CARTESIAN_POINT('Ctrl Pts',(7.60490080717506,1.26029489868599,12.0332120738256));
#26029=CARTESIAN_POINT('Ctrl Pts',(7.64018184602719,1.16377757878312,12.0392230274012));
#26030=CARTESIAN_POINT('Ctrl Pts',(7.67547718543311,1.06722113726788,12.045236417412));
#26031=CARTESIAN_POINT('Ctrl Pts',(7.70637501566812,0.969059846948902,12.0512498074228));
#26032=CARTESIAN_POINT('Ctrl Pts',(7.73274191522095,0.869736479337045,12.0572631974337));
#26033=CARTESIAN_POINT('Ctrl Pts',(7.75911344850643,0.770395656584837,12.0632776442408));
#26034=CARTESIAN_POINT('Ctrl Pts',(7.78095236506544,0.669892777560101,12.0692920910479));
#26035=CARTESIAN_POINT('Ctrl Pts',(7.79817607439928,0.568682337786512,12.075306537855));
#26036=CARTESIAN_POINT('Ctrl Pts',(7.81541945859331,0.467356284052392,12.0813278550405));
#26037=CARTESIAN_POINT('Ctrl Pts',(7.82803704330347,0.365321490399033,12.087349172226));
#26038=CARTESIAN_POINT('Ctrl Pts',(7.83599799990535,0.263039007058008,12.0933704894115));
#26039=CARTESIAN_POINT('Ctrl Pts',(7.84287822894921,0.17464172671174,12.0985743918385));
#26040=CARTESIAN_POINT('Ctrl Pts',(7.84628115626159,0.0860596860178569,
12.1037782942655));
#26041=CARTESIAN_POINT('Ctrl Pts',(7.84621824929258,-0.00241029600555718,
12.1089821966925));
#26042=CARTESIAN_POINT('',(1.88323467920355,-2.20655152809225,11.));
#26043=CARTESIAN_POINT('Origin',(4.45646910621825,3.5527136788005E-15,11.));
#26044=CARTESIAN_POINT('Ctrl Pts',(1.88323467920354,-2.20655152809226,11.));
#26045=CARTESIAN_POINT('Ctrl Pts',(1.86599707596286,-2.18644939427239,11.0015541500662));
#26046=CARTESIAN_POINT('Ctrl Pts',(1.8489951410639,-2.1661453996546,11.0030951979296));
#26047=CARTESIAN_POINT('Ctrl Pts',(1.81139159419215,-2.12015425598179,11.006526711438));
#26048=CARTESIAN_POINT('Ctrl Pts',(1.79092266321204,-2.09436181098513,11.0084107827258));
#26049=CARTESIAN_POINT('Ctrl Pts',(1.62499832560114,-1.87891046881364,11.0238519423018));
#26050=CARTESIAN_POINT('Ctrl Pts',(1.49959158403363,-1.67464106458276,11.0366502112481));
#26051=CARTESIAN_POINT('Ctrl Pts',(1.33667743832326,-1.33295299818795,11.0574582868395));
#26052=CARTESIAN_POINT('Ctrl Pts',(1.28447620893895,-1.20346180213168,11.0652154451724));
#26053=CARTESIAN_POINT('Ctrl Pts',(1.21548125192911,-0.996304529957284,
11.077703238766));
#26054=CARTESIAN_POINT('Ctrl Pts',(1.19318050994874,-0.920636325469628,
11.0822788091142));
#26055=CARTESIAN_POINT('Ctrl Pts',(1.1523122573658,-0.761719512053923,11.0919578357044));
#26056=CARTESIAN_POINT('Ctrl Pts',(1.13420681741972,-0.678410363563903,
11.0970707307868));
#26057=CARTESIAN_POINT('Ctrl Pts',(1.06422917855726,-0.285601044751504,
11.1214147892952));
#26058=CARTESIAN_POINT('Ctrl Pts',(1.05236403147467,0.0294219237589118,
11.14179860344));
#26059=CARTESIAN_POINT('Ctrl Pts',(1.09634753074839,0.46378243409643,11.1698014612439));
#26060=CARTESIAN_POINT('Ctrl Pts',(1.11537236474605,0.585310845423136,11.1775990267017));
#26061=CARTESIAN_POINT('Ctrl Pts',(1.15078591102381,0.751726609831858,11.1880304145553));
#26062=CARTESIAN_POINT('Ctrl Pts',(1.16157756953607,0.79769954298666,11.1908852127355));
#26063=CARTESIAN_POINT('Ctrl Pts',(1.18344704280919,0.882828367067341,11.1961042093075));
#26064=CARTESIAN_POINT('Ctrl Pts',(1.19427523192246,0.922036107538697,11.1984788403858));
#26065=CARTESIAN_POINT('Ctrl Pts',(1.22738459860688,1.03402645834213,11.2051961989925));
#26066=CARTESIAN_POINT('Ctrl Pts',(1.25141577354736,1.10626953407051,11.2094520277691));
#26067=CARTESIAN_POINT('Ctrl Pts',(1.34699503400008,1.36424923960056,11.2245713213735));
#26068=CARTESIAN_POINT('Ctrl Pts',(1.43243035575875,1.54441045902614,11.2350010545271));
#26069=CARTESIAN_POINT('Ctrl Pts',(1.5873827163874,1.80837236019493,11.2513924892617));
#26070=CARTESIAN_POINT('Ctrl Pts',(1.64592345453565,1.89807758131636,11.2571777844786));
#26071=CARTESIAN_POINT('Ctrl Pts',(1.76041897694343,2.0565864989518,11.2679745692397));
#26072=CARTESIAN_POINT('Ctrl Pts',(1.81501514150776,2.12625338449111,11.2729414045865));
#26073=CARTESIAN_POINT('Ctrl Pts',(1.91502022565397,2.24406019877022,11.2818003746455));
#26074=CARTESIAN_POINT('Ctrl Pts',(1.95922996613896,2.29315598508195,11.2856436733013));
#26075=CARTESIAN_POINT('Ctrl Pts',(2.05967356350227,2.398349410893,11.2942393478943));
#26076=CARTESIAN_POINT('Ctrl Pts',(2.1165002418265,2.45382413784225,11.2990160694685));
#26077=CARTESIAN_POINT('Ctrl Pts',(2.36518002948247,2.68008836632022,11.3195885037407));
#26078=CARTESIAN_POINT('Ctrl Pts',(2.57414599822951,2.83075716253,11.33617056169));
#26079=CARTESIAN_POINT('Ctrl Pts',(2.88432174146297,3.00475251093036,11.359070476376));
#26080=CARTESIAN_POINT('Ctrl Pts',(2.97265184442071,3.04933978594295,11.3654082948755));
#26081=CARTESIAN_POINT('Ctrl Pts',(3.12559804265472,3.11832194519425,11.3759503750373));
#26082=CARTESIAN_POINT('Ctrl Pts',(3.18924058666404,3.14472300507211,11.3802155435408));
#26083=CARTESIAN_POINT('Ctrl Pts',(3.29060010282618,3.18319284747261,11.3867720965788));
#26084=CARTESIAN_POINT('Ctrl Pts',(3.32779580161469,3.19657071234315,11.3891280939164));
#26085=CARTESIAN_POINT('Ctrl Pts',(3.41127574389892,3.22495613083378,11.3943002819086));
#26086=CARTESIAN_POINT('Ctrl Pts',(3.4576636707273,3.23962334989183,11.3970995439316));
#26087=CARTESIAN_POINT('Ctrl Pts',(3.63159529065526,3.29052661118421,11.4073724179686));
#26088=CARTESIAN_POINT('Ctrl Pts',(3.76092336929158,3.32027172265474,11.4145718351935));
#26089=CARTESIAN_POINT('Ctrl Pts',(4.06731017860474,3.37204542548141,11.4312592311656));
#26090=CARTESIAN_POINT('Ctrl Pts',(4.24501204395672,3.38783416809086,11.440668178534));
#26091=CARTESIAN_POINT('Ctrl Pts',(4.54231166880054,3.39075825727141,11.4568327327308));
#26092=CARTESIAN_POINT('Ctrl Pts',(4.66146210208325,3.38564391744804,11.4634206011539));
#26093=CARTESIAN_POINT('Ctrl Pts',(4.85233760093863,3.36733738452042,11.4743083452772));
#26094=CARTESIAN_POINT('Ctrl Pts',(4.92434078053615,3.35808992285324,11.4784918963722));
#26095=CARTESIAN_POINT('Ctrl Pts',(5.07197939904934,3.33428806425678,11.4872541801692));
#26096=CARTESIAN_POINT('Ctrl Pts',(5.14752646565309,3.31945299500239,11.4918389858457));
#26097=CARTESIAN_POINT('Ctrl Pts',(5.39176457972627,3.26279330462831,11.507012139282));
#26098=CARTESIAN_POINT('Ctrl Pts',(5.55774102229941,3.21057400687688,11.5178926534708));
#26099=CARTESIAN_POINT('Ctrl Pts',(5.90438543180064,3.07145903335125,11.5416331507391));
#26100=CARTESIAN_POINT('Ctrl Pts',(6.08286584137707,2.98079861255615,11.5545033000869));
#26101=CARTESIAN_POINT('Ctrl Pts',(6.30284899078352,2.84338443618124,11.570554953987));
#26102=CARTESIAN_POINT('Ctrl Pts',(6.35253513118355,2.8104960842805,11.5741917594508));
#26103=CARTESIAN_POINT('Ctrl Pts',(6.43471717966392,2.75292593343445,11.5801945342524));
#26104=CARTESIAN_POINT('Ctrl Pts',(6.46767730413894,2.72893909535353,11.5825965726888));
#26105=CARTESIAN_POINT('Ctrl Pts',(6.54904336713181,2.66744933865935,11.5885146334459));
#26106=CARTESIAN_POINT('Ctrl Pts',(6.59687960221767,2.62921981924175,11.5919876026597));
#26107=CARTESIAN_POINT('Ctrl Pts',(6.83676138376692,2.4266234467912,11.6095157968681));
#26108=CARTESIAN_POINT('Ctrl Pts',(7.01103279304588,2.24243578382843,11.6226839857892));
#26109=CARTESIAN_POINT('Ctrl Pts',(7.24547380827723,1.93145799718472,11.6437250880342));
#26110=CARTESIAN_POINT('Ctrl Pts',(7.32105273238859,1.81747984360567,11.6512200627761));
#26111=CARTESIAN_POINT('Ctrl Pts',(7.4265070189314,1.63545617439083,11.6631202900468));
#26112=CARTESIAN_POINT('Ctrl Pts',(7.46137672294725,1.57046845839114,11.6673549373204));
#26113=CARTESIAN_POINT('Ctrl Pts',(7.52666551280824,1.43863962808292,11.6759471247199));
#26114=CARTESIAN_POINT('Ctrl Pts',(7.55708705302273,1.37184441781834,11.6803016692319));
#26115=CARTESIAN_POINT('Ctrl Pts',(7.63631703766182,1.18175546240165,11.6927163876306));
#26116=CARTESIAN_POINT('Ctrl Pts',(7.68009141904249,1.05651869234713,11.7009260284344));
#26117=CARTESIAN_POINT('Ctrl Pts',(7.77124250330589,0.736678651269657,11.7219078270026));
#26118=CARTESIAN_POINT('Ctrl Pts',(7.80892991403089,0.539832381377944,11.7348513874113));
#26119=CARTESIAN_POINT('Ctrl Pts',(7.83621918018113,0.269798371086886,11.7520789207683));
#26120=CARTESIAN_POINT('Ctrl Pts',(7.84115195959594,0.198556561711271,11.7565713628072));
#26121=CARTESIAN_POINT('Ctrl Pts',(7.84594020274366,0.0710536103046219,
11.7644649827159));
#26122=CARTESIAN_POINT('Ctrl Pts',(7.84665245852064,0.0148509416709774,
11.7678935900683));
#26123=CARTESIAN_POINT('Ctrl Pts',(7.84547994795152,-0.0812683973432962,
11.7736428003223));
#26124=CARTESIAN_POINT('Ctrl Pts',(7.84428782265352,-0.121176166923975,
11.7759940772057));
#26125=CARTESIAN_POINT('Ctrl Pts',(7.83949257344823,-0.221985910305632,
11.7818483196353));
#26126=CARTESIAN_POINT('Ctrl Pts',(7.83495030864903,-0.282827206983951,
11.7853064847601));
#26127=CARTESIAN_POINT('Ctrl Pts',(7.80310914697135,-0.595411722914734,
11.8028328868572));
#26128=CARTESIAN_POINT('Ctrl Pts',(7.74930659200723,-0.843657386814209,
11.8159983886954));
#26129=CARTESIAN_POINT('Ctrl Pts',(7.65780130280229,-1.11488409573876,11.8314418949571));
#26130=CARTESIAN_POINT('Ctrl Pts',(7.64679635725797,-1.14599546259751,11.8332287944345));
#26131=CARTESIAN_POINT('Ctrl Pts',(7.6353412143218,-1.17693550495398,11.8350241089739));
#26132=CARTESIAN_POINT('Origin',(4.45646910621825,3.5527136788005E-15,11.));
#26133=CARTESIAN_POINT('',(7.63534122785692,-1.17693546839596,13.4294624954408));
#26134=CARTESIAN_POINT('',(7.63534118037484,-1.17693559664385,13.0872737913614));
#26135=CARTESIAN_POINT('',(7.63534122785693,-1.17693546839596,11.));
#26136=CARTESIAN_POINT('',(7.84621822868222,0.00243910941253872,13.3589821967011));
#26137=CARTESIAN_POINT('Ctrl Pts',(7.84621822868283,0.00243910857111449,
13.3589821967504));
#26138=CARTESIAN_POINT('Ctrl Pts',(7.84629283776119,-0.101248796474601,
13.3650553057062));
#26139=CARTESIAN_POINT('Ctrl Pts',(7.84160563766044,-0.205006137387628,
13.3711284146619));
#26140=CARTESIAN_POINT('Ctrl Pts',(7.83216418985855,-0.308363040565317,
13.3772015236177));
#26141=CARTESIAN_POINT('Ctrl Pts',(7.82272594910728,-0.411684835693171,
13.3832725696729));
#26142=CARTESIAN_POINT('Ctrl Pts',(7.80853671345539,-0.514606036863708,
13.3893436157281));
#26143=CARTESIAN_POINT('Ctrl Pts',(7.78965603869954,-0.616660308140516,
13.3954146617833));
#26144=CARTESIAN_POINT('Ctrl Pts',(7.77077031345568,-0.718741878435034,
13.4014873318136));
#26145=CARTESIAN_POINT('Ctrl Pts',(7.74719071430171,-0.819955632267821,
13.4075600018439));
#26146=CARTESIAN_POINT('Ctrl Pts',(7.71902814867664,-0.91984431126849,13.4136326718741));
#26147=CARTESIAN_POINT('Ctrl Pts',(7.69455739458182,-1.00663865142994,13.4189092797297));
#26148=CARTESIAN_POINT('Ctrl Pts',(7.66662732283726,-1.09243253871243,13.4241858875853));
#26149=CARTESIAN_POINT('Ctrl Pts',(7.63534122785692,-1.17693546839597,13.4294624954408));
#26150=CARTESIAN_POINT('Ctrl Pts',(7.63534122785693,-1.17693546839596,12.1796263343991));
#26151=CARTESIAN_POINT('Ctrl Pts',(7.59924171155339,-1.27443932401376,12.1857302847185));
#26152=CARTESIAN_POINT('Ctrl Pts',(7.55861770762308,-1.37037367847503,12.1918342350379));
#26153=CARTESIAN_POINT('Ctrl Pts',(7.5136320904601,-1.46429489867357,12.1979381853572));
#26154=CARTESIAN_POINT('Ctrl Pts',(7.46867510623004,-1.5581563388765,12.2040382505682));
#26155=CARTESIAN_POINT('Ctrl Pts',(7.41936221301803,-1.6500068108107,12.2101383157791));
#26156=CARTESIAN_POINT('Ctrl Pts',(7.36590431060266,-1.73942285082974,12.2162383809901));
#26157=CARTESIAN_POINT('Ctrl Pts',(7.31246346601551,-1.82881035917466,12.2223364997374));
#26158=CARTESIAN_POINT('Ctrl Pts',(7.2548804594675,-1.91576461544835,12.2284346184847));
#26159=CARTESIAN_POINT('Ctrl Pts',(7.19341164031467,-1.99988765373304,12.234532737232));
#26160=CARTESIAN_POINT('Ctrl Pts',(7.13194677682776,-2.08400527849848,12.2406304635507));
#26161=CARTESIAN_POINT('Ctrl Pts',(7.06659684914164,-2.16529170479224,12.2467281898694));
#26162=CARTESIAN_POINT('Ctrl Pts',(6.9976604290699,-2.2433795316806,12.2528259161881));
#26163=CARTESIAN_POINT('Ctrl Pts',(6.92871088510468,-2.32148222467778,12.2589248033724));
#26164=CARTESIAN_POINT('Ctrl Pts',(6.85617377320426,-2.39638478970671,12.2650236905566));
#26165=CARTESIAN_POINT('Ctrl Pts',(6.78038608409376,-2.46775504101237,12.2711225777408));
#26166=CARTESIAN_POINT('Ctrl Pts',(6.7045217732068,-2.53919744804022,12.2772276309339));
#26167=CARTESIAN_POINT('Ctrl Pts',(6.62540063383492,-2.60710011987618,12.2833326841271));
#26168=CARTESIAN_POINT('Ctrl Pts',(6.54339438856573,-2.67116976779816,12.2894377373203));
#26169=CARTESIAN_POINT('Ctrl Pts',(6.46134143492393,-2.73527590792848,12.2955462677742));
#26170=CARTESIAN_POINT('Ctrl Pts',(6.37640044843766,-2.79554442959542,12.3016547982282));
#26171=CARTESIAN_POINT('Ctrl Pts',(6.28897236312811,-2.85172524551625,12.3077633286821));
#26172=CARTESIAN_POINT('Ctrl Pts',(6.20141581713618,-2.90798860957851,12.3138808345813));
#26173=CARTESIAN_POINT('Ctrl Pts',(6.1113652427459,-2.96015206216199,12.3199983404804));
#26174=CARTESIAN_POINT('Ctrl Pts',(6.0192463995132,-3.00801133542773,12.3261158463796));
#26175=CARTESIAN_POINT('Ctrl Pts',(5.97584577192874,-3.03055962655446,12.3289980318908));
#26176=CARTESIAN_POINT('Ctrl Pts',(5.93198634547982,-3.05215320939512,12.331880217402));
#26177=CARTESIAN_POINT('Ctrl Pts',(5.88771403383095,-3.07277448239907,12.3347624029133));
#26178=CARTESIAN_POINT('Ctrl Pts',(5.79374212281867,-3.11654496466023,12.3408800974789));
#26179=CARTESIAN_POINT('Ctrl Pts',(5.69761202737596,-3.1560699057085,12.3469977920445));
#26180=CARTESIAN_POINT('Ctrl Pts',(5.59974222852627,-3.19113328306858,12.3531154866101));
#26181=CARTESIAN_POINT('Ctrl Pts',(5.50199565204499,-3.22615251409901,12.35922547873));
#26182=CARTESIAN_POINT('Ctrl Pts',(5.40251412457098,-3.25672120866668,12.3653354708498));
#26183=CARTESIAN_POINT('Ctrl Pts',(5.30173822038799,-3.28267043535148,12.3714454629697));
#26184=CARTESIAN_POINT('Ctrl Pts',(5.20106084450981,-3.30859429155375,12.3775494813683));
#26185=CARTESIAN_POINT('Ctrl Pts',(5.09909201849968,-3.32990755705062,12.3836534997669));
#26186=CARTESIAN_POINT('Ctrl Pts',(4.99628888419061,-3.34649064989129,12.3897575181655));
#26187=CARTESIAN_POINT('Ctrl Pts',(4.89355347132187,-3.36306281863962,12.3958575155493));
#26188=CARTESIAN_POINT('Ctrl Pts',(4.78998526172517,-3.37491094449382,12.4019575129331));
#26189=CARTESIAN_POINT('Ctrl Pts',(4.68605226650424,-3.38196638584908,12.408057510317));
#26190=CARTESIAN_POINT('Ctrl Pts',(4.58215400582777,-3.3890194692665,12.4141554690737));
#26191=CARTESIAN_POINT('Ctrl Pts',(4.47789162550102,-3.39128302356307,12.4202534278303));
#26192=CARTESIAN_POINT('Ctrl Pts',(4.37373817058073,-3.38874027549892,12.426351386587));
#26193=CARTESIAN_POINT('Ctrl Pts',(4.26959298581961,-3.38619772933812,12.4324488611437));
#26194=CARTESIAN_POINT('Ctrl Pts',(4.16555713410043,-3.37884965056749,12.4385463357005));
#26195=CARTESIAN_POINT('Ctrl Pts',(4.0621026914221,-3.36673138123326,12.4446438102573));
#26196=CARTESIAN_POINT('Ctrl Pts',(3.95863010421886,-3.35461098651674,12.4507423542295));
#26197=CARTESIAN_POINT('Ctrl Pts',(3.85573955074917,-3.33771878829351,12.4568408982018));
#26198=CARTESIAN_POINT('Ctrl Pts',(3.75389614779341,-3.31614177932581,12.462939442174));
#26199=CARTESIAN_POINT('Ctrl Pts',(3.65195056971743,-3.29454312307,12.469044104554));
#26200=CARTESIAN_POINT('Ctrl Pts',(3.55105465609129,-3.26825036007636,12.4751487669339));
#26201=CARTESIAN_POINT('Ctrl Pts',(3.45166144513326,-3.23740121497551,12.4812534293139));
#26202=CARTESIAN_POINT('Ctrl Pts',(3.35221295032704,-3.20653491116292,12.4873614871896));
#26203=CARTESIAN_POINT('Ctrl Pts',(3.25426922269691,-3.17110732122112,12.4934695450653));
#26204=CARTESIAN_POINT('Ctrl Pts',(3.15826452624802,-3.13130482882844,12.4995776029411));
#26205=CARTESIAN_POINT('Ctrl Pts',(3.0621171747642,-3.09144319322556,12.5056947368854));
#26206=CARTESIAN_POINT('Ctrl Pts',(2.96791499270935,-3.04719385380684,12.5118118708297));
#26207=CARTESIAN_POINT('Ctrl Pts',(2.87606885046154,-2.99878977157521,12.517929004774));
#26208=CARTESIAN_POINT('Ctrl Pts',(2.82731833954408,-2.973097633816,12.5211758848044));
#26209=CARTESIAN_POINT('Ctrl Pts',(2.77923113941815,-2.94623572387818,12.5244227648349));
#26210=CARTESIAN_POINT('Ctrl Pts',(2.73186526944357,-2.91824376443813,12.5276696448653));
#26211=CARTESIAN_POINT('Ctrl Pts',(2.64262191263345,-2.86550333286866,12.5337871820969));
#26212=CARTESIAN_POINT('Ctrl Pts',(2.55565895113433,-2.8085820529641,12.5399047193284));
#26213=CARTESIAN_POINT('Ctrl Pts',(2.47139121516819,-2.7477028276297,12.54602225656));
#26214=CARTESIAN_POINT('Ctrl Pts',(2.38722962559938,-2.6869002877594,12.5521320879415));
#26215=CARTESIAN_POINT('Ctrl Pts',(2.30575685286816,-2.62214996278217,12.558241919323));
#26216=CARTESIAN_POINT('Ctrl Pts',(2.22736139037672,-2.55371961140524,12.5643517507045));
#26217=CARTESIAN_POINT('Ctrl Pts',(2.14904261733581,-2.48535620122465,12.5704556052144));
#26218=CARTESIAN_POINT('Ctrl Pts',(2.07379548602307,-2.41332020266512,12.5765594597244));
#26219=CARTESIAN_POINT('Ctrl Pts',(2.00197716475091,-2.33792095071066,12.5826633142343));
#26220=CARTESIAN_POINT('Ctrl Pts',(1.93020620209745,-2.26257141872127,12.5887631437251));
#26221=CARTESIAN_POINT('Ctrl Pts',(1.8618598449964,-2.18386335119967,12.5948629732159));
#26222=CARTESIAN_POINT('Ctrl Pts',(1.79725940115328,-2.10214385972707,12.6009628027067));
#26223=CARTESIAN_POINT('Ctrl Pts',(1.73268057287378,-2.02045171191905,12.6070605911704));
#26224=CARTESIAN_POINT('Ctrl Pts',(1.67184542949749,-1.93575047638809,12.6131583796341));
#26225=CARTESIAN_POINT('Ctrl Pts',(1.61503535218568,-1.84842075403421,12.6192561680979));
#26226=CARTESIAN_POINT('Ctrl Pts',(1.55822980625213,-1.76109799741638,12.6253534701799));
#26227=CARTESIAN_POINT('Ctrl Pts',(1.50544891930639,-1.67114752740054,12.6314507722618));
#26228=CARTESIAN_POINT('Ctrl Pts',(1.4569305466712,-1.57897862312647,12.6375480743438));
#26229=CARTESIAN_POINT('Ctrl Pts',(1.40840367996345,-1.48679358291633,12.6436464438756));
#26230=CARTESIAN_POINT('Ctrl Pts',(1.36414100829734,-1.39238971280386,12.6497448134073));
#26231=CARTESIAN_POINT('Ctrl Pts',(1.32433385594505,-1.29619976720259,12.6558431829391));
#26232=CARTESIAN_POINT('Ctrl Pts',(1.2844867784221,-1.19991334647645,12.6619476689205));
#26233=CARTESIAN_POINT('Ctrl Pts',(1.24910430528545,-1.10183766688726,12.6680521549019));
#26234=CARTESIAN_POINT('Ctrl Pts',(1.21832909176972,-1.00242421625141,12.6741566408834));
#26235=CARTESIAN_POINT('Ctrl Pts',(1.18753676689898,-0.902955490650669,
12.6802645210257));
#26236=CARTESIAN_POINT('Ctrl Pts',(1.16135691147584,-0.802147923491726,
12.6863724011681));
#26237=CARTESIAN_POINT('Ctrl Pts',(1.13988143393021,-0.700465041616654,
12.6924802813104));
#26238=CARTESIAN_POINT('Ctrl Pts',(1.11837404622141,-0.598631070325962,
12.6985972370811));
#26239=CARTESIAN_POINT('Ctrl Pts',(1.10158506425489,-0.495919606182577,
12.7047141928517));
#26240=CARTESIAN_POINT('Ctrl Pts',(1.0895547535995,-0.392801227887379,12.7108311486224));
#26241=CARTESIAN_POINT('Ctrl Pts',(1.08316572271305,-0.338037346657733,
12.7140797280206));
#26242=CARTESIAN_POINT('Ctrl Pts',(1.07811796237808,-0.28315874308651,12.7173283074189));
#26243=CARTESIAN_POINT('Ctrl Pts',(1.07441152813231,-0.228235845150309,
12.7205768868171));
#26244=CARTESIAN_POINT('Ctrl Pts',(1.06743161727289,-0.124805727059441,
12.726694571124));
#26245=CARTESIAN_POINT('Ctrl Pts',(1.06518963076198,-0.020891687627824,
12.7328122554308));
#26246=CARTESIAN_POINT('Ctrl Pts',(1.06773634292286,0.0830380724030555,
12.7389299397376));
#26247=CARTESIAN_POINT('Ctrl Pts',(1.07027984816573,0.186836960077974,12.7450399204208));
#26248=CARTESIAN_POINT('Ctrl Pts',(1.07760005143083,0.290651107318951,12.7511499011039));
#26249=CARTESIAN_POINT('Ctrl Pts',(1.08969583892884,0.394008666358254,12.7572598817871));
#26250=CARTESIAN_POINT('Ctrl Pts',(1.10177979810024,0.497265153270898,12.7633638875929));
#26251=CARTESIAN_POINT('Ctrl Pts',(1.11863000429741,0.600065519871241,12.7694678933986));
#26252=CARTESIAN_POINT('Ctrl Pts',(1.14019333927317,0.701940239673467,12.7755718992044));
#26253=CARTESIAN_POINT('Ctrl Pts',(1.16174246346846,0.803747821471268,12.7816718823167));
#26254=CARTESIAN_POINT('Ctrl Pts',(1.18799845112701,0.904630555004316,12.7877718654291));
#26255=CARTESIAN_POINT('Ctrl Pts',(1.21885674812158,1.0041271240235,12.7938718485414));
#26256=CARTESIAN_POINT('Ctrl Pts',(1.24970472697017,1.10359042419044,12.799969791991));
#26257=CARTESIAN_POINT('Ctrl Pts',(1.28515183016389,1.20166807570536,12.8060677354407));
#26258=CARTESIAN_POINT('Ctrl Pts',(1.32504330395334,1.29791275030704,12.8121656788904));
#26259=CARTESIAN_POINT('Ctrl Pts',(1.36493160354042,1.39414976662875,12.8182631371209));
#26260=CARTESIAN_POINT('Ctrl Pts',(1.4092634073296,1.4885537036636,12.8243605953514));
#26261=CARTESIAN_POINT('Ctrl Pts',(1.45783569400808,1.58069691012439,12.8304580535819));
#26262=CARTESIAN_POINT('Ctrl Pts',(1.5064164916417,1.67285626214371,12.836556580224));
#26263=CARTESIAN_POINT('Ctrl Pts',(1.55923905039582,1.76275372054627,12.8426551068661));
#26264=CARTESIAN_POINT('Ctrl Pts',(1.61605467255734,1.84998673172291,12.8487536335082));
#26265=CARTESIAN_POINT('Ctrl Pts',(1.67292728220228,1.93730723978136,12.8548582771244));
#26266=CARTESIAN_POINT('Ctrl Pts',(1.73380071967899,2.02195760801406,12.8609629207405));
#26267=CARTESIAN_POINT('Ctrl Pts',(1.79838331220078,2.10356482527697,12.8670675643567));
#26268=CARTESIAN_POINT('Ctrl Pts',(1.86300181767719,2.18521742251265,12.8731756026304));
#26269=CARTESIAN_POINT('Ctrl Pts',(1.93133330827163,2.26382317713033,12.8792836409042));
#26270=CARTESIAN_POINT('Ctrl Pts',(2.00304748164049,2.33904411983918,12.8853916791779));
#26271=CARTESIAN_POINT('Ctrl Pts',(2.07486820335519,2.41437682102814,12.8915087923854));
#26272=CARTESIAN_POINT('Ctrl Pts',(2.15008133734535,2.48631437397807,12.897625905593));
#26273=CARTESIAN_POINT('Ctrl Pts',(2.22832155775466,2.55455741074177,12.9037430188005));
#26274=CARTESIAN_POINT('Ctrl Pts',(2.26985240000642,2.59078162866687,12.9069900554567));
#26275=CARTESIAN_POINT('Ctrl Pts',(2.31223562210947,2.62596557660632,12.9102370921129));
#26276=CARTESIAN_POINT('Ctrl Pts',(2.35541325923941,2.66006943337501,12.9134841287691));
#26277=CARTESIAN_POINT('Ctrl Pts',(2.43676289320398,2.72432344191568,12.9196017688488));
#26278=CARTESIAN_POINT('Ctrl Pts',(2.52119126830436,2.78494389035308,12.9257194089284));
#26279=CARTESIAN_POINT('Ctrl Pts',(2.60834098847442,2.841624099508,12.9318370490081));
#26280=CARTESIAN_POINT('Ctrl Pts',(2.69538095956685,2.89823293034224,12.9379469850429));
#26281=CARTESIAN_POINT('Ctrl Pts',(2.7851351077961,2.95091115840678,12.9440569210777));
#26282=CARTESIAN_POINT('Ctrl Pts',(2.87721368190512,2.99939283310432,12.9501668571124));
#26283=CARTESIAN_POINT('Ctrl Pts',(2.96920220750083,3.047827095005,12.9562708179172));
#26284=CARTESIAN_POINT('Ctrl Pts',(3.06351026360784,3.09207276888496,12.962374778722));
#26285=CARTESIAN_POINT('Ctrl Pts',(3.15972060002561,3.131908104365,12.9684787395268));
#26286=CARTESIAN_POINT('Ctrl Pts',(3.2558675257344,3.17171718500633,12.9745786773077));
#26287=CARTESIAN_POINT('Ctrl Pts',(3.35391384652886,3.20712154625899,12.9806786150886));
#26288=CARTESIAN_POINT('Ctrl Pts',(3.45341999148072,3.23794649985516,12.9867785528696));
#26289=CARTESIAN_POINT('Ctrl Pts',(3.55289286117137,3.26876114546097,12.9928764508064));
#26290=CARTESIAN_POINT('Ctrl Pts',(3.65382417897349,3.29499930205128,12.9989743487432));
#26291=CARTESIAN_POINT('Ctrl Pts',(3.75575751735508,3.31653559180855,13.00507224668));
#26292=CARTESIAN_POINT('Ctrl Pts',(3.85768274271901,3.33807016746225,13.0111696592765));
#26293=CARTESIAN_POINT('Ctrl Pts',(3.96060941417043,3.35490353306712,13.017267071873));
#26294=CARTESIAN_POINT('Ctrl Pts',(4.06407003205697,3.36696124555918,13.0233644844696));
#26295=CARTESIAN_POINT('Ctrl Pts',(4.16754877766877,3.37902107072853,13.0294629654168));
#26296=CARTESIAN_POINT('Ctrl Pts',(4.27156123349589,3.38630353094607,13.035561446364));
#26297=CARTESIAN_POINT('Ctrl Pts',(4.3756347637861,3.38878604688812,13.0416599273112));
#26298=CARTESIAN_POINT('Ctrl Pts',(4.47981268632778,3.39127105294872,13.0477645254157));
#26299=CARTESIAN_POINT('Ctrl Pts',(4.58405138014277,3.38894649161483,13.0538691235202));
#26300=CARTESIAN_POINT('Ctrl Pts',(4.68787826684144,3.38184193345575,13.0599737216247));
#26301=CARTESIAN_POINT('Ctrl Pts',(4.79176289060649,3.37473342452477,13.0660817144336));
#26302=CARTESIAN_POINT('Ctrl Pts',(4.89523482901213,3.36283967216909,13.0721897072425));
#26303=CARTESIAN_POINT('Ctrl Pts',(4.9978285542204,3.3462419234955,13.0782977000514));
#26304=CARTESIAN_POINT('Ctrl Pts',(5.10057471614357,3.32961951340837,13.0844147682921));
#26305=CARTESIAN_POINT('Ctrl Pts',(5.20243964332922,3.30827923643923,13.0905318365328));
#26306=CARTESIAN_POINT('Ctrl Pts',(5.30296983350351,3.2823530555389,13.0966489047735));
#26307=CARTESIAN_POINT('Ctrl Pts',(5.35634027807688,3.26858911260453,13.0998963934227));
#26308=CARTESIAN_POINT('Ctrl Pts',(5.40933481077559,3.25353349967415,13.1031438820719));
#26309=CARTESIAN_POINT('Ctrl Pts',(5.46188777968828,3.23721150892829,13.1063913707211));
#26310=CARTESIAN_POINT('Ctrl Pts',(5.56088732379996,3.20646406161434,13.1125090059837));
#26311=CARTESIAN_POINT('Ctrl Pts',(5.65863159018404,3.17112253339257,13.1186266412464));
#26312=CARTESIAN_POINT('Ctrl Pts',(5.75466552655046,3.13130821171227,13.1247442765091));
#26313=CARTESIAN_POINT('Ctrl Pts',(5.85057852101174,3.09154403084778,13.1308542074279));
#26314=CARTESIAN_POINT('Ctrl Pts',(5.94478507870008,3.04731841852647,13.1369641383468));
#26315=CARTESIAN_POINT('Ctrl Pts',(6.03684543611479,2.99880238068512,13.1430740692656));
#26316=CARTESIAN_POINT('Ctrl Pts',(6.12881575838942,2.95033379158704,13.1491780246647));
#26317=CARTESIAN_POINT('Ctrl Pts',(6.21864368080046,2.89758331959839,13.1552819800638));
#26318=CARTESIAN_POINT('Ctrl Pts',(6.30591033829472,2.84076964775314,13.1613859354628));
#26319=CARTESIAN_POINT('Ctrl Pts',(6.39311947380145,2.78399342475053,13.1674858674278));
#26320=CARTESIAN_POINT('Ctrl Pts',(6.47777034684508,2.72315955986921,13.1735857993927));
#26321=CARTESIAN_POINT('Ctrl Pts',(6.55947027975403,2.65853176144412,13.1796857313577));
#26322=CARTESIAN_POINT('Ctrl Pts',(6.64114288847495,2.59392557750576,13.1857836232269));
#26323=CARTESIAN_POINT('Ctrl Pts',(6.71986618601038,2.52552824588085,13.1918815150961));
#26324=CARTESIAN_POINT('Ctrl Pts',(6.79527862666104,2.45364526563768,13.1979794069653));
#26325=CARTESIAN_POINT('Ctrl Pts',(6.87068506210165,2.38176800954813,13.2040768132498));
#26326=CARTESIAN_POINT('Ctrl Pts',(6.94278085764178,2.30640595036319,13.2101742195344));
#26327=CARTESIAN_POINT('Ctrl Pts',(7.01124021072977,2.22790252615616,13.216271625819));
#26328=CARTESIAN_POINT('Ctrl Pts',(7.07971155618826,2.14938535010799,13.222370100217));
#26329=CARTESIAN_POINT('Ctrl Pts',(7.14454491413589,2.06772603590349,13.228468574615));
#26330=CARTESIAN_POINT('Ctrl Pts',(7.20545434862895,1.98330159065841,13.234567049013));
#26331=CARTESIAN_POINT('Ctrl Pts',(7.26642487592567,1.89879246680648,13.240671640245));
#26332=CARTESIAN_POINT('Ctrl Pts',(7.32346337260496,1.81151301957376,13.246776231477));
#26333=CARTESIAN_POINT('Ctrl Pts',(7.37632694268223,1.7218697039381,13.252880822709));
#26334=CARTESIAN_POINT('Ctrl Pts',(7.42921990801619,1.63217654134226,13.258988808453));
#26335=CARTESIAN_POINT('Ctrl Pts',(7.47793312346699,1.54011726738474,13.2650967941971));
#26336=CARTESIAN_POINT('Ctrl Pts',(7.5222702978688,1.44612174998307,13.2712047799411));
#26337=CARTESIAN_POINT('Ctrl Pts',(7.56667334808656,1.35198657480011,13.2773218408811));
#26338=CARTESIAN_POINT('Ctrl Pts',(7.6066872097305,1.25590980320544,13.2834389018211));
#26339=CARTESIAN_POINT('Ctrl Pts',(7.64216421798083,1.15834006983787,13.2895559627611));
#26340=CARTESIAN_POINT('Ctrl Pts',(7.66099897510223,1.10654026142646,13.2928035127317));
#26341=CARTESIAN_POINT('Ctrl Pts',(7.67855584428645,1.05431990122149,13.2960510627023));
#26342=CARTESIAN_POINT('Ctrl Pts',(7.69481855117705,1.00174744064313,13.299298612673));
#26343=CARTESIAN_POINT('Ctrl Pts',(7.73124472625844,0.883992526509213,13.3065726676388));
#26344=CARTESIAN_POINT('Ctrl Pts',(7.7612676626192,0.764172971569869,13.3138467226047));
#26345=CARTESIAN_POINT('Ctrl Pts',(7.78468903878415,0.642928567549356,13.3211207775705));
#26346=CARTESIAN_POINT('Ctrl Pts',(7.80788532081294,0.52284939840633,13.3283249242992));
#26347=CARTESIAN_POINT('Ctrl Pts',(7.82460627941273,0.401372698938182,13.3355290710279));
#26348=CARTESIAN_POINT('Ctrl Pts',(7.83470626179514,0.27913936157369,13.3427332177567));
#26349=CARTESIAN_POINT('Ctrl Pts',(7.8422997773657,0.187240117062702,13.3481495440715));
#26350=CARTESIAN_POINT('Ctrl Pts',(7.84615168825675,0.0949135788670932,
13.3535658703863));
#26351=CARTESIAN_POINT('Ctrl Pts',(7.84621822868222,0.00243910941253646,
13.3589821967011));
#26352=CARTESIAN_POINT('Ctrl Pts',(7.6353412143218,-1.17693550495398,11.8350241089739));
#26353=CARTESIAN_POINT('Ctrl Pts',(7.59939412479864,-1.27402765636897,11.8406579393705));
#26354=CARTESIAN_POINT('Ctrl Pts',(7.55901381146477,-1.36943260069423,11.8463767776613));
#26355=CARTESIAN_POINT('Ctrl Pts',(7.48271919242755,-1.52891420592338,11.8563684436921));
#26356=CARTESIAN_POINT('Ctrl Pts',(7.44898437731065,-1.59393207582782,11.8605705113664));
#26357=CARTESIAN_POINT('Ctrl Pts',(7.37777340050005,-1.72093732018166,11.8690677127489));
#26358=CARTESIAN_POINT('Ctrl Pts',(7.34036371683698,-1.78291748472974,11.8733589661347));
#26359=CARTESIAN_POINT('Ctrl Pts',(7.23141182631281,-1.95101727885506,11.8854234247197));
#26360=CARTESIAN_POINT('Ctrl Pts',(7.15580663627251,-2.05434823706306,11.8933343672199));
#26361=CARTESIAN_POINT('Ctrl Pts',(6.9237314505997,-2.33653535712539,11.9163500508177));
#26362=CARTESIAN_POINT('Ctrl Pts',(6.75407388599113,-2.50355444928424,11.931795940656));
#26363=CARTESIAN_POINT('Ctrl Pts',(6.50706173627038,-2.70029944414172,11.9516617985081));
#26364=CARTESIAN_POINT('Ctrl Pts',(6.44407945362782,-2.74699000628053,11.956524804522));
#26365=CARTESIAN_POINT('Ctrl Pts',(6.34531078721631,-2.81503267195845,11.963784911166));
#26366=CARTESIAN_POINT('Ctrl Pts',(6.31065742938208,-2.83797782725912,11.9662660369821));
#26367=CARTESIAN_POINT('Ctrl Pts',(6.23512791481641,-2.88601402732262,11.9715212601879));
#26368=CARTESIAN_POINT('Ctrl Pts',(6.19412507662408,-2.91088583940233,11.9742835275195));
#26369=CARTESIAN_POINT('Ctrl Pts',(6.02296686748904,-3.00980221776042,11.9855023245916));
#26370=CARTESIAN_POINT('Ctrl Pts',(5.88849332338007,-3.07605909063025,11.9935928935305));
#26371=CARTESIAN_POINT('Ctrl Pts',(5.59564813971285,-3.19696518230707,12.0105678650837));
#26372=CARTESIAN_POINT('Ctrl Pts',(5.43673052756863,-3.24921549845157,12.0194182542229));
#26373=CARTESIAN_POINT('Ctrl Pts',(5.16297343628663,-3.31730167323249,12.0347829003798));
#26374=CARTESIAN_POINT('Ctrl Pts',(5.05000409631921,-3.33936395396416,12.0411530313047));
#26375=CARTESIAN_POINT('Ctrl Pts',(4.86542865271063,-3.36574793624902,12.0517511978732));
#26376=CARTESIAN_POINT('Ctrl Pts',(4.79442123605421,-3.37361740332017,12.0558724504454));
#26377=CARTESIAN_POINT('Ctrl Pts',(4.64721185745451,-3.38523791809803,12.0645325923212));
#26378=CARTESIAN_POINT('Ctrl Pts',(4.57102606595582,-3.38867140970339,12.0690784597731));
#26379=CARTESIAN_POINT('Ctrl Pts',(4.20637445379349,-3.39279440411933,12.0911712598678));
#26380=CARTESIAN_POINT('Ctrl Pts',(3.91875224933209,-3.35922767031148,12.1097366117395));
#26381=CARTESIAN_POINT('Ctrl Pts',(3.51999442944,-3.26012822152478,12.1359373946312));
#26382=CARTESIAN_POINT('Ctrl Pts',(3.40275317250551,-3.22414458090072,12.1436784140135));
#26383=CARTESIAN_POINT('Ctrl Pts',(3.24406718969492,-3.16585665797537,12.1540035090913));
#26384=CARTESIAN_POINT('Ctrl Pts',(3.20075584311501,-3.14892862338292,12.1568050012285));
#26385=CARTESIAN_POINT('Ctrl Pts',(3.11826335098376,-3.11471392803585,12.1620906774738));
#26386=CARTESIAN_POINT('Ctrl Pts',(3.07903599894315,-3.09756609483025,12.1645804651959));
#26387=CARTESIAN_POINT('Ctrl Pts',(2.9611219389252,-3.04333811757872,12.1720207928299));
#26388=CARTESIAN_POINT('Ctrl Pts',(2.88352299211825,-3.0039661795607,12.1768580591568));
#26389=CARTESIAN_POINT('Ctrl Pts',(2.56983477908364,-2.8293148452143,12.1964960817438));
#26390=CARTESIAN_POINT('Ctrl Pts',(2.34894263725578,-2.66884908466894,12.210608147046));
#26391=CARTESIAN_POINT('Ctrl Pts',(2.07601817461247,-2.41535576104555,12.2310706382502));
#26392=CARTESIAN_POINT('Ctrl Pts',(2.00551506299891,-2.34378154487994,12.23667974451));
#26393=CARTESIAN_POINT('Ctrl Pts',(1.89155580699101,-2.21731819085286,12.2464087645975));
#26394=CARTESIAN_POINT('Ctrl Pts',(1.84643145505943,-2.16402002049441,12.2504588488683));
#26395=CARTESIAN_POINT('Ctrl Pts',(1.75292972627744,-2.04639947403242,12.2593141725608));
#26396=CARTESIAN_POINT('Ctrl Pts',(1.70513306459173,-1.98167212289564,12.2641378871508));
#26397=CARTESIAN_POINT('Ctrl Pts',(1.51596121347347,-1.70543871393861,12.2845467611581));
#26398=CARTESIAN_POINT('Ctrl Pts',(1.39633239272305,-1.48008013236416,12.300863095758));
#26399=CARTESIAN_POINT('Ctrl Pts',(1.26756112844971,-1.15352786223426,12.3233147791539));
#26400=CARTESIAN_POINT('Ctrl Pts',(1.23594445242736,-1.06206553357178,12.3294729747448));
#26401=CARTESIAN_POINT('Ctrl Pts',(1.18872657029609,-0.903847210691334,
12.3397915948604));
#26402=CARTESIAN_POINT('Ctrl Pts',(1.17115733061626,-0.837740332106849,
12.3440059256093));
#26403=CARTESIAN_POINT('Ctrl Pts',(1.1463787369525,-0.731675804999072,12.3505691078849));
#26404=CARTESIAN_POINT('Ctrl Pts',(1.13786661108437,-0.69204464645415,12.3529770085836));
#26405=CARTESIAN_POINT('Ctrl Pts',(1.12009369889256,-0.601406870737667,
12.3583759504963));
#26406=CARTESIAN_POINT('Ctrl Pts',(1.11128813892158,-0.55032354653126,12.3613451447146));
#26407=CARTESIAN_POINT('Ctrl Pts',(1.06453215217256,-0.236202091498968,
12.3792610135361));
#26408=CARTESIAN_POINT('Ctrl Pts',(1.05644910169118,0.0303660499579962,
12.3930626936703));
#26409=CARTESIAN_POINT('Ctrl Pts',(1.09191895413979,0.436166562009752,12.415016004438));
#26410=CARTESIAN_POINT('Ctrl Pts',(1.11306186505697,0.576247973025385,12.4227574877883));
#26411=CARTESIAN_POINT('Ctrl Pts',(1.15848830373778,0.786891539037361,12.4349288004372));
#26412=CARTESIAN_POINT('Ctrl Pts',(1.1764417810872,0.85865899249561,12.4391703511497));
#26413=CARTESIAN_POINT('Ctrl Pts',(1.21661518773907,0.999504326079326,12.4477134786788));
#26414=CARTESIAN_POINT('Ctrl Pts',(1.23873399972851,1.06857004365929,12.4520099754027));
#26415=CARTESIAN_POINT('Ctrl Pts',(1.30552719999954,1.25618935389685,12.4639976465676));
#26416=CARTESIAN_POINT('Ctrl Pts',(1.35465512984795,1.37302261147682,12.4718215591557));
#26417=CARTESIAN_POINT('Ctrl Pts',(1.51479286503673,1.70111972168263,12.4947970005818));
#26418=CARTESIAN_POINT('Ctrl Pts',(1.64169858755669,1.90376616259543,12.5102993430162));
#26419=CARTESIAN_POINT('Ctrl Pts',(1.83730522303411,2.15326804677619,12.5302357786496));
#26420=CARTESIAN_POINT('Ctrl Pts',(1.88793913090982,2.21342229628961,12.5351112721881));
#26421=CARTESIAN_POINT('Ctrl Pts',(1.96856950286904,2.30271569972786,12.5423920715016));
#26422=CARTESIAN_POINT('Ctrl Pts',(1.99708783076453,2.33314989176322,12.5448814009696));
#26423=CARTESIAN_POINT('Ctrl Pts',(2.05971417491399,2.39755857450699,12.55015445583));
#26424=CARTESIAN_POINT('Ctrl Pts',(2.09399765259246,2.43134746031777,12.5529262038059));
#26425=CARTESIAN_POINT('Ctrl Pts',(2.22359553564354,2.55374506318365,12.5630393415191));
#26426=CARTESIAN_POINT('Ctrl Pts',(2.32327505129667,2.6375797846765,12.5701152373717));
#26427=CARTESIAN_POINT('Ctrl Pts',(2.5848749665293,2.833040088811,12.5876670197476));
#26428=CARTESIAN_POINT('Ctrl Pts',(2.75212912853562,2.93669968774034,12.5980235958127));
#26429=CARTESIAN_POINT('Ctrl Pts',(3.02476398440121,3.07449552821056,12.6147137268906));
#26430=CARTESIAN_POINT('Ctrl Pts',(3.12442190893559,3.11896611154662,12.6207731176418));
#26431=CARTESIAN_POINT('Ctrl Pts',(3.29190333729299,3.18420904588795,12.6310095543348));
#26432=CARTESIAN_POINT('Ctrl Pts',(3.35854486819454,3.20779706586694,12.6350952727651));
#26433=CARTESIAN_POINT('Ctrl Pts',(3.49964936771098,3.25282931956057,12.6437965943737));
#26434=CARTESIAN_POINT('Ctrl Pts',(3.57420744985247,3.2738380471302,12.6484229844899));
#26435=CARTESIAN_POINT('Ctrl Pts',(3.89666806233474,3.35288463269726,12.6685793779479));
#26436=CARTESIAN_POINT('Ctrl Pts',(4.14993097592737,3.38544104252741,12.6848614926114));
#26437=CARTESIAN_POINT('Ctrl Pts',(4.5065347992183,3.39091900890328,12.7076852506868));
#26438=CARTESIAN_POINT('Ctrl Pts',(4.60868905497216,3.38787088068285,12.7141992932499));
#26439=CARTESIAN_POINT('Ctrl Pts',(4.7810628131189,3.3749138758117,12.725017599064));
#26440=CARTESIAN_POINT('Ctrl Pts',(4.8513942573988,3.36740853466274,12.7293818736601));
#26441=CARTESIAN_POINT('Ctrl Pts',(4.96185500546183,3.35211195056281,12.7361082266828));
#26442=CARTESIAN_POINT('Ctrl Pts',(5.00216406107272,3.34578646349311,12.7385347970792));
#26443=CARTESIAN_POINT('Ctrl Pts',(5.09247575967662,3.32993845836428,12.7438998099865));
#26444=CARTESIAN_POINT('Ctrl Pts',(5.142395913438,3.32001500209211,12.746818944577));
#26445=CARTESIAN_POINT('Ctrl Pts',(5.37801584642126,3.26763503907511,12.7604545105832));
#26446=CARTESIAN_POINT('Ctrl Pts',(5.56015879023537,3.21069621808778,12.7705858259196));
#26447=CARTESIAN_POINT('Ctrl Pts',(5.86470278742348,3.08649197024779,12.7881558314274));
#26448=CARTESIAN_POINT('Ctrl Pts',(5.9895142863646,3.0264376557331,12.7955535988208));
#26449=CARTESIAN_POINT('Ctrl Pts',(6.20122032760839,2.90810881486592,12.8088433710381));
#26450=CARTESIAN_POINT('Ctrl Pts',(6.28974217509598,2.85313177000169,12.8146465952904));
#26451=CARTESIAN_POINT('Ctrl Pts',(6.43341893650006,2.75445031050719,12.8245917401459));
#26452=CARTESIAN_POINT('Ctrl Pts',(6.48999944734876,2.71294682648828,12.82865468865));
#26453=CARTESIAN_POINT('Ctrl Pts',(6.60742021645467,2.62107721505996,12.8374279275551));
#26454=CARTESIAN_POINT('Ctrl Pts',(6.66786933557167,2.57028091566056,12.8421529970381));
#26455=CARTESIAN_POINT('Ctrl Pts',(6.92442278681109,2.33894088160492,12.8631703412766));
#26456=CARTESIAN_POINT('Ctrl Pts',(7.10059453398932,2.13775607919232,12.8802905622182));
#26457=CARTESIAN_POINT('Ctrl Pts',(7.30368557874387,1.84182351181568,12.9032273525282));
#26458=CARTESIAN_POINT('Ctrl Pts',(7.35286906891361,1.7634693865021,12.9091049078491));
#26459=CARTESIAN_POINT('Ctrl Pts',(7.43180014423054,1.6254937466807,12.919024677382));
#26460=CARTESIAN_POINT('Ctrl Pts',(7.46310890545218,1.56682577365974,12.9231160110645));
#26461=CARTESIAN_POINT('Ctrl Pts',(7.51062329382593,1.47111412955073,12.9295483015617));
#26462=CARTESIAN_POINT('Ctrl Pts',(7.52792616979899,1.43463815450433,12.9319437576622));
#26463=CARTESIAN_POINT('Ctrl Pts',(7.56598182415703,1.35056666294337,12.9373326001084));
#26464=CARTESIAN_POINT('Ctrl Pts',(7.58630027160577,1.30278822334662,12.9403037975482));
#26465=CARTESIAN_POINT('Ctrl Pts',(7.66006920353912,1.11762223201926,12.9515389208032));
#26466=CARTESIAN_POINT('Ctrl Pts',(7.7056385530825,0.977260540281947,12.9594778719187));
#26467=CARTESIAN_POINT('Ctrl Pts',(7.78167456611536,0.677856454243271,12.9760106523204));
#26468=CARTESIAN_POINT('Ctrl Pts',(7.81018681229028,0.51870657280797,12.9845782001725));
#26469=CARTESIAN_POINT('Ctrl Pts',(7.83918761306181,0.245751029150855,12.9995425814277));
#26470=CARTESIAN_POINT('Ctrl Pts',(7.84549940580953,0.13284753890433,13.0058069524936));
#26471=CARTESIAN_POINT('Ctrl Pts',(7.84657713646169,-0.051228267440547,
13.0162761682707));
#26472=CARTESIAN_POINT('Ctrl Pts',(7.84475774865628,-0.122294007574997,
13.0203792879573));
#26473=CARTESIAN_POINT('Ctrl Pts',(7.83635119928191,-0.269513960458309,
13.0290315105716));
#26474=CARTESIAN_POINT('Ctrl Pts',(7.82941958043541,-0.345607415734581,
13.0335885742225));
#26475=CARTESIAN_POINT('Ctrl Pts',(7.79843587348286,-0.592908989731343,
13.0486968707893));
#26476=CARTESIAN_POINT('Ctrl Pts',(7.76386322198776,-0.762505344958133,
13.0595433922846));
#26477=CARTESIAN_POINT('Ctrl Pts',(7.6926492407927,-1.01248795280147,13.0761160301206));
#26478=CARTESIAN_POINT('Ctrl Pts',(7.66556896018746,-1.09529115884783,13.0817024939094));
#26479=CARTESIAN_POINT('Ctrl Pts',(7.63534118037484,-1.17693559664385,13.0872737913614));
#26480=CARTESIAN_POINT('Origin',(4.45646910621825,3.5527136788005E-15,11.));
#26481=CARTESIAN_POINT('',(7.63534122785693,-1.17693546839596,14.6796206134749));
#26482=CARTESIAN_POINT('',(7.63534113152507,-1.17693572858576,14.3356579957882));
#26483=CARTESIAN_POINT('',(7.63534122785693,-1.17693546839596,11.));
#26484=CARTESIAN_POINT('',(7.84621807431328,-0.00264495721902113,14.6089821967061));
#26485=CARTESIAN_POINT('Ctrl Pts',(7.84621807431269,-0.0026449579738531,
14.6089821967504));
#26486=CARTESIAN_POINT('Ctrl Pts',(7.8461078714415,-0.143879742266134,14.6172792981224));
#26487=CARTESIAN_POINT('Ctrl Pts',(7.83716707831609,-0.284765752000311,
14.6255763994944));
#26488=CARTESIAN_POINT('Ctrl Pts',(7.8195478372724,-0.424389574838021,14.6338735008664));
#26489=CARTESIAN_POINT('Ctrl Pts',(7.80838097683225,-0.512881453681321,
14.6391321026897));
#26490=CARTESIAN_POINT('Ctrl Pts',(7.79372905419119,-0.600866932194777,
14.6443907045131));
#26491=CARTESIAN_POINT('Ctrl Pts',(7.77564046454811,-0.688118126881346,
14.6496493063364));
#26492=CARTESIAN_POINT('Ctrl Pts',(7.75459665394175,-0.789623974069688,
14.6557670315438));
#26493=CARTESIAN_POINT('Ctrl Pts',(7.72885907290368,-0.89032385383473,14.6618847567511));
#26494=CARTESIAN_POINT('Ctrl Pts',(7.69850452231244,-0.989753213326928,
14.6680024819585));
#26495=CARTESIAN_POINT('Ctrl Pts',(7.67928914682901,-1.05269509319353,14.671875192464));
#26496=CARTESIAN_POINT('Ctrl Pts',(7.65822466204407,-1.11512790720145,14.6757479029694));
#26497=CARTESIAN_POINT('Ctrl Pts',(7.63534122785692,-1.17693546839596,14.6796206134749));
#26498=CARTESIAN_POINT('Ctrl Pts',(7.63534122785692,-1.17693546839597,13.4294624954408));
#26499=CARTESIAN_POINT('Ctrl Pts',(7.59929922010739,-1.27428399490357,13.4355412195942));
#26500=CARTESIAN_POINT('Ctrl Pts',(7.55880248267084,-1.36991849247735,13.4416199437476));
#26501=CARTESIAN_POINT('Ctrl Pts',(7.51405356222015,-1.46341462235265,13.4476986679009));
#26502=CARTESIAN_POINT('Ctrl Pts',(7.46927795159138,-1.55696651733538,13.4537810176665));
#26503=CARTESIAN_POINT('Ctrl Pts',(7.42024531040631,-1.64837712732693,13.459863367432));
#26504=CARTESIAN_POINT('Ctrl Pts',(7.36720343152648,-1.73724803927718,13.4659457171975));
#26505=CARTESIAN_POINT('Ctrl Pts',(7.31408188775627,-1.82625242861565,13.4720372021924));
#26506=CARTESIAN_POINT('Ctrl Pts',(7.25693932145514,-1.9127091478361,13.4781286871872));
#26507=CARTESIAN_POINT('Ctrl Pts',(7.19606594651401,-1.99625003823206,13.4842201721821));
#26508=CARTESIAN_POINT('Ctrl Pts',(7.16946512903899,-2.03275624442273,13.4868820663297));
#26509=CARTESIAN_POINT('Ctrl Pts',(7.14215239520289,-2.06870609562014,13.4895439604773));
#26510=CARTESIAN_POINT('Ctrl Pts',(7.11415422067151,-2.10407102896113,13.4922058546248));
#26511=CARTESIAN_POINT('Ctrl Pts',(7.04980801601922,-2.18534772918755,13.4983234958086));
#26512=CARTESIAN_POINT('Ctrl Pts',(6.98162835676472,-2.26379847575191,13.5044411369924));
#26513=CARTESIAN_POINT('Ctrl Pts',(6.9098923138079,-2.33904245941807,13.5105587781762));
#26514=CARTESIAN_POINT('Ctrl Pts',(6.83824661186574,-2.41419168433323,13.516668715089));
#26515=CARTESIAN_POINT('Ctrl Pts',(6.76305372283813,-2.48614187112884,13.5227786520018));
#26516=CARTESIAN_POINT('Ctrl Pts',(6.68463159050479,-2.55454438327425,13.5288885889146));
#26517=CARTESIAN_POINT('Ctrl Pts',(6.60628615420595,-2.62287999847009,13.5349925503723));
#26518=CARTESIAN_POINT('Ctrl Pts',(6.52471807458976,-2.68767456155618,13.54109651183));
#26519=CARTESIAN_POINT('Ctrl Pts',(6.4402822431893,-2.74861610634899,13.5472004732877));
#26520=CARTESIAN_POINT('Ctrl Pts',(6.35590206676477,-2.8095174821738,13.5533004113845));
#26521=CARTESIAN_POINT('Ctrl Pts',(6.26865824172616,-2.86657064266844,13.5594003494812));
#26522=CARTESIAN_POINT('Ctrl Pts',(6.17893822835096,-2.9195042705568,13.565500287578));
#26523=CARTESIAN_POINT('Ctrl Pts',(6.08924822078695,-2.97242019541118,13.5715981856216));
#26524=CARTESIAN_POINT('Ctrl Pts',(5.99708403686773,-3.02121911075121,13.5776960836653));
#26525=CARTESIAN_POINT('Ctrl Pts',(5.9028609070006,-3.06567379561648,13.5837939817089));
#26526=CARTESIAN_POINT('Ctrl Pts',(5.80864527971112,-3.11012494074873,13.5898913942035));
#26527=CARTESIAN_POINT('Ctrl Pts',(5.71237141703989,-3.15023236235972,13.5959888066981));
#26528=CARTESIAN_POINT('Ctrl Pts',(5.61447706529752,-3.18581584985841,13.6020862191926));
#26529=CARTESIAN_POINT('Ctrl Pts',(5.5165655644685,-3.22140557085576,13.6081846998291));
#26530=CARTESIAN_POINT('Ctrl Pts',(5.41703340990849,-3.25246963786218,13.6142831804655));
#26531=CARTESIAN_POINT('Ctrl Pts',(5.31633530185756,-3.27887712305551,13.6203816611019));
#26532=CARTESIAN_POINT('Ctrl Pts',(5.2155361925113,-3.3053110952431,13.6264862585806));
#26533=CARTESIAN_POINT('Ctrl Pts',(5.11356920641443,-3.32707905227634,13.6325908560593));
#26534=CARTESIAN_POINT('Ctrl Pts',(5.0109010101027,-3.34410082480404,13.638695453538));
#26535=CARTESIAN_POINT('Ctrl Pts',(4.90817572407401,-3.36113206246515,13.6448034455416));
#26536=CARTESIAN_POINT('Ctrl Pts',(4.80474887296885,-3.37341180815158,13.6509114375451));
#26537=CARTESIAN_POINT('Ctrl Pts',(4.70109217569869,-3.38091180251392,13.6570194295487));
#26538=CARTESIAN_POINT('Ctrl Pts',(4.59728146691846,-3.38842294025135,13.6631364967118));
#26539=CARTESIAN_POINT('Ctrl Pts',(4.4932406545901,-3.39114013356474,13.669253563875));
#26540=CARTESIAN_POINT('Ctrl Pts',(4.38944144750029,-3.38908724518369,13.6753706310381));
#26541=CARTESIAN_POINT('Ctrl Pts',(4.33433550805494,-3.3879973876984,13.678618119551));
#26542=CARTESIAN_POINT('Ctrl Pts',(4.27929758883208,-3.38556399141405,13.681865608064));
#26543=CARTESIAN_POINT('Ctrl Pts',(4.22439740407751,-3.38179653254974,13.6851130965769));
#26544=CARTESIAN_POINT('Ctrl Pts',(4.12097530172035,-3.37469931570006,13.6912307825353));
#26545=CARTESIAN_POINT('Ctrl Pts',(4.01771563058386,-3.36284229879227,13.6973484684937));
#26546=CARTESIAN_POINT('Ctrl Pts',(3.91508915340603,-3.3462386061357,13.7034661544522));
#26547=CARTESIAN_POINT('Ctrl Pts',(3.81259191307791,-3.32965582240041,13.7095761364488));
#26548=CARTESIAN_POINT('Ctrl Pts',(3.71072669758179,-3.30833831589669,13.7156861184454));
#26549=CARTESIAN_POINT('Ctrl Pts',(3.60996085344077,-3.2823511147468,13.721796100442));
#26550=CARTESIAN_POINT('Ctrl Pts',(3.50929355255171,-3.25638932759839,13.7279001072245));
#26551=CARTESIAN_POINT('Ctrl Pts',(3.40972389432364,-3.22576703404182,13.734004114007));
#26552=CARTESIAN_POINT('Ctrl Pts',(3.31170988001849,-3.19060047272148,13.7401081207895));
#26553=CARTESIAN_POINT('Ctrl Pts',(3.2137604675027,-3.15545708995169,13.7462081043742));
#26554=CARTESIAN_POINT('Ctrl Pts',(3.11736505866215,-3.11577553953006,13.7523080879589));
#26555=CARTESIAN_POINT('Ctrl Pts',(3.02296655182748,-3.07172190945976,13.7584080715437));
#26556=CARTESIAN_POINT('Ctrl Pts',(2.92859961403187,-3.02768301193996,13.7645060151532));
#26557=CARTESIAN_POINT('Ctrl Pts',(2.83622863543238,-2.97927512095402,13.7706039587626));
#26558=CARTESIAN_POINT('Ctrl Pts',(2.74627585447121,-2.92671216626761,13.7767019023721));
#26559=CARTESIAN_POINT('Ctrl Pts',(2.65633023574562,-2.8741533967577,13.7827993604501));
#26560=CARTESIAN_POINT('Ctrl Pts',(2.56880279846301,-2.81744043624613,13.7888968185281));
#26561=CARTESIAN_POINT('Ctrl Pts',(2.48408974638786,-2.7568323712941,13.794994276606));
#26562=CARTESIAN_POINT('Ctrl Pts',(2.39936185502347,-2.69621368955298,13.8010928027832));
#26563=CARTESIAN_POINT('Ctrl Pts',(2.31744967407315,-2.63169879489073,13.8071913289604));
#26564=CARTESIAN_POINT('Ctrl Pts',(2.23871835293567,-2.56358862901491,13.8132898551376));
#26565=CARTESIAN_POINT('Ctrl Pts',(2.15990806840072,-2.49541015220486,13.8193944978176));
#26566=CARTESIAN_POINT('Ctrl Pts',(2.08428533522398,-2.4236294831259,13.8254991404976));
#26567=CARTESIAN_POINT('Ctrl Pts',(2.01218021056879,-2.34858614002228,13.8316037831775));
#26568=CARTESIAN_POINT('Ctrl Pts',(1.94003499301122,-2.27350107026686,13.8377118202465));
#26569=CARTESIAN_POINT('Ctrl Pts',(1.87141156017656,-2.1951500321528,13.8438198573155));
#26570=CARTESIAN_POINT('Ctrl Pts',(1.80660001705502,-2.1139060700034,13.8499278943845));
#26571=CARTESIAN_POINT('Ctrl Pts',(1.74169218537689,-2.03254140614763,13.8560450059802));
#26572=CARTESIAN_POINT('Ctrl Pts',(1.68060780208891,-1.94827557919912,13.8621621175758));
#26573=CARTESIAN_POINT('Ctrl Pts',(1.62359398184741,-1.86151110451184,13.8682792291714));
#26574=CARTESIAN_POINT('Ctrl Pts',(1.59333035991995,-1.81545547716486,13.8715262656238));
#26575=CARTESIAN_POINT('Ctrl Pts',(1.5642128977516,-1.76869626324997,13.8747733020763));
#26576=CARTESIAN_POINT('Ctrl Pts',(1.5362731965169,-1.72129628811065,13.8780203385288));
#26577=CARTESIAN_POINT('Ctrl Pts',(1.48363383219249,-1.63199309408694,13.8841378676089));
#26578=CARTESIAN_POINT('Ctrl Pts',(1.43501147634242,-1.54013187947467,13.8902553966891));
#26579=CARTESIAN_POINT('Ctrl Pts',(1.39066155975781,-1.44610827760795,13.8963729257693));
#26580=CARTESIAN_POINT('Ctrl Pts',(1.34636749575522,-1.35220308545513,13.9024827506683));
#26581=CARTESIAN_POINT('Ctrl Pts',(1.3063353522736,-1.25614130243304,13.9085925755673));
#26582=CARTESIAN_POINT('Ctrl Pts',(1.27077582408489,-1.15834510171639,13.9147024004663));
#26583=CARTESIAN_POINT('Ctrl Pts',(1.23525107195512,-1.06064454249481,13.9208062501557));
#26584=CARTESIAN_POINT('Ctrl Pts',(1.20419038018315,-0.961213336674987,
13.9269100998452));
#26585=CARTESIAN_POINT('Ctrl Pts',(1.17775692561686,-0.860494915310985,
13.9330139495347));
#26586=CARTESIAN_POINT('Ctrl Pts',(1.1513408911021,-0.759842868929724,13.9391137766937));
#26587=CARTESIAN_POINT('Ctrl Pts',(1.12954613655457,-0.65790570418471,13.9452136038527));
#26588=CARTESIAN_POINT('Ctrl Pts',(1.11248618679602,-0.555142591693679,
13.9513134310117));
#26589=CARTESIAN_POINT('Ctrl Pts',(1.09543194105117,-0.452413838166731,
13.9574112186866));
#26590=CARTESIAN_POINT('Ctrl Pts',(1.08310942254938,-0.34886010476542,13.9635090063614));
#26591=CARTESIAN_POINT('Ctrl Pts',(1.07558101662333,-0.244950583047285,
13.9696067940362));
#26592=CARTESIAN_POINT('Ctrl Pts',(1.06805320928708,-0.141049323261376,
13.9757040968709));
#26593=CARTESIAN_POINT('Ctrl Pts',(1.06531878676402,-0.0367927553354598,
13.9818013997056));
#26594=CARTESIAN_POINT('Ctrl Pts',(1.06738816919642,0.0673458596739129,
13.9878987025402));
#26595=CARTESIAN_POINT('Ctrl Pts',(1.0694579144371,0.171502732474264,13.9939970743663));
#26596=CARTESIAN_POINT('Ctrl Pts',(1.07633312966777,0.275541186363404,14.0000954461923));
#26597=CARTESIAN_POINT('Ctrl Pts',(1.08797215363175,0.37898989817075,14.0061938180184));
#26598=CARTESIAN_POINT('Ctrl Pts',(1.09962285556094,0.482542404803256,14.0122983086199));
#26599=CARTESIAN_POINT('Ctrl Pts',(1.11604686192597,0.585503564954292,14.0184027992214));
#26600=CARTESIAN_POINT('Ctrl Pts',(1.13715085018088,0.687409177737005,14.0245072898229));
#26601=CARTESIAN_POINT('Ctrl Pts',(1.15826657705757,0.789371473239115,14.0306151759108));
#26602=CARTESIAN_POINT('Ctrl Pts',(1.18406736617564,0.890276640175051,14.0367230619988));
#26603=CARTESIAN_POINT('Ctrl Pts',(1.21440965026856,0.989674464956628,14.0428309480867));
#26604=CARTESIAN_POINT('Ctrl Pts',(1.2447970295493,1.08922001637488,14.0489479118126));
#26605=CARTESIAN_POINT('Ctrl Pts',(1.27973924018433,1.18725335180328,14.0550648755385));
#26606=CARTESIAN_POINT('Ctrl Pts',(1.31904409608155,1.28334304387748,14.0611818392645));
#26607=CARTESIAN_POINT('Ctrl Pts',(1.339918011708,1.33437409536318,14.0644304196699));
#26608=CARTESIAN_POINT('Ctrl Pts',(1.36202158688407,1.38485734260872,14.0676790000753));
#26609=CARTESIAN_POINT('Ctrl Pts',(1.38532083165587,1.43473110308257,14.0709275804807));
#26610=CARTESIAN_POINT('Ctrl Pts',(1.42919782694037,1.52865306383986,14.0770452872358));
#26611=CARTESIAN_POINT('Ctrl Pts',(1.47745655938762,1.62070886166848,14.0831629939909));
#26612=CARTESIAN_POINT('Ctrl Pts',(1.5299152038231,1.71046406535645,14.089280700746));
#26613=CARTESIAN_POINT('Ctrl Pts',(1.58230777925693,1.80010622691829,14.0953907025598));
#26614=CARTESIAN_POINT('Ctrl Pts',(1.63888953601503,1.88745319155252,14.1015007043735));
#26615=CARTESIAN_POINT('Ctrl Pts',(1.69943146028127,1.97209241197929,14.1076107061873));
#26616=CARTESIAN_POINT('Ctrl Pts',(1.75991416835196,2.05664884658965,14.1137147317942));
#26617=CARTESIAN_POINT('Ctrl Pts',(1.82434909401893,2.13850246040086,14.1198187574012));
#26618=CARTESIAN_POINT('Ctrl Pts',(1.89246281734669,2.21726787130628,14.1259227830081));
#26619=CARTESIAN_POINT('Ctrl Pts',(1.96053162936574,2.29598134763066,14.1320227838787));
#26620=CARTESIAN_POINT('Ctrl Pts',(2.03227413749924,2.37161035018557,14.1381227847492));
#26621=CARTESIAN_POINT('Ctrl Pts',(2.10737585959488,2.44380154291802,14.1442227856198));
#26622=CARTESIAN_POINT('Ctrl Pts',(2.18245245420379,2.51596858196682,14.1503207455559));
#26623=CARTESIAN_POINT('Ctrl Pts',(2.26088572236917,2.58469980352577,14.1564187054921));
#26624=CARTESIAN_POINT('Ctrl Pts',(2.34232399418702,2.64967837817621,14.1625166654282));
#26625=CARTESIAN_POINT('Ctrl Pts',(2.42375576872593,2.71465176872935,14.1686141388591));
#26626=CARTESIAN_POINT('Ctrl Pts',(2.50819173768904,2.77587284305098,14.17471161229));
#26627=CARTESIAN_POINT('Ctrl Pts',(2.59524748423437,2.83306532511337,14.1808090857209));
#26628=CARTESIAN_POINT('Ctrl Pts',(2.68231846628117,2.8902678163501,14.1869076262619));
#26629=CARTESIAN_POINT('Ctrl Pts',(2.77200978174592,2.94344008108176,14.1930061668028));
#26630=CARTESIAN_POINT('Ctrl Pts',(2.86390915502518,2.9923498900289,14.1991047073438));
#26631=CARTESIAN_POINT('Ctrl Pts',(2.95590067464842,3.04130874022537,14.2052093628146));
#26632=CARTESIAN_POINT('Ctrl Pts',(3.05010429684792,3.0859964013375,14.2113140182853));
#26633=CARTESIAN_POINT('Ctrl Pts',(3.14608440038722,3.12622727664259,14.2174186737561));
#26634=CARTESIAN_POINT('Ctrl Pts',(3.24211785825333,3.16648051586676,14.2235267227404));
#26635=CARTESIAN_POINT('Ctrl Pts',(3.33992936572046,3.20227188799659,14.2296347717247));
#26636=CARTESIAN_POINT('Ctrl Pts',(3.43906641780329,3.23346514317165,14.235742820709));
#26637=CARTESIAN_POINT('Ctrl Pts',(3.53835073078122,3.26470473366313,14.2418599427568));
#26638=CARTESIAN_POINT('Ctrl Pts',(3.63896410986365,3.29133245872545,14.2479770648045));
#26639=CARTESIAN_POINT('Ctrl Pts',(3.74044204364157,3.31326278887713,14.2540941868523));
#26640=CARTESIAN_POINT('Ctrl Pts',(3.79430504025231,3.32490308598071,14.257341065379));
#26641=CARTESIAN_POINT('Ctrl Pts',(3.84841148040424,3.33522084499568,14.2605879439058));
#26642=CARTESIAN_POINT('Ctrl Pts',(3.90269138321293,3.34420921833594,14.2638348224326));
#26643=CARTESIAN_POINT('Ctrl Pts',(4.00496826297327,3.36114555631361,14.2699527516752));
#26644=CARTESIAN_POINT('Ctrl Pts',(4.1081843232239,3.37341244336819,14.2760706809178));
#26645=CARTESIAN_POINT('Ctrl Pts',(4.21187841710675,3.3809141452128,14.2821886101604));
#26646=CARTESIAN_POINT('Ctrl Pts',(4.31544196361134,3.38840640266697,14.2882988371358));
#26647=CARTESIAN_POINT('Ctrl Pts',(4.41948192640586,3.39114537336765,14.2944090641111));
#26648=CARTESIAN_POINT('Ctrl Pts',(4.52352852080174,3.38908661698337,14.3005192910865));
#26649=CARTESIAN_POINT('Ctrl Pts',(4.62747339020213,3.38702987341829,14.3066235441728));
#26650=CARTESIAN_POINT('Ctrl Pts',(4.73142445543331,3.380184740341,14.3127277972591));
#26651=CARTESIAN_POINT('Ctrl Pts',(4.83490922267138,3.3685587631447,14.3188320503454));
#26652=CARTESIAN_POINT('Ctrl Pts',(4.93832580055099,3.35694044666938,14.324932281148));
#26653=CARTESIAN_POINT('Ctrl Pts',(5.04127627031441,3.34054759880824,14.3310325119505));
#26654=CARTESIAN_POINT('Ctrl Pts',(5.14329134486078,3.31943975318217,14.337132742753));
#26655=CARTESIAN_POINT('Ctrl Pts',(5.24527231194867,3.29833896469909,14.34323093402));
#26656=CARTESIAN_POINT('Ctrl Pts',(5.34631808977652,3.27252639827933,14.349329125287));
#26657=CARTESIAN_POINT('Ctrl Pts',(5.44596846752743,3.24211290310328,14.355427316554));
#26658=CARTESIAN_POINT('Ctrl Pts',(5.54561091307468,3.21170182885169,14.3615250224029));
#26659=CARTESIAN_POINT('Ctrl Pts',(5.64385777313427,3.17669067861854,14.3676227282518));
#26660=CARTESIAN_POINT('Ctrl Pts',(5.74026376159041,3.13724024348438,14.3737204341007));
#26661=CARTESIAN_POINT('Ctrl Pts',(5.83668663355153,3.09778289942652,14.379819207836));
#26662=CARTESIAN_POINT('Ctrl Pts',(5.93126760004852,3.05388488660293,14.3859179815714));
#26663=CARTESIAN_POINT('Ctrl Pts',(6.02358194473019,3.00575488253302,14.3920167553067));
#26664=CARTESIAN_POINT('Ctrl Pts',(6.1159888446647,2.95757662285656,14.3981216437315));
#26665=CARTESIAN_POINT('Ctrl Pts',(6.20612420804209,2.90515809698845,14.4042265321562));
#26666=CARTESIAN_POINT('Ctrl Pts',(6.29358857292772,2.84875360948207,14.4103314205809));
#26667=CARTESIAN_POINT('Ctrl Pts',(6.38110155870265,2.79231776707651,14.4164397026747));
#26668=CARTESIAN_POINT('Ctrl Pts',(6.46594024217969,2.7318917955,14.4225479847684));
#26669=CARTESIAN_POINT('Ctrl Pts',(6.54773630843541,2.66777183271562,14.4286562668622));
#26670=CARTESIAN_POINT('Ctrl Pts',(6.62965384610285,2.60355664845231,14.4347736200725));
#26671=CARTESIAN_POINT('Ctrl Pts',(6.70851942143287,2.53563679506501,14.4408909732828));
#26672=CARTESIAN_POINT('Ctrl Pts',(6.78399975764928,2.46434699852701,14.4470083264931));
#26673=CARTESIAN_POINT('Ctrl Pts',(6.82403372786696,2.42653564613393,14.4502529057902));
#26674=CARTESIAN_POINT('Ctrl Pts',(6.86311603266176,2.38777688581644,14.4534974850874));
#26675=CARTESIAN_POINT('Ctrl Pts',(6.90120154150049,2.34812443928745,14.4567420643846));
#26676=CARTESIAN_POINT('Ctrl Pts',(6.9756608983498,2.27060162927189,14.4630854032313));
#26677=CARTESIAN_POINT('Ctrl Pts',(7.04657001351865,2.18938676520692,14.469428742078));
#26678=CARTESIAN_POINT('Ctrl Pts',(7.11354011887247,2.10484647806263,14.4757720809248));
#26679=CARTESIAN_POINT('Ctrl Pts',(7.17716397400672,2.02453035859624,14.481798466425));
#26680=CARTESIAN_POINT('Ctrl Pts',(7.23723258799101,1.94121348097766,14.4878248519252));
#26681=CARTESIAN_POINT('Ctrl Pts',(7.29344937492137,1.85524877509437,14.4938512374254));
#26682=CARTESIAN_POINT('Ctrl Pts',(7.34961845323007,1.76935702353404,14.4998725086072));
#26683=CARTESIAN_POINT('Ctrl Pts',(7.40194195912083,1.68082227180889,14.5058937797891));
#26684=CARTESIAN_POINT('Ctrl Pts',(7.4501644639003,1.59002929780962,14.5119150509709));
#26685=CARTESIAN_POINT('Ctrl Pts',(7.49835921900135,1.49928857069888,14.5179328572075));
#26686=CARTESIAN_POINT('Ctrl Pts',(7.5424574574542,1.40629258939893,14.5239506634441));
#26687=CARTESIAN_POINT('Ctrl Pts',(7.5822484268014,1.3114528971773,14.5299684696807));
#26688=CARTESIAN_POINT('Ctrl Pts',(7.62202736757881,1.21664187442204,14.5359844567708));
#26689=CARTESIAN_POINT('Ctrl Pts',(7.65750145937001,1.11998865268956,14.5420004438609));
#26690=CARTESIAN_POINT('Ctrl Pts',(7.68850750006142,1.02192606543904,14.548016430951));
#26691=CARTESIAN_POINT('Ctrl Pts',(7.71952301078012,0.923833527399664,14.5540342554754));
#26692=CARTESIAN_POINT('Ctrl Pts',(7.74606760777517,0.824331180515576,14.5600520799997));
#26693=CARTESIAN_POINT('Ctrl Pts',(7.768027719248,0.723867815950181,14.5660699045241));
#26694=CARTESIAN_POINT('Ctrl Pts',(7.78999175642468,0.623386492030765,14.5720888048261));
#26695=CARTESIAN_POINT('Ctrl Pts',(7.80736959523124,0.52194423900002,14.5781077051281));
#26696=CARTESIAN_POINT('Ctrl Pts',(7.8200989427707,0.419999268039994,14.5841266054301));
#26697=CARTESIAN_POINT('Ctrl Pts',(7.83283950703884,0.317964466153722,14.590150809411));
#26698=CARTESIAN_POINT('Ctrl Pts',(7.84092336412678,0.215426498290773,14.5961750133919));
#26699=CARTESIAN_POINT('Ctrl Pts',(7.84434019546452,0.112847441926262,14.6021992173728));
#26700=CARTESIAN_POINT('Ctrl Pts',(7.84562259429113,0.0743476599604382,
14.6044602104839));
#26701=CARTESIAN_POINT('Ctrl Pts',(7.84624810502525,0.0358420830154314,
14.606721203595));
#26702=CARTESIAN_POINT('Ctrl Pts',(7.84621807431328,-0.0026449572190203,
14.6089821967061));
#26703=CARTESIAN_POINT('Ctrl Pts',(7.63534118037484,-1.17693559664385,13.0872737913614));
#26704=CARTESIAN_POINT('Ctrl Pts',(7.61078196418787,-1.24326939326156,13.0918003129721));
#26705=CARTESIAN_POINT('Ctrl Pts',(7.58414505308867,-1.30883829589362,13.0963165266834));
#26706=CARTESIAN_POINT('Ctrl Pts',(7.51900898479892,-1.45579851001032,13.1064781970875));
#26707=CARTESIAN_POINT('Ctrl Pts',(7.47928913008439,-1.53657454578565,13.1120921354455));
#26708=CARTESIAN_POINT('Ctrl Pts',(7.41583733814597,-1.65360387171743,13.1201767496037));
#26709=CARTESIAN_POINT('Ctrl Pts',(7.39455172315452,-1.69113488675286,13.1227614784648));
#26710=CARTESIAN_POINT('Ctrl Pts',(7.34925064900939,-1.76757151201247,13.1279938090185));
#26711=CARTESIAN_POINT('Ctrl Pts',(7.32515342140494,-1.80641768869974,13.1306365108775));
#26712=CARTESIAN_POINT('Ctrl Pts',(7.24845778784824,-1.92464814904058,13.138665454069));
#26713=CARTESIAN_POINT('Ctrl Pts',(7.19329225887402,-2.00231690846836,13.1439200856325));
#26714=CARTESIAN_POINT('Ctrl Pts',(7.00757048412473,-2.24175478279824,13.160387588591));
#26715=CARTESIAN_POINT('Ctrl Pts',(6.86538677605168,-2.39388863739322,13.1712905176747));
#26716=CARTESIAN_POINT('Ctrl Pts',(6.64148260839246,-2.59317858126606,13.1875282510223));
#26717=CARTESIAN_POINT('Ctrl Pts',(6.57034620338852,-2.65148661492758,13.1925667182765));
#26718=CARTESIAN_POINT('Ctrl Pts',(6.43169872917916,-2.75600185095779,13.2022639292715));
#26719=CARTESIAN_POINT('Ctrl Pts',(6.36471464615591,-2.80279784428053,13.2068989017737));
#26720=CARTESIAN_POINT('Ctrl Pts',(6.23765415249025,-2.88489661338535,13.2156449354446));
#26721=CARTESIAN_POINT('Ctrl Pts',(6.17805313344893,-2.9208553645319,13.2197297285821));
#26722=CARTESIAN_POINT('Ctrl Pts',(6.03216555724536,-3.00285594055521,13.2297055909474));
#26723=CARTESIAN_POINT('Ctrl Pts',(5.94491484472188,-3.04704605515623,13.2356546106145));
#26724=CARTESIAN_POINT('Ctrl Pts',(5.6434460138536,-3.18369155678734,13.2561562572981));
#26725=CARTESIAN_POINT('Ctrl Pts',(5.42165239914339,-3.25779183649517,13.2712023388256));
#26726=CARTESIAN_POINT('Ctrl Pts',(5.07646650795671,-3.33474424778458,13.2937557554643));
#26727=CARTESIAN_POINT('Ctrl Pts',(4.95756803085305,-3.35467143186798,13.3013632913643));
#26728=CARTESIAN_POINT('Ctrl Pts',(4.79187773083286,-3.37343251348913,13.3115479624383));
#26729=CARTESIAN_POINT('Ctrl Pts',(4.74579824427791,-3.37769670072365,13.3143358840097));
#26730=CARTESIAN_POINT('Ctrl Pts',(4.66230090379853,-3.38370211587476,13.3192906002656));
#26731=CARTESIAN_POINT('Ctrl Pts',(4.62491588752283,-3.38576912071431,13.3214729899031));
#26732=CARTESIAN_POINT('Ctrl Pts',(4.51088435797457,-3.39018042211444,13.3280391914891));
#26733=CARTESIAN_POINT('Ctrl Pts',(4.4341813645076,-3.39054408842784,13.3323320831021));
#26734=CARTESIAN_POINT('Ctrl Pts',(4.12530267015517,-3.38152450747078,13.3493448430437));
#26735=CARTESIAN_POINT('Ctrl Pts',(3.89438109492653,-3.3508876727214,13.3614774078569));
#26736=CARTESIAN_POINT('Ctrl Pts',(3.53943768799696,-3.26604341622901,13.3812042907396));
#26737=CARTESIAN_POINT('Ctrl Pts',(3.41240719546698,-3.22767971391738,13.3884841856169));
#26738=CARTESIAN_POINT('Ctrl Pts',(3.21929175106573,-3.15676226176972,13.4001246252176));
#26739=CARTESIAN_POINT('Ctrl Pts',(3.15146488721055,-3.12933198239916,13.4043265173063));
#26740=CARTESIAN_POINT('Ctrl Pts',(3.0175015341898,-3.07004210748855,13.4128842679216));
#26741=CARTESIAN_POINT('Ctrl Pts',(2.95140690789296,-3.03818577387404,13.417238239867));
#26742=CARTESIAN_POINT('Ctrl Pts',(2.76702000447868,-2.94182108555106,13.4297828428999));
#26743=CARTESIAN_POINT('Ctrl Pts',(2.65147615423855,-2.87237592559581,13.4381302917912));
#26744=CARTESIAN_POINT('Ctrl Pts',(2.37866539689465,-2.6854361810908,13.4590061915412));
#26745=CARTESIAN_POINT('Ctrl Pts',(2.22687080265957,-2.56080500113723,13.4716830138176));
#26746=CARTESIAN_POINT('Ctrl Pts',(2.01563532629613,-2.35427599483544,13.4904223071858));
#26747=CARTESIAN_POINT('Ctrl Pts',(1.94764818503486,-2.28168920322794,13.4966506267712));
#26748=CARTESIAN_POINT('Ctrl Pts',(1.85413777866381,-2.17261036555619,13.5053955852988));
#26749=CARTESIAN_POINT('Ctrl Pts',(1.82598953162957,-2.13844377800599,13.5080534679178));
#26750=CARTESIAN_POINT('Ctrl Pts',(1.77096178265462,-2.06891924013892,13.5132854149777));
#26751=CARTESIAN_POINT('Ctrl Pts',(1.74409168914495,-2.03356474828833,13.5158587319844));
#26752=CARTESIAN_POINT('Ctrl Pts',(1.65862143537455,-1.91639732272909,13.5241422967821));
#26753=CARTESIAN_POINT('Ctrl Pts',(1.60296463275702,-1.83249712087603,13.5296955889111));
#26754=CARTESIAN_POINT('Ctrl Pts',(1.44716782202941,-1.57328617990728,13.5461222043731));
#26755=CARTESIAN_POINT('Ctrl Pts',(1.35886565655006,-1.39139516313471,13.5567204116079));
#26756=CARTESIAN_POINT('Ctrl Pts',(1.24122107107703,-1.08139971131767,13.5746617927697));
#26757=CARTESIAN_POINT('Ctrl Pts',(1.20218579876288,-0.957539042409238,
13.581795547008));
#26758=CARTESIAN_POINT('Ctrl Pts',(1.15246897373447,-0.761115911058011,
13.5932671517121));
#26759=CARTESIAN_POINT('Ctrl Pts',(1.13687322374893,-0.689924905624793,
13.5974551854113));
#26760=CARTESIAN_POINT('Ctrl Pts',(1.11014802912544,-0.545863097076909,
13.606018670329));
#26761=CARTESIAN_POINT('Ctrl Pts',(1.09907719306723,-0.473021775956921,
13.6103933686582));
#26762=CARTESIAN_POINT('Ctrl Pts',(1.07412122129508,-0.262949999343718,
13.6231567213181));
#26763=CARTESIAN_POINT('Ctrl Pts',(1.06622634454318,-0.125167713253653,
13.6317122703283));
#26764=CARTESIAN_POINT('Ctrl Pts',(1.06771488854485,0.272124175616757,13.6568189481909));
#26765=CARTESIAN_POINT('Ctrl Pts',(1.09846364833005,0.530568255769381,13.6737461673805));
#26766=CARTESIAN_POINT('Ctrl Pts',(1.17159015607771,0.838596312333952,13.6933472274091));
#26767=CARTESIAN_POINT('Ctrl Pts',(1.18620139841751,0.893881103396226,13.6968380644214));
#26768=CARTESIAN_POINT('Ctrl Pts',(1.21340117076398,0.987175531749563,13.7026535808208));
#26769=CARTESIAN_POINT('Ctrl Pts',(1.22527554651082,1.02537487673441,13.7050109413401));
#26770=CARTESIAN_POINT('Ctrl Pts',(1.25674456755835,1.12062722063087,13.7108337075722));
#26771=CARTESIAN_POINT('Ctrl Pts',(1.27719027523242,1.17738248505034,13.7142563416665));
#26772=CARTESIAN_POINT('Ctrl Pts',(1.37565483209962,1.42940394058866,13.7293653938634));
#26773=CARTESIAN_POINT('Ctrl Pts',(1.47022956198287,1.61771441049224,13.7404340956421));
#26774=CARTESIAN_POINT('Ctrl Pts',(1.67155468800349,1.93996060283554,13.760785975133));
#26775=CARTESIAN_POINT('Ctrl Pts',(1.77212765093836,2.07689648618657,13.769969562884));
#26776=CARTESIAN_POINT('Ctrl Pts',(1.93213535107965,2.26361598318493,13.7838052629432));
#26777=CARTESIAN_POINT('Ctrl Pts',(1.98368384144824,2.31981680811819,13.7881615779485));
#26778=CARTESIAN_POINT('Ctrl Pts',(2.08691822265776,2.4250147693373,13.796731899266));
#26779=CARTESIAN_POINT('Ctrl Pts',(2.13833956164798,2.47421550079124,13.8009337757446));
#26780=CARTESIAN_POINT('Ctrl Pts',(2.27586259718405,2.59774722999733,13.8120214511218));
#26781=CARTESIAN_POINT('Ctrl Pts',(2.36421922520013,2.66942347973461,13.8190041824762));
#26782=CARTESIAN_POINT('Ctrl Pts',(2.58796179419694,2.83298501455062,13.8363397563454));
#26783=CARTESIAN_POINT('Ctrl Pts',(2.72671799455055,2.91977372002874,13.8468150722673));
#26784=CARTESIAN_POINT('Ctrl Pts',(2.99843663105924,3.06353933953465,13.8664965580249));
#26785=CARTESIAN_POINT('Ctrl Pts',(3.12985976312979,3.12269837708176,13.8756820254468));
#26786=CARTESIAN_POINT('Ctrl Pts',(3.31335398373097,3.19161386866007,13.8877576643366));
#26787=CARTESIAN_POINT('Ctrl Pts',(3.36247134863246,3.20878182769038,13.8909192229858));
#26788=CARTESIAN_POINT('Ctrl Pts',(3.45036101518317,3.23724887816915,13.8964287401332));
#26789=CARTESIAN_POINT('Ctrl Pts',(3.48897049672086,3.24899682826651,13.8987971818032));
#26790=CARTESIAN_POINT('Ctrl Pts',(3.59154378570079,3.27821662143074,13.9049647483041));
#26791=CARTESIAN_POINT('Ctrl Pts',(3.6558251658698,3.29450610223103,13.9087063445116));
#26792=CARTESIAN_POINT('Ctrl Pts',(3.81040943591592,3.32888670139834,13.9174978846356));
#26793=CARTESIAN_POINT('Ctrl Pts',(3.90105342166349,3.34520475621724,13.9224881702002));
#26794=CARTESIAN_POINT('Ctrl Pts',(4.2676011516645,3.39587978158245,13.9423765631823));
#26795=CARTESIAN_POINT('Ctrl Pts',(4.54656441299923,3.39993331084547,13.956955043098));
#26796=CARTESIAN_POINT('Ctrl Pts',(4.89841967273763,3.36167472098892,13.9768776631696));
#26797=CARTESIAN_POINT('Ctrl Pts',(4.97364734803257,3.3509256440861,13.9812203634815));
#26798=CARTESIAN_POINT('Ctrl Pts',(5.11863902437216,3.32520946985065,13.9897857369685));
#26799=CARTESIAN_POINT('Ctrl Pts',(5.18841699528812,3.31054953273259,13.9939970677708));
#26800=CARTESIAN_POINT('Ctrl Pts',(5.36937046529832,3.26653175542016,14.0051713214528));
#26801=CARTESIAN_POINT('Ctrl Pts',(5.47959899762967,3.23370059869532,14.0122344207196));
#26802=CARTESIAN_POINT('Ctrl Pts',(5.74542376035879,3.13957198013849,14.0298844242536));
#26803=CARTESIAN_POINT('Ctrl Pts',(5.8985622568264,3.0722430424454,14.0406010019327));
#26804=CARTESIAN_POINT('Ctrl Pts',(6.17799358335042,2.92387717791532,14.060850471175));
#26805=CARTESIAN_POINT('Ctrl Pts',(6.30512353791423,2.84520436517367,14.0703627033318));
#26806=CARTESIAN_POINT('Ctrl Pts',(6.46569938650064,2.73051287052803,14.082446919164));
#26807=CARTESIAN_POINT('Ctrl Pts',(6.50414640408515,2.70180033828092,14.0853452345017));
#26808=CARTESIAN_POINT('Ctrl Pts',(6.57492556085352,2.64656277872113,14.0906711249749));
#26809=CARTESIAN_POINT('Ctrl Pts',(6.60739967357696,2.62023855722424,14.0931088165143));
#26810=CARTESIAN_POINT('Ctrl Pts',(6.70000469248057,2.54228886728828,14.100066552028));
#26811=CARTESIAN_POINT('Ctrl Pts',(6.75882614837989,2.48914411900959,14.1044953466474));
#26812=CARTESIAN_POINT('Ctrl Pts',(6.9899088925653,2.26515505759865,14.1221821276839));
#26813=CARTESIAN_POINT('Ctrl Pts',(7.14546472943476,2.07811434792671,14.1348228197469));
#26814=CARTESIAN_POINT('Ctrl Pts',(7.34801936292616,1.77329282884427,14.1546774779979));
#26815=CARTESIAN_POINT('Ctrl Pts',(7.41064253472399,1.66687904799674,14.1614807233479));
#26816=CARTESIAN_POINT('Ctrl Pts',(7.50049269678464,1.49316391094426,14.1725706555008));
#26817=CARTESIAN_POINT('Ctrl Pts',(7.53160355190887,1.42799339733243,14.1767267002323));
#26818=CARTESIAN_POINT('Ctrl Pts',(7.5905380079332,1.29366406403061,14.1853113003037));
#26819=CARTESIAN_POINT('Ctrl Pts',(7.61820874850869,1.2244818380462,14.1897419755079));
#26820=CARTESIAN_POINT('Ctrl Pts',(7.69371447104145,1.01603168115716,14.2031388340943));
#26821=CARTESIAN_POINT('Ctrl Pts',(7.7347765606307,0.874511207641564,14.2123028973801));
#26822=CARTESIAN_POINT('Ctrl Pts',(7.80982716998081,0.534574062973371,14.2343667223056));
#26823=CARTESIAN_POINT('Ctrl Pts',(7.83561314585523,0.334907602015024,14.2473786631015));
#26824=CARTESIAN_POINT('Ctrl Pts',(7.8468295138858,0.0516807095146062,14.2652453393694));
#26825=CARTESIAN_POINT('Ctrl Pts',(7.84708312737092,-0.0308724860350004,
14.2703782550505));
#26826=CARTESIAN_POINT('Ctrl Pts',(7.84289991434231,-0.155893278208164,
14.2779649048766));
#26827=CARTESIAN_POINT('Ctrl Pts',(7.84067564013924,-0.198401320532778,
14.2805113548649));
#26828=CARTESIAN_POINT('Ctrl Pts',(7.83434283382549,-0.287300981476298,
14.28575333076));
#26829=CARTESIAN_POINT('Ctrl Pts',(7.83007794313444,-0.333671503058707,
14.2884413932368));
#26830=CARTESIAN_POINT('Ctrl Pts',(7.81091591323208,-0.503553200940941,
14.2981660767072));
#26831=CARTESIAN_POINT('Ctrl Pts',(7.7901779705527,-0.626314399420544,14.3049552114575));
#26832=CARTESIAN_POINT('Ctrl Pts',(7.72974380590606,-0.893561105008769,
14.3197127536322));
#26833=CARTESIAN_POINT('Ctrl Pts',(7.68716662343717,-1.03695645662067,14.3276212883842));
#26834=CARTESIAN_POINT('Ctrl Pts',(7.63534113152507,-1.17693572858576,14.3356579957882));
#26835=CARTESIAN_POINT('Origin',(4.45646910621825,3.5527136788005E-15,11.));
#26836=CARTESIAN_POINT('',(7.63534122786267,-1.17693546838044,15.9331819277137));
#26837=CARTESIAN_POINT('',(7.63534118765004,-1.1769355769937,15.5865253037982));
#26838=CARTESIAN_POINT('',(7.63534122785693,-1.17693546839596,11.));
#26839=CARTESIAN_POINT('',(7.84621680191345,0.00395247126457767,15.8589808168116));
#26840=CARTESIAN_POINT('Ctrl Pts',(7.84621673818046,0.00400675761810125,
15.8598626507015));
#26841=CARTESIAN_POINT('Ctrl Pts',(7.84635597463948,-0.113788353100374,
15.8674415510758));
#26842=CARTESIAN_POINT('Ctrl Pts',(7.84035501031268,-0.231516686720479,
15.8749656324585));
#26843=CARTESIAN_POINT('Ctrl Pts',(7.81594889922953,-0.46751264752174,15.8898584151366));
#26844=CARTESIAN_POINT('Ctrl Pts',(7.79738934461118,-0.585601546171405,
15.8972129536422));
#26845=CARTESIAN_POINT('Ctrl Pts',(7.75665422830044,-0.777899395116433,
15.9090356595868));
#26846=CARTESIAN_POINT('Ctrl Pts',(7.73810725094379,-0.852761209403362,
15.9136000387725));
#26847=CARTESIAN_POINT('Ctrl Pts',(7.69333519420788,-1.01025069608165,15.9231472973591));
#26848=CARTESIAN_POINT('Ctrl Pts',(7.66646200780271,-1.09263703021642,15.9281085052823));
#26849=CARTESIAN_POINT('Ctrl Pts',(7.63608789069674,-1.17491727604896,15.9330604654293));
#26850=CARTESIAN_POINT('Ctrl Pts',(7.63571479859986,-1.1759264635252,15.9331212021678));
#26851=CARTESIAN_POINT('Ctrl Pts',(7.63534122786842,-1.17693546836491,15.9331819277137));
#26852=CARTESIAN_POINT('Ctrl Pts',(7.63534122785692,-1.17693546839596,14.6796206134749));
#26853=CARTESIAN_POINT('Ctrl Pts',(7.59925654215824,-1.27439926693538,14.6857274565409));
#26854=CARTESIAN_POINT('Ctrl Pts',(7.55864642848513,-1.37030743254935,14.6918342996069));
#26855=CARTESIAN_POINT('Ctrl Pts',(7.51367023832885,-1.46421525067923,14.697941142673));
#26856=CARTESIAN_POINT('Ctrl Pts',(7.46873004583586,-1.55804790766262,14.7040430979955));
#26857=CARTESIAN_POINT('Ctrl Pts',(7.41943091115226,-1.64988302006714,14.710145053318));
#26858=CARTESIAN_POINT('Ctrl Pts',(7.36598036809627,-1.7392956274035,14.7162470086406));
#26859=CARTESIAN_POINT('Ctrl Pts',(7.31255275719406,-1.82866987360182,14.7223463460107));
#26860=CARTESIAN_POINT('Ctrl Pts',(7.25497749599115,-1.91562331656183,14.7284456833808));
#26861=CARTESIAN_POINT('Ctrl Pts',(7.19350781112107,-1.99975603271096,14.7345450207509));
#26862=CARTESIAN_POINT('Ctrl Pts',(7.13204884861661,-2.08387407330507,14.740643294193));
#26863=CARTESIAN_POINT('Ctrl Pts',(7.06669706390409,-2.16517202256828,14.746741567635));
#26864=CARTESIAN_POINT('Ctrl Pts',(6.9977482079261,-2.24328009613667,14.752839841077));
#26865=CARTESIAN_POINT('Ctrl Pts',(6.92879382502816,-2.32139443082518,14.7589386033549));
#26866=CARTESIAN_POINT('Ctrl Pts',(6.85624207946546,-2.3963180635243,14.7650373656327));
#26867=CARTESIAN_POINT('Ctrl Pts',(6.78042749679774,-2.46771604147543,14.7711361279105));
#26868=CARTESIAN_POINT('Ctrl Pts',(6.70454113290327,-2.53918161901314,14.7772406644949));
#26869=CARTESIAN_POINT('Ctrl Pts',(6.62538607070449,-2.60711458175522,14.7833452010792));
#26870=CARTESIAN_POINT('Ctrl Pts',(6.54333202014636,-2.67121849367877,14.7894497376635));
#26871=CARTESIAN_POINT('Ctrl Pts',(6.4612393624972,-2.73535256700868,14.7955571464815));
#26872=CARTESIAN_POINT('Ctrl Pts',(6.3762453448536,-2.79565375292429,14.8016645552994));
#26873=CARTESIAN_POINT('Ctrl Pts',(6.28874935509067,-2.85186853695818,14.8077719641173));
#26874=CARTESIAN_POINT('Ctrl Pts',(6.20111478934914,-2.90817235385781,14.8138890458374));
#26875=CARTESIAN_POINT('Ctrl Pts',(6.11097070112765,-2.96037662220921,14.8200061275576));
#26876=CARTESIAN_POINT('Ctrl Pts',(6.01874207763718,-3.00827329630701,14.8261232092777));
#26877=CARTESIAN_POINT('Ctrl Pts',(5.93615235562846,-3.05116424327304,14.831600988948));
#26878=CARTESIAN_POINT('Ctrl Pts',(5.85189155830507,-3.09060148796669,14.8370787686182));
#26879=CARTESIAN_POINT('Ctrl Pts',(5.76627707734561,-3.12646895734968,14.8425565482884));
#26880=CARTESIAN_POINT('Ctrl Pts',(5.67063788999286,-3.16653619347313,14.8486757280147));
#26881=CARTESIAN_POINT('Ctrl Pts',(5.57300807714975,-3.20227406034225,14.8547949077409));
#26882=CARTESIAN_POINT('Ctrl Pts',(5.47381452586385,-3.23348316210648,14.8609140874672));
#26883=CARTESIAN_POINT('Ctrl Pts',(5.37474561246936,-3.2646530492586,14.8670255783704));
#26884=CARTESIAN_POINT('Ctrl Pts',(5.27411726975106,-3.29130535986388,14.8731370692736));
#26885=CARTESIAN_POINT('Ctrl Pts',(5.17237659623641,-3.31328862736645,14.8792485601769));
#26886=CARTESIAN_POINT('Ctrl Pts',(5.07073518188626,-3.33525044778508,14.8853540886517));
#26887=CARTESIAN_POINT('Ctrl Pts',(4.96798400832247,-3.35255219560697,14.8914596171266));
#26888=CARTESIAN_POINT('Ctrl Pts',(4.86458477785658,-3.3650923703612,14.8975651456014));
#26889=CARTESIAN_POINT('Ctrl Pts',(4.76125347176171,-3.37762430730284,14.9036666632709));
#26890=CARTESIAN_POINT('Ctrl Pts',(4.65727537604443,-3.38540084126951,14.9097681809405));
#26891=CARTESIAN_POINT('Ctrl Pts',(4.55312104360974,-3.38837180154399,14.91586969861));
#26892=CARTESIAN_POINT('Ctrl Pts',(4.44900141669852,-3.39134177185742,14.9219691831777));
#26893=CARTESIAN_POINT('Ctrl Pts',(4.34470609398513,-3.3895093396803,14.9280686677454));
#26894=CARTESIAN_POINT('Ctrl Pts',(4.24070861432847,-3.38287636082661,14.9341681523131));
#26895=CARTESIAN_POINT('Ctrl Pts',(4.13671933112334,-3.37624390474414,14.9402671561564));
#26896=CARTESIAN_POINT('Ctrl Pts',(4.03302826812358,-3.36481168187265,14.9463661599996));
#26897=CARTESIAN_POINT('Ctrl Pts',(3.93010594542762,-3.34863358483165,14.9524651638429));
#26898=CARTESIAN_POINT('Ctrl Pts',(3.82716555195804,-3.3324526472919,14.9585652385299));
#26899=CARTESIAN_POINT('Ctrl Pts',(3.72499458654479,-3.31152424580401,14.9646653132168));
#26900=CARTESIAN_POINT('Ctrl Pts',(3.62405458660875,-3.28595361045211,14.9707653879037));
#26901=CARTESIAN_POINT('Ctrl Pts',(3.52301346137032,-3.26035735752309,14.9768715738637));
#26902=CARTESIAN_POINT('Ctrl Pts',(3.42320617622278,-3.23010968941689,14.9829777598236));
#26903=CARTESIAN_POINT('Ctrl Pts',(3.32508020856909,-3.19536605489515,14.9890839457836));
#26904=CARTESIAN_POINT('Ctrl Pts',(3.22689971002588,-3.16060311252513,14.9951935250935));
#26905=CARTESIAN_POINT('Ctrl Pts',(3.13040278355711,-3.12133938647638,15.0013031044034));
#26906=CARTESIAN_POINT('Ctrl Pts',(3.03601624188276,-3.07777821207134,15.0074126837134));
#26907=CARTESIAN_POINT('Ctrl Pts',(2.94148975664343,-3.03415245106389,15.0135313214791));
#26908=CARTESIAN_POINT('Ctrl Pts',(2.84908028160397,-2.98621671291607,15.0196499592447));
#26909=CARTESIAN_POINT('Ctrl Pts',(2.75918943086372,-2.93421995871618,15.0257685970104));
#26910=CARTESIAN_POINT('Ctrl Pts',(2.71171104319487,-2.90675640671846,15.029000328087));
#26911=CARTESIAN_POINT('Ctrl Pts',(2.66493479381262,-2.87816067354097,15.0322320591637));
#26912=CARTESIAN_POINT('Ctrl Pts',(2.61891630898795,-2.84847411430946,15.0354637902403));
#26913=CARTESIAN_POINT('Ctrl Pts',(2.53190268614322,-2.79234156065477,15.0415744788063));
#26914=CARTESIAN_POINT('Ctrl Pts',(2.447324003263,-2.73212835339743,15.0476851673722));
#26915=CARTESIAN_POINT('Ctrl Pts',(2.36558555678323,-2.66807253372205,15.0537958559381));
#26916=CARTESIAN_POINT('Ctrl Pts',(2.28395036483308,-2.60409763133609,15.0598988252936));
#26917=CARTESIAN_POINT('Ctrl Pts',(2.20514860836062,-2.53629002873644,15.066001794649));
#26918=CARTESIAN_POINT('Ctrl Pts',(2.12955756925958,-2.46493159370978,15.0721047640044));
#26919=CARTESIAN_POINT('Ctrl Pts',(2.0540406049299,-2.39364308575148,15.0782017528089));
#26920=CARTESIAN_POINT('Ctrl Pts',(1.98172840905519,-2.3188109566093,15.0842987416134));
#26921=CARTESIAN_POINT('Ctrl Pts',(1.91296537712471,-2.24075742609218,15.0903957304179));
#26922=CARTESIAN_POINT('Ctrl Pts',(1.84424747924138,-2.16275512763431,15.0964887173369));
#26923=CARTESIAN_POINT('Ctrl Pts',(1.77907439344342,-2.08153595168046,15.1025817042559));
#26924=CARTESIAN_POINT('Ctrl Pts',(1.71775323376058,-1.99745849329803,15.1086746911749));
#26925=CARTESIAN_POINT('Ctrl Pts',(1.65645243872213,-1.91340895688494,15.1147656546242));
#26926=CARTESIAN_POINT('Ctrl Pts',(1.5990012778261,-1.82650336887972,15.1208566180734));
#26927=CARTESIAN_POINT('Ctrl Pts',(1.54566567361456,-1.73713224575521,15.1269475815227));
#26928=CARTESIAN_POINT('Ctrl Pts',(1.49233409906925,-1.64776787488939,15.1330380847812));
#26929=CARTESIAN_POINT('Ctrl Pts',(1.44311768089322,-1.55593870543276,15.1391285880398));
#26930=CARTESIAN_POINT('Ctrl Pts',(1.39823773191259,-1.46206221608812,15.1452190912983));
#26931=CARTESIAN_POINT('Ctrl Pts',(1.35334966028844,-1.36816873641094,15.1513106968528));
#26932=CARTESIAN_POINT('Ctrl Pts',(1.3127998010773,-1.27222758501815,15.1574023024073));
#26933=CARTESIAN_POINT('Ctrl Pts',(1.27676205110674,-1.17467787336532,15.1634939079618));
#26934=CARTESIAN_POINT('Ctrl Pts',(1.24068756600035,-1.07702872426397,15.1695917230038));
#26935=CARTESIAN_POINT('Ctrl Pts',(1.20913452112613,-0.977768141438918,
15.1756895380458));
#26936=CARTESIAN_POINT('Ctrl Pts',(1.18222744528331,-0.877352043536669,
15.1817873530878));
#26937=CARTESIAN_POINT('Ctrl Pts',(1.15530519760434,-0.776879324967353,
15.1878886064466));
#26938=CARTESIAN_POINT('Ctrl Pts',(1.13303422816773,-0.675250209564502,
15.1939898598054));
#26939=CARTESIAN_POINT('Ctrl Pts',(1.11548787895925,-0.572930625471287,
15.2000911131641));
#26940=CARTESIAN_POINT('Ctrl Pts',(1.09791505400747,-0.470456651025431,
15.2062015727239));
#26941=CARTESIAN_POINT('Ctrl Pts',(1.08508113806529,-0.367290549925763,
15.2123120322837));
#26942=CARTESIAN_POINT('Ctrl Pts',(1.07700758983372,-0.263903243208449,
15.2184224918435));
#26943=CARTESIAN_POINT('Ctrl Pts',(1.07262603066434,-0.207794381435347,
15.2217386719598));
#26944=CARTESIAN_POINT('Ctrl Pts',(1.06964563234854,-0.151620379755214,
15.225054852076));
#26945=CARTESIAN_POINT('Ctrl Pts',(1.0680634074785,-0.0954561849645197,
15.2283710321923));
#26946=CARTESIAN_POINT('Ctrl Pts',(1.06513996899317,0.00831703441671776,
15.2344982576959));
#26947=CARTESIAN_POINT('Ctrl Pts',(1.06698351873962,0.112386429627051,15.2406254831995));
#26948=CARTESIAN_POINT('Ctrl Pts',(1.0736259808533,0.216280955405394,15.2467527087032));
#26949=CARTESIAN_POINT('Ctrl Pts',(1.08026006332207,0.320044415440628,15.2528722045468));
#26950=CARTESIAN_POINT('Ctrl Pts',(1.09168099275754,0.423633025198743,15.2589917003904));
#26951=CARTESIAN_POINT('Ctrl Pts',(1.1078686999171,0.526574193651555,15.265111196234));
#26952=CARTESIAN_POINT('Ctrl Pts',(1.12404049789571,0.629414192144985,15.271224677874));
#26953=CARTESIAN_POINT('Ctrl Pts',(1.14496969006219,0.731607598516677,15.277338159514));
#26954=CARTESIAN_POINT('Ctrl Pts',(1.17058433753088,0.83268622506223,15.283451641154));
#26955=CARTESIAN_POINT('Ctrl Pts',(1.19618171898921,0.933696717755195,15.2895610018925));
#26956=CARTESIAN_POINT('Ctrl Pts',(1.22645816970146,1.03359351584041,15.2956703626311));
#26957=CARTESIAN_POINT('Ctrl Pts',(1.26129068445046,1.13191868770221,15.3017797233697));
#26958=CARTESIAN_POINT('Ctrl Pts',(1.29611119508855,1.23020997437724,15.3078869786776));
#26959=CARTESIAN_POINT('Ctrl Pts',(1.33548450685337,1.32693031283058,15.3139942339855));
#26960=CARTESIAN_POINT('Ctrl Pts',(1.37923800531681,1.42163772253867,15.3201014892935));
#26961=CARTESIAN_POINT('Ctrl Pts',(1.42298747046021,1.51633640185244,15.3262081816175));
#26962=CARTESIAN_POINT('Ctrl Pts',(1.47111614124288,1.60902213721648,15.3323148739415));
#26963=CARTESIAN_POINT('Ctrl Pts',(1.52340393979046,1.69927448988912,15.3384215662655));
#26964=CARTESIAN_POINT('Ctrl Pts',(1.57570011738232,1.78954130537107,15.3445292371782));
#26965=CARTESIAN_POINT('Ctrl Pts',(1.63215653474165,1.8773735969273,15.3506369080909));
#26966=CARTESIAN_POINT('Ctrl Pts',(1.69250844011902,1.96237776657714,15.3567445790035));
#26967=CARTESIAN_POINT('Ctrl Pts',(1.75291890778438,2.04746441976471,15.3628581764761));
#26968=CARTESIAN_POINT('Ctrl Pts',(1.81723216529803,2.12971712583411,15.3689717739487));
#26969=CARTESIAN_POINT('Ctrl Pts',(1.88514165812614,2.20877346443409,15.3750853714212));
#26970=CARTESIAN_POINT('Ctrl Pts',(1.95308777961948,2.28787244402635,15.3812022664139));
#26971=CARTESIAN_POINT('Ctrl Pts',(2.02463371065202,2.36377131310707,15.3873191614065));
#26972=CARTESIAN_POINT('Ctrl Pts',(2.09943561816621,2.43614412519072,15.3934360563991));
#26973=CARTESIAN_POINT('Ctrl Pts',(2.17434565711162,2.50862155727688,15.3995617937948));
#26974=CARTESIAN_POINT('Ctrl Pts',(2.25252075476105,2.5775624729625,15.4056875311904));
#26975=CARTESIAN_POINT('Ctrl Pts',(2.33358354254727,2.64268082561201,15.411813268586));
#26976=CARTESIAN_POINT('Ctrl Pts',(2.3753341480884,2.67621940390675,15.4149682704387));
#26977=CARTESIAN_POINT('Ctrl Pts',(2.41785027223247,2.70874467938232,15.4181232722915));
#26978=CARTESIAN_POINT('Ctrl Pts',(2.46107751393011,2.74022215448416,15.4212782741442));
#26979=CARTESIAN_POINT('Ctrl Pts',(2.54498702904448,2.80132389424574,15.427402529712));
#26980=CARTESIAN_POINT('Ctrl Pts',(2.63183486823323,2.85866212129903,15.4335267852798));
#26981=CARTESIAN_POINT('Ctrl Pts',(2.72125043459067,2.91194457779249,15.4396510408476));
#26982=CARTESIAN_POINT('Ctrl Pts',(2.81055518966647,2.96516100218959,15.4457677067234));
#26983=CARTESIAN_POINT('Ctrl Pts',(2.90242098265036,3.01433143556791,15.4518843725992));
#26984=CARTESIAN_POINT('Ctrl Pts',(2.9964465891759,3.05920566687324,15.458001038475));
#26985=CARTESIAN_POINT('Ctrl Pts',(3.09038192539221,3.10403681618329,15.464111831979));
#26986=CARTESIAN_POINT('Ctrl Pts',(3.18647257007655,3.14457978562317,15.470222625483));
#26987=CARTESIAN_POINT('Ctrl Pts',(3.28429165528187,3.18062966816578,15.476333418987));
#26988=CARTESIAN_POINT('Ctrl Pts',(3.38204828979246,3.21665653536117,15.4824403111737));
#26989=CARTESIAN_POINT('Ctrl Pts',(3.48153077341354,3.24819587466238,15.4885472033603));
#26990=CARTESIAN_POINT('Ctrl Pts',(3.58229186616218,3.27509071866231,15.4946540955469));
#26991=CARTESIAN_POINT('Ctrl Pts',(3.683020481052,3.30197689377107,15.500759019327));
#26992=CARTESIAN_POINT('Ctrl Pts',(3.78502647661581,3.32422144061892,15.5068639431072));
#26993=CARTESIAN_POINT('Ctrl Pts',(3.8878477862843,3.34171735145518,15.5129688668874));
#26994=CARTESIAN_POINT('Ctrl Pts',(3.99066195666558,3.35921204748166,15.5190733667788));
#26995=CARTESIAN_POINT('Ctrl Pts',(4.09429091070886,3.37195869258122,15.5251778666701));
#26996=CARTESIAN_POINT('Ctrl Pts',(4.19826358574929,3.37990162160075,15.5312823665615));
#26997=CARTESIAN_POINT('Ctrl Pts',(4.30225533447414,3.38784600774275,15.5373879863173));
#26998=CARTESIAN_POINT('Ctrl Pts',(4.40659050696824,3.3909848943031,15.5434936060731));
#26999=CARTESIAN_POINT('Ctrl Pts',(4.51079499737456,3.38931464459264,15.5495992258289));
#27000=CARTESIAN_POINT('Ctrl Pts',(4.61510446294567,3.38764271227964,15.5557109963604));
#27001=CARTESIAN_POINT('Ctrl Pts',(4.71928255921592,3.38115197747714,15.5618227668918));
#27002=CARTESIAN_POINT('Ctrl Pts',(4.82285732306245,3.36989090877698,15.5679345374233));
#27003=CARTESIAN_POINT('Ctrl Pts',(4.92649008825309,3.35862353393528,15.5740497305153));
#27004=CARTESIAN_POINT('Ctrl Pts',(5.02951842934428,3.34258056854254,15.5801649236074));
#27005=CARTESIAN_POINT('Ctrl Pts',(5.13147947861677,3.3218618363283,15.5862801166994));
#27006=CARTESIAN_POINT('Ctrl Pts',(5.23359142989047,3.30111244046186,15.5924043602562));
#27007=CARTESIAN_POINT('Ctrl Pts',(5.33463252415536,3.27567356157461,15.5985286038129));
#27008=CARTESIAN_POINT('Ctrl Pts',(5.43415391523411,3.24569522240146,15.6046528473696));
#27009=CARTESIAN_POINT('Ctrl Pts',(5.48579046667504,3.23014099796741,15.6078304036118));
#27010=CARTESIAN_POINT('Ctrl Pts',(5.5370182091448,3.2133655359543,15.611007959854));
#27011=CARTESIAN_POINT('Ctrl Pts',(5.58777668886605,3.19539484507684,15.6141855160962));
#27012=CARTESIAN_POINT('Ctrl Pts',(5.68459211532516,3.16111800876059,15.6202463056308));
#27013=CARTESIAN_POINT('Ctrl Pts',(5.78001811340089,3.12237696064005,15.6263070951653));
#27014=CARTESIAN_POINT('Ctrl Pts',(5.87361055453002,3.0793043334456,15.6323678846999));
#27015=CARTESIAN_POINT('Ctrl Pts',(5.967083541579,3.03628668078754,15.6384209387162));
#27016=CARTESIAN_POINT('Ctrl Pts',(6.05872723190476,2.98894861657474,15.6444739927325));
#27017=CARTESIAN_POINT('Ctrl Pts',(6.14811421064749,2.93747202593669,15.6505270467488));
#27018=CARTESIAN_POINT('Ctrl Pts',(6.23741355706659,2.8860459014103,15.6565741665318));
#27019=CARTESIAN_POINT('Ctrl Pts',(6.32446021598998,2.83048953163787,15.6626212863147));
#27020=CARTESIAN_POINT('Ctrl Pts',(6.40884914271364,2.77103180342527,15.6686684060977));
#27021=CARTESIAN_POINT('Ctrl Pts',(6.49318591791259,2.71161081950249,15.6747117888203));
#27022=CARTESIAN_POINT('Ctrl Pts',(6.57486787119696,2.64829351790517,15.6807551715428));
#27023=CARTESIAN_POINT('Ctrl Pts',(6.65351760202964,2.58135293393851,15.6867985542654));
#27024=CARTESIAN_POINT('Ctrl Pts',(6.73214331204496,2.51443279463865,15.6928400912475));
#27025=CARTESIAN_POINT('Ctrl Pts',(6.8077383092479,2.44389185254269,15.6988816282296));
#27026=CARTESIAN_POINT('Ctrl Pts',(6.87995779939702,2.37004380055194,15.7049231652116));
#27027=CARTESIAN_POINT('Ctrl Pts',(6.95217457789299,2.29619852136258,15.7109644753498));
#27028=CARTESIAN_POINT('Ctrl Pts',(7.02101579796853,2.21904668959344,15.7170057854879));
#27029=CARTESIAN_POINT('Ctrl Pts',(7.0861738280999,2.13893855409952,15.7230470956261));
#27030=CARTESIAN_POINT('Ctrl Pts',(7.15134686593554,2.05881196747679,15.7290897972457));
#27031=CARTESIAN_POINT('Ctrl Pts',(7.21283475474115,1.97572806112051,15.7351324988654));
#27032=CARTESIAN_POINT('Ctrl Pts',(7.27037105363037,1.89006901801239,15.7411752004851));
#27033=CARTESIAN_POINT('Ctrl Pts',(7.32797339400618,1.80431165348532,15.7472248380566));
#27034=CARTESIAN_POINT('Ctrl Pts',(7.38161484736974,1.71597361231948,15.7532744756282));
#27035=CARTESIAN_POINT('Ctrl Pts',(7.43107318596542,1.62546474315855,15.7593241131997));
#27036=CARTESIAN_POINT('Ctrl Pts',(7.48056239692778,1.53489937749825,15.7653775270127));
#27037=CARTESIAN_POINT('Ctrl Pts',(7.5258631056482,1.44216087624684,15.7714309408257));
#27038=CARTESIAN_POINT('Ctrl Pts',(7.56680071099599,1.34768036671191,15.7774843546387));
#27039=CARTESIAN_POINT('Ctrl Pts',(7.60780727671575,1.2530407025067,15.7835479655715));
#27040=CARTESIAN_POINT('Ctrl Pts',(7.64443591059099,1.15665357617439,15.7896115765044));
#27041=CARTESIAN_POINT('Ctrl Pts',(7.676561438148,1.05896668330369,15.7956751874372));
#27042=CARTESIAN_POINT('Ctrl Pts',(7.69672519224084,0.997652998028258,15.7994810443075));
#27043=CARTESIAN_POINT('Ctrl Pts',(7.71511595455904,0.93582753295867,15.8032869011778));
#27044=CARTESIAN_POINT('Ctrl Pts',(7.73171311583309,0.87360273579135,15.8070927580481));
#27045=CARTESIAN_POINT('Ctrl Pts',(7.76750271846708,0.739423117492312,15.8152995894948));
#27046=CARTESIAN_POINT('Ctrl Pts',(7.79504513129767,0.603033542451122,15.8235064209414));
#27047=CARTESIAN_POINT('Ctrl Pts',(7.81413184432017,0.465302052071446,15.8317132523881));
#27048=CARTESIAN_POINT('Ctrl Pts',(7.83277876971196,0.330744110000419,15.839730985641));
#27049=CARTESIAN_POINT('Ctrl Pts',(7.84335525746938,0.194904947860224,15.8477487188939));
#27050=CARTESIAN_POINT('Ctrl Pts',(7.84571229878143,0.0586143682396561,
15.8557664521468));
#27051=CARTESIAN_POINT('Ctrl Pts',(7.84602728349793,0.0404010898538724,
15.8568379070351));
#27052=CARTESIAN_POINT('Ctrl Pts',(7.84619554872783,0.0221797858149499,
15.8579093619233));
#27053=CARTESIAN_POINT('Ctrl Pts',(7.84621680191345,0.00395247126457767,
15.8589808168116));
#27054=CARTESIAN_POINT('Ctrl Pts',(7.63534113152507,-1.17693572858576,14.3356579957882));
#27055=CARTESIAN_POINT('Ctrl Pts',(7.58665830007405,-1.30842675843014,14.3432073630502));
#27056=CARTESIAN_POINT('Ctrl Pts',(7.52981495633585,-1.43690350974026,14.3508698715488));
#27057=CARTESIAN_POINT('Ctrl Pts',(7.43034157789848,-1.62855023279599,14.3630352623339));
#27058=CARTESIAN_POINT('Ctrl Pts',(7.39337400048291,-1.69430864236812,14.3673500024656));
#27059=CARTESIAN_POINT('Ctrl Pts',(7.3171048693977,-1.81997040719947,14.3759065961932));
#27060=CARTESIAN_POINT('Ctrl Pts',(7.27803684851843,-1.87996904659493,14.3801387631629));
#27061=CARTESIAN_POINT('Ctrl Pts',(7.1697796117886,-2.03524121704058,14.3915056785217));
#27062=CARTESIAN_POINT('Ctrl Pts',(7.09748081369061,-2.12821834469454,14.3987479684427));
#27063=CARTESIAN_POINT('Ctrl Pts',(6.90572744719545,-2.34996308525917,14.4171216305944));
#27064=CARTESIAN_POINT('Ctrl Pts',(6.78082891353199,-2.47356780965724,14.4284001614553));
#27065=CARTESIAN_POINT('Ctrl Pts',(6.54513791918609,-2.67313672004542,14.448146401));
#27066=CARTESIAN_POINT('Ctrl Pts',(6.43833404809872,-2.75325515800436,14.4566174958412));
#27067=CARTESIAN_POINT('Ctrl Pts',(6.28614368746979,-2.85396311487142,14.467810967368));
#27068=CARTESIAN_POINT('Ctrl Pts',(6.24462221213434,-2.88016033644655,14.4707809031204));
#27069=CARTESIAN_POINT('Ctrl Pts',(6.16712095307125,-2.92673594625997,14.4761517285764));
#27070=CARTESIAN_POINT('Ctrl Pts',(6.13131182239407,-2.94737425722543,14.4785656933484));
#27071=CARTESIAN_POINT('Ctrl Pts',(6.02910052406289,-3.00381848249485,14.4852875006851));
#27072=CARTESIAN_POINT('Ctrl Pts',(5.96186458046848,-3.03807193768808,14.4895144352655));
#27073=CARTESIAN_POINT('Ctrl Pts',(5.79041986550873,-3.11832382280282,14.4999455924316));
#27074=CARTESIAN_POINT('Ctrl Pts',(5.68493106863429,-3.16136864905155,14.5060552710834));
#27075=CARTESIAN_POINT('Ctrl Pts',(5.36434262180131,-3.27370930169096,14.5242198963593));
#27076=CARTESIAN_POINT('Ctrl Pts',(5.14430083175794,-3.32690333446928,14.5362052077099));
#27077=CARTESIAN_POINT('Ctrl Pts',(4.84118412000192,-3.36880224647428,14.5533268161884));
#27078=CARTESIAN_POINT('Ctrl Pts',(4.76139765575346,-3.37695889736455,14.5578841101741));
#27079=CARTESIAN_POINT('Ctrl Pts',(4.61169672140212,-3.386914471621,14.5665701949982));
#27080=CARTESIAN_POINT('Ctrl Pts',(4.54186975807453,-3.38939389127869,14.5706763849023));
#27081=CARTESIAN_POINT('Ctrl Pts',(4.3710570939619,-3.39017749914986,14.5808734183801));
#27082=CARTESIAN_POINT('Ctrl Pts',(4.27013270249032,-3.38612971543642,14.5870296703624));
#27083=CARTESIAN_POINT('Ctrl Pts',(3.89507564888938,-3.35426895289127,14.6103964485958));
#27084=CARTESIAN_POINT('Ctrl Pts',(3.62447768362533,-3.29758189131736,14.6283357623796));
#27085=CARTESIAN_POINT('Ctrl Pts',(3.28423225754883,-3.18171737751498,14.6509980102216));
#27086=CARTESIAN_POINT('Ctrl Pts',(3.20572417750778,-3.15168270766108,14.6562251345375));
#27087=CARTESIAN_POINT('Ctrl Pts',(3.08939687548366,-3.10214706804349,14.6638902516287));
#27088=CARTESIAN_POINT('Ctrl Pts',(3.0506974745338,-3.08480301837545,14.6664261899912));
#27089=CARTESIAN_POINT('Ctrl Pts',(2.96993186230833,-3.04677014599326,14.6716749052445));
#27090=CARTESIAN_POINT('Ctrl Pts',(2.92794978728981,-3.02592638411615,14.6743793807556));
#27091=CARTESIAN_POINT('Ctrl Pts',(2.77233647371357,-2.9446000788038,14.684362339319));
#27092=CARTESIAN_POINT('Ctrl Pts',(2.66173957348852,-2.87852809822419,14.6913749023029));
#27093=CARTESIAN_POINT('Ctrl Pts',(2.32034767048848,-2.64723185885417,14.7135618886605));
#27094=CARTESIAN_POINT('Ctrl Pts',(2.10644564829221,-2.45931597448323,14.7284149760165));
#27095=CARTESIAN_POINT('Ctrl Pts',(1.86824108031662,-2.19025487106494,14.7486522756236));
#27096=CARTESIAN_POINT('Ctrl Pts',(1.81995673141202,-2.1318869563682,14.7529830975558));
#27097=CARTESIAN_POINT('Ctrl Pts',(1.72999089231061,-2.01539774554924,14.7615476289362));
#27098=CARTESIAN_POINT('Ctrl Pts',(1.68811383121299,-1.95747783878978,14.7657707974927));
#27099=CARTESIAN_POINT('Ctrl Pts',(1.58294498875684,-1.80188817326071,14.7770438672238));
#27100=CARTESIAN_POINT('Ctrl Pts',(1.52280149843369,-1.70221379493733,14.7841975758383));
#27101=CARTESIAN_POINT('Ctrl Pts',(1.38710717112199,-1.44870179233611,14.8022070655818));
#27102=CARTESIAN_POINT('Ctrl Pts',(1.31786626984022,-1.29185342656602,14.8132009644796));
#27103=CARTESIAN_POINT('Ctrl Pts',(1.21353971397055,-0.996932400158895,
14.8332140649252));
#27104=CARTESIAN_POINT('Ctrl Pts',(1.17471713020541,-0.860566842966036,
14.8422223309456));
#27105=CARTESIAN_POINT('Ctrl Pts',(1.13421693637355,-0.674827950371699,
14.8538717916236));
#27106=CARTESIAN_POINT('Ctrl Pts',(1.12491086327081,-0.627273830276235,
14.8568004474482));
#27107=CARTESIAN_POINT('Ctrl Pts',(1.10952079673458,-0.538581191569215,
14.8621432926503));
#27108=CARTESIAN_POINT('Ctrl Pts',(1.1031684688041,-0.497501378902117,14.8645688951387));
#27109=CARTESIAN_POINT('Ctrl Pts',(1.08714444288074,-0.379549574504474,
14.8714155560912));
#27110=CARTESIAN_POINT('Ctrl Pts',(1.07934971595382,-0.302444835208961,
14.8757501548422));
#27111=CARTESIAN_POINT('Ctrl Pts',(1.05884368415505,0.00562206874243125,
14.8927376340647));
#27112=CARTESIAN_POINT('Ctrl Pts',(1.06713816428454,0.237355099552328,14.9048160444102));
#27113=CARTESIAN_POINT('Ctrl Pts',(1.11719527366864,0.597667210703678,14.9244786301573));
#27114=CARTESIAN_POINT('Ctrl Pts',(1.14310031675231,0.727693949935586,14.9317520085179));
#27115=CARTESIAN_POINT('Ctrl Pts',(1.19500238578548,0.926597992621719,14.9433829339954));
#27116=CARTESIAN_POINT('Ctrl Pts',(1.21574190170364,0.996712133932492,14.9475820310902));
#27117=CARTESIAN_POINT('Ctrl Pts',(1.2617824576632,1.13567357929309,14.9561332479691));
#27118=CARTESIAN_POINT('Ctrl Pts',(1.28708340665714,1.2044792870784,14.9604834579008));
#27119=CARTESIAN_POINT('Ctrl Pts',(1.36505824067115,1.39701767719163,14.9730082906015));
#27120=CARTESIAN_POINT('Ctrl Pts',(1.42288665691261,1.51850272654646,14.9813390990154));
#27121=CARTESIAN_POINT('Ctrl Pts',(1.60426636518422,1.84759095634546,15.0050575059857));
#27122=CARTESIAN_POINT('Ctrl Pts',(1.74299680962739,2.04590208162645,15.0207635131366));
#27123=CARTESIAN_POINT('Ctrl Pts',(1.94730839967958,2.28020908736534,15.0402064664162));
#27124=CARTESIAN_POINT('Ctrl Pts',(1.9946167381705,2.33120680529413,15.044495683185));
#27125=CARTESIAN_POINT('Ctrl Pts',(2.07200824219159,2.40964796146776,15.0511392392657));
#27126=CARTESIAN_POINT('Ctrl Pts',(2.10107235135283,2.43806555070188,15.053555381949));
#27127=CARTESIAN_POINT('Ctrl Pts',(2.16795749864627,2.50114983282787,15.0589326165445));
#27128=CARTESIAN_POINT('Ctrl Pts',(2.20606680305857,2.53549323590168,15.0618732435799));
#27129=CARTESIAN_POINT('Ctrl Pts',(2.29227548982036,2.60970720895876,15.0682953773071));
#27130=CARTESIAN_POINT('Ctrl Pts',(2.34072739422313,2.64914014221746,15.0717541803964));
#27131=CARTESIAN_POINT('Ctrl Pts',(2.5056517970391,2.77595218334675,15.0831359743811));
#27132=CARTESIAN_POINT('Ctrl Pts',(2.62666148457519,2.85716751379135,15.090867503483));
#27133=CARTESIAN_POINT('Ctrl Pts',(2.91504857675248,3.02485934193698,15.1086988718904));
#27134=CARTESIAN_POINT('Ctrl Pts',(3.08514059464031,3.10567235453147,15.118813556833));
#27135=CARTESIAN_POINT('Ctrl Pts',(3.33323004691758,3.19917015252111,15.1337102988387));
#27136=CARTESIAN_POINT('Ctrl Pts',(3.40631725950975,3.22390066125,15.1381120743341));
#27137=CARTESIAN_POINT('Ctrl Pts',(3.5479582078042,3.26650001131454,15.146703113605));
#27138=CARTESIAN_POINT('Ctrl Pts',(3.61635348425968,3.28475555331739,15.1508777403627));
#27139=CARTESIAN_POINT('Ctrl Pts',(3.7924795844436,3.32590514944427,15.1617130095826));
#27140=CARTESIAN_POINT('Ctrl Pts',(3.90083988234605,3.34571360508594,15.1684612664841));
#27141=CARTESIAN_POINT('Ctrl Pts',(4.1989099542007,3.38532115905227,15.1872315736512));
#27142=CARTESIAN_POINT('Ctrl Pts',(4.3896267794975,3.39444526709788,15.199485802204));
#27143=CARTESIAN_POINT('Ctrl Pts',(4.71063843488363,3.38273124638337,15.2200182019993));
#27144=CARTESIAN_POINT('Ctrl Pts',(4.84082033104307,3.37042310054339,15.2283105864281));
#27145=CARTESIAN_POINT('Ctrl Pts',(5.01882257874528,3.34314309902446,15.2393598723331));
#27146=CARTESIAN_POINT('Ctrl Pts',(5.06750369496389,3.33458910640888,15.2423508945855));
#27147=CARTESIAN_POINT('Ctrl Pts',(5.15658138557914,3.31692039853889,15.2477465933055));
#27148=CARTESIAN_POINT('Ctrl Pts',(5.19702846418774,3.30812485669626,15.2501648877283));
#27149=CARTESIAN_POINT('Ctrl Pts',(5.31052830341169,3.28125736917216,15.2568816765116));
#27150=CARTESIAN_POINT('Ctrl Pts',(5.38315857167098,3.26148972639281,15.2611001485773));
#27151=CARTESIAN_POINT('Ctrl Pts',(5.56339371484462,3.20592745947531,15.2714988217269));
#27152=CARTESIAN_POINT('Ctrl Pts',(5.66997433634521,3.16712178894913,15.2775857755976));
#27153=CARTESIAN_POINT('Ctrl Pts',(5.98255982154462,3.03520876974245,15.2957402386209));
#27154=CARTESIAN_POINT('Ctrl Pts',(6.18138621916954,2.926789627391,15.307736739289));
#27155=CARTESIAN_POINT('Ctrl Pts',(6.43414839274631,2.75419969122762,15.3248694910294));
#27156=CARTESIAN_POINT('Ctrl Pts',(6.49872275389224,2.7066639871127,15.3294274881923));
#27157=CARTESIAN_POINT('Ctrl Pts',(6.61647908348397,2.61336440861976,15.3381283550049));
#27158=CARTESIAN_POINT('Ctrl Pts',(6.67004371982324,2.56815167529463,15.3422491055993));
#27159=CARTESIAN_POINT('Ctrl Pts',(6.79794085571625,2.45322105327304,15.3525174249781));
#27160=CARTESIAN_POINT('Ctrl Pts',(6.87060127560662,2.38175277996041,15.3587321617202));
#27161=CARTESIAN_POINT('Ctrl Pts',(7.13101337127555,2.10143745365094,15.3824962629268));
#27162=CARTESIAN_POINT('Ctrl Pts',(7.29577961548857,1.87283606016177,15.4008007176375));
#27163=CARTESIAN_POINT('Ctrl Pts',(7.4687210491343,1.55662984957034,15.4234755609165));
#27164=CARTESIAN_POINT('Ctrl Pts',(7.50449258466896,1.48536627018671,15.4284225009341));
#27165=CARTESIAN_POINT('Ctrl Pts',(7.55515400789082,1.3748841065386,15.4357803426442));
#27166=CARTESIAN_POINT('Ctrl Pts',(7.57188376927471,1.33654275360874,15.4382781052162));
#27167=CARTESIAN_POINT('Ctrl Pts',(7.60607147938297,1.25405821995434,15.4435206211345));
#27168=CARTESIAN_POINT('Ctrl Pts',(7.62332024031651,1.20983946454218,15.4462547959012));
#27169=CARTESIAN_POINT('Ctrl Pts',(7.68853669589925,1.03168785497911,15.4570220163268));
#27170=CARTESIAN_POINT('Ctrl Pts',(7.72898510253545,0.895146443451765,15.464723959605));
#27171=CARTESIAN_POINT('Ctrl Pts',(7.81671710716394,0.511925485432159,15.4857933823505));
#27172=CARTESIAN_POINT('Ctrl Pts',(7.84537866092038,0.261953575955565,15.4989885251966));
#27173=CARTESIAN_POINT('Ctrl Pts',(7.84646533925544,-0.0695636817773458,
15.51751063256));
#27174=CARTESIAN_POINT('Ctrl Pts',(7.84384964399876,-0.150217268898216,
15.5220897220954));
#27175=CARTESIAN_POINT('Ctrl Pts',(7.83364721216822,-0.299779499649458,
15.5307589005805));
#27176=CARTESIAN_POINT('Ctrl Pts',(7.82681933920101,-0.36869771872418,15.5348241423345));
#27177=CARTESIAN_POINT('Ctrl Pts',(7.80525540834102,-0.534433442984226,
15.5447895926238));
#27178=CARTESIAN_POINT('Ctrl Pts',(7.78842605609443,-0.630911194058193,
15.5507490720102));
#27179=CARTESIAN_POINT('Ctrl Pts',(7.74079236167246,-0.847993049410495,
15.5645217296209));
#27180=CARTESIAN_POINT('Ctrl Pts',(7.7074747316849,-0.967899760807301,15.5723917826965));
#27181=CARTESIAN_POINT('Ctrl Pts',(7.65731059974537,-1.11627074897095,15.5823947841524));
#27182=CARTESIAN_POINT('Ctrl Pts',(7.6465404989509,-1.14668653131824,15.5844594627058));
#27183=CARTESIAN_POINT('Ctrl Pts',(7.63534118765004,-1.1769355769937,15.5865253037982));
#27184=CARTESIAN_POINT('Origin',(4.45646910621825,3.5527136788005E-15,11.));
#27185=CARTESIAN_POINT('',(1.91109182286968,-2.23862894377631,16.));
#27186=CARTESIAN_POINT('Ctrl Pts',(7.63534118765004,-1.1769355769937,15.5865253037982));
#27187=CARTESIAN_POINT('Ctrl Pts',(7.57287868542809,-1.34564515492739,15.5980472269201));
#27188=CARTESIAN_POINT('Ctrl Pts',(7.49706535147243,-1.50916707843466,15.609622999056));
#27189=CARTESIAN_POINT('Ctrl Pts',(7.38299228721335,-1.71130966053183,15.6239307665769));
#27190=CARTESIAN_POINT('Ctrl Pts',(7.35634675334713,-1.75608341487065,15.6270983971135));
#27191=CARTESIAN_POINT('Ctrl Pts',(7.30731325697073,-1.83431488249896,15.6326072562216));
#27192=CARTESIAN_POINT('Ctrl Pts',(7.28534509373262,-1.86801613048383,15.6349694244418));
#27193=CARTESIAN_POINT('Ctrl Pts',(7.22605793113205,-1.95552266151023,15.6410851910244));
#27194=CARTESIAN_POINT('Ctrl Pts',(7.187771701958,-2.00865088652369,15.6447831805304));
#27195=CARTESIAN_POINT('Ctrl Pts',(7.09317533200132,-2.13220766450349,15.6534293053547));
#27196=CARTESIAN_POINT('Ctrl Pts',(7.03554688153645,-2.20156505412838,15.6583206365791));
#27197=CARTESIAN_POINT('Ctrl Pts',(6.78504263841076,-2.4796981632243,15.6784523425935));
#27198=CARTESIAN_POINT('Ctrl Pts',(6.56908494627282,-2.6660843509193,15.6933318109013));
#27199=CARTESIAN_POINT('Ctrl Pts',(6.2690541879617,-2.8654364258646,15.7136158457069));
#27200=CARTESIAN_POINT('Ctrl Pts',(6.2043060658752,-2.90538385109082,15.7179651487505));
#27201=CARTESIAN_POINT('Ctrl Pts',(6.07601642730848,-2.97869316118489,15.7265625524124));
#27202=CARTESIAN_POINT('Ctrl Pts',(6.01265104129785,-3.0122820496391,15.7307999191233));
#27203=CARTESIAN_POINT('Ctrl Pts',(5.84334705324833,-3.09525898965031,15.7421167677686));
#27204=CARTESIAN_POINT('Ctrl Pts',(5.73584343432221,-3.14121880076511,15.7493004664225));
#27205=CARTESIAN_POINT('Ctrl Pts',(5.46402481317999,-3.24115548378397,15.7674347008708));
#27206=CARTESIAN_POINT('Ctrl Pts',(5.29754601618224,-3.28828838792893,15.7785252537061));
#27207=CARTESIAN_POINT('Ctrl Pts',(4.99426819976438,-3.34960470921569,15.7982985254542));
#27208=CARTESIAN_POINT('Ctrl Pts',(4.85879821671769,-3.36856295242495,15.8069772564395));
#27209=CARTESIAN_POINT('Ctrl Pts',(4.67331741345244,-3.3831671935792,15.8183833240157));
#27210=CARTESIAN_POINT('Ctrl Pts',(4.62400801301181,-3.38596732532963,15.8213695487727));
#27211=CARTESIAN_POINT('Ctrl Pts',(4.53210569139429,-3.38917343707562,15.8268290512374));
#27212=CARTESIAN_POINT('Ctrl Pts',(4.48953469607301,-3.38985608390243,15.8293138195986));
#27213=CARTESIAN_POINT('Ctrl Pts',(4.36599785529308,-3.38950956413695,15.836421574768));
#27214=CARTESIAN_POINT('Ctrl Pts',(4.28506305037642,-3.38638183531605,15.840951438062));
#27215=CARTESIAN_POINT('Ctrl Pts',(3.95145715744809,-3.36149664033698,15.8593677203472));
#27216=CARTESIAN_POINT('Ctrl Pts',(3.70151064721115,-3.31432439675801,15.8726173148998));
#27217=CARTESIAN_POINT('Ctrl Pts',(3.3530882847967,-3.20706589827191,15.8925709104828));
#27218=CARTESIAN_POINT('Ctrl Pts',(3.24869857339809,-3.16922833422206,15.89874304801));
#27219=CARTESIAN_POINT('Ctrl Pts',(3.08026511340122,-3.09864535013521,15.9091548543334));
#27220=CARTESIAN_POINT('Ctrl Pts',(3.01507087895972,-3.06886143883022,15.9133012205377));
#27221=CARTESIAN_POINT('Ctrl Pts',(2.88006749071585,-3.0019341215573,15.9221615100324));
#27222=CARTESIAN_POINT('Ctrl Pts',(2.81051621535204,-2.96436976939012,15.9268873165097));
#27223=CARTESIAN_POINT('Ctrl Pts',(2.56913471593602,-2.82288562411376,15.9438927047818));
#27224=CARTESIAN_POINT('Ctrl Pts',(2.40530800731997,-2.70618437371263,15.9565884738196));
#27225=CARTESIAN_POINT('Ctrl Pts',(2.13105570550647,-2.47154271046629,15.9796856731913));
#27226=CARTESIAN_POINT('Ctrl Pts',(2.0168726413096,-2.35890438871753,15.9899931553525));
#27227=CARTESIAN_POINT('Ctrl Pts',(1.91109182286968,-2.23862894377631,16.));
#27228=CARTESIAN_POINT('',(7.02970353323295,-2.20655152809223,16.));
#27229=CARTESIAN_POINT('Origin',(4.45646910621825,4.66293670342566E-15,
16.));
#27230=CARTESIAN_POINT('Ctrl Pts',(7.63534122786842,-1.17693546836491,15.9331819277137));
#27231=CARTESIAN_POINT('Ctrl Pts',(7.60150329790276,-1.26833083804343,15.9386824302914));
#27232=CARTESIAN_POINT('Ctrl Pts',(7.56373832442186,-1.35822782981906,15.9440894988472));
#27233=CARTESIAN_POINT('Ctrl Pts',(7.41799056413079,-1.66714887260322,15.9628796855318));
#27234=CARTESIAN_POINT('Ctrl Pts',(7.29029618195467,-1.87600691097348,15.975933202696));
#27235=CARTESIAN_POINT('Ctrl Pts',(7.1216017376502,-2.09487803078569,15.9916272221289));
#27236=CARTESIAN_POINT('Ctrl Pts',(7.1015435677313,-2.12014784525936,15.9934733811096));
#27237=CARTESIAN_POINT('Ctrl Pts',(7.06422882167378,-2.16580411711061,15.9968789069984));
#27238=CARTESIAN_POINT('Ctrl Pts',(7.04708601173215,-2.18628044376383,15.9984327879153));
#27239=CARTESIAN_POINT('Ctrl Pts',(7.02970353323297,-2.20655152809224,16.));
#27240=CARTESIAN_POINT('Origin',(4.45646910621825,2.93978508838399E-15,
8.23961502859548));
#27241=CARTESIAN_POINT('',(8.54146786266509,-0.00318744843224361,15.0103849714045));
#27242=CARTESIAN_POINT('Ctrl Pts',(7.70074909849077,2.48902547716684,14.8803008071898));
#27243=CARTESIAN_POINT('Ctrl Pts',(8.23604156339096,1.78066392614847,14.9236620772348));
#27244=CARTESIAN_POINT('Ctrl Pts',(8.53482634894621,0.886500306172487,14.9670233472798));
#27245=CARTESIAN_POINT('Ctrl Pts',(8.54231068068493,-0.00318084115196966,
15.0103846173248));
#27246=CARTESIAN_POINT('',(5.51582329814257,3.94524950998694,16.));
#27247=CARTESIAN_POINT('Ctrl Pts',(8.54146786266509,-0.00318744843224361,
15.0103849714045));
#27248=CARTESIAN_POINT('Ctrl Pts',(8.5413411088023,-0.16563380102107,15.0183039705911));
#27249=CARTESIAN_POINT('Ctrl Pts',(8.5315207628645,-0.327697487422329,15.0262229697777));
#27250=CARTESIAN_POINT('Ctrl Pts',(8.5121651071872,-0.488420871507605,15.0341419689643));
#27251=CARTESIAN_POINT('Ctrl Pts',(8.49838784829654,-0.602822972332438,
15.0397786729731));
#27252=CARTESIAN_POINT('Ctrl Pts',(8.47978051169544,-0.716546691674619,
15.0454153769818));
#27253=CARTESIAN_POINT('Ctrl Pts',(8.45641452956138,-0.829253646525672,
15.0510520809906));
#27254=CARTESIAN_POINT('Ctrl Pts',(8.43220699270667,-0.946019881631264,
15.0568917978597));
#27255=CARTESIAN_POINT('Ctrl Pts',(8.40284581144963,-1.06190116149562,15.0627315147288));
#27256=CARTESIAN_POINT('Ctrl Pts',(8.36841025348841,-1.17641041320381,15.0685712315979));
#27257=CARTESIAN_POINT('Ctrl Pts',(8.33401631542241,-1.2907812654395,15.074403890402));
#27258=CARTESIAN_POINT('Ctrl Pts',(8.29456031716066,-1.40378300303146,15.0802365492062));
#27259=CARTESIAN_POINT('Ctrl Pts',(8.25017254001739,-1.51493869723509,15.0860692080103));
#27260=CARTESIAN_POINT('Ctrl Pts',(8.20582704431374,-1.62598851042653,15.0918963109334));
#27261=CARTESIAN_POINT('Ctrl Pts',(8.15655926661547,-1.7351954043223,15.0977234138565));
#27262=CARTESIAN_POINT('Ctrl Pts',(8.10254912597376,-1.84209812158294,15.1035505167796));
#27263=CARTESIAN_POINT('Ctrl Pts',(8.04832335640828,-1.94942763495255,15.109400883703));
#27264=CARTESIAN_POINT('Ctrl Pts',(7.98931739859561,-2.05443413914575,15.1152512506265));
#27265=CARTESIAN_POINT('Ctrl Pts',(7.92576215543467,-2.15667121709787,15.1211016175499));
#27266=CARTESIAN_POINT('Ctrl Pts',(7.86252503512946,-2.2583965520437,15.12692270073));
#27267=CARTESIAN_POINT('Ctrl Pts',(7.79478429093661,-2.35737977853133,15.13274378391));
#27268=CARTESIAN_POINT('Ctrl Pts',(7.72281287859392,-2.45320675049259,15.1385648670901));
#27269=CARTESIAN_POINT('Ctrl Pts',(7.65085054814479,-2.54902163028654,15.1443852157221));
#27270=CARTESIAN_POINT('Ctrl Pts',(7.57465885507154,-2.64168072367093,15.1502055643542));
#27271=CARTESIAN_POINT('Ctrl Pts',(7.49455278544562,-2.73080071737431,15.1560259129862));
#27272=CARTESIAN_POINT('Ctrl Pts',(7.41443824631905,-2.81993013360768,15.1618468769954));
#27273=CARTESIAN_POINT('Ctrl Pts',(7.33040877887661,-2.90551940457022,15.1676678410046));
#27274=CARTESIAN_POINT('Ctrl Pts',(7.24281775831271,-2.98722047880151,15.1734888050138));
#27275=CARTESIAN_POINT('Ctrl Pts',(7.15445059989371,-3.06964550048889,15.1793613481746));
#27276=CARTESIAN_POINT('Ctrl Pts',(7.06245876169525,-3.1481127873312,15.1852338913353));
#27277=CARTESIAN_POINT('Ctrl Pts',(6.96724001975915,-3.22230576136355,15.191106434496));
#27278=CARTESIAN_POINT('Ctrl Pts',(6.87272504013762,-3.29595037466282,15.1969355736536));
#27279=CARTESIAN_POINT('Ctrl Pts',(6.77503106424927,-3.36538345784704,15.2027647128113));
#27280=CARTESIAN_POINT('Ctrl Pts',(6.67457632515266,-3.43033895778694,15.2085938519689));
#27281=CARTESIAN_POINT('Ctrl Pts',(6.57299960105461,-3.49601994959859,15.2144880971312));
#27282=CARTESIAN_POINT('Ctrl Pts',(6.46860043536605,-3.55712251093729,15.2203823422935));
#27283=CARTESIAN_POINT('Ctrl Pts',(6.36183591102191,-3.6134197568442,15.2262765874557));
#27284=CARTESIAN_POINT('Ctrl Pts',(6.25507138667778,-3.66971700275111,15.232170832618));
#27285=CARTESIAN_POINT('Ctrl Pts',(6.14594190981078,-3.72120880250603,15.2380650777802));
#27286=CARTESIAN_POINT('Ctrl Pts',(6.03492343531498,-3.76771906210581,15.2439593229425));
#27287=CARTESIAN_POINT('Ctrl Pts',(5.92492052612997,-3.81380385912867,15.2497996492327));
#27288=CARTESIAN_POINT('Ctrl Pts',(5.81273256134718,-3.85513637126823,15.2556399755229));
#27289=CARTESIAN_POINT('Ctrl Pts',(5.69880623137363,-3.89150658067803,15.2614803018131));
#27290=CARTESIAN_POINT('Ctrl Pts',(5.58501722399287,-3.92783295077993,15.2673135883896));
#27291=CARTESIAN_POINT('Ctrl Pts',(5.46949440303382,-3.95920879479499,15.2731468749661));
#27292=CARTESIAN_POINT('Ctrl Pts',(5.35270492787875,-3.98547191082465,15.2789801615426));
#27293=CARTESIAN_POINT('Ctrl Pts',(5.23602634221444,-4.01171009050144,15.2848079095192));
#27294=CARTESIAN_POINT('Ctrl Pts',(5.11808388891667,-4.03284511277884,15.2906356574958));
#27295=CARTESIAN_POINT('Ctrl Pts',(4.99935986061935,-4.04876458055856,15.2964634054723));
#27296=CARTESIAN_POINT('Ctrl Pts',(4.88017982787431,-4.06474519306371,15.3023135371149));
#27297=CARTESIAN_POINT('Ctrl Pts',(4.76021259868044,-4.07546998267526,15.3081636687575));
#27298=CARTESIAN_POINT('Ctrl Pts',(4.63995681778763,-4.08087702089915,15.3140138004001));
#27299=CARTESIAN_POINT('Ctrl Pts',(4.52028412955,-4.08625784163686,15.3198355660983));
#27300=CARTESIAN_POINT('Ctrl Pts',(4.40032609066979,-4.0863723552476,15.3256573317965));
#27301=CARTESIAN_POINT('Ctrl Pts',(4.28057873228645,-4.08121153291003,15.3314790974947));
#27302=CARTESIAN_POINT('Ctrl Pts',(4.1608462210599,-4.07605135044911,15.3373001413676));
#27303=CARTESIAN_POINT('Ctrl Pts',(4.0413247433305,-4.06561715068618,15.3431211852406));
#27304=CARTESIAN_POINT('Ctrl Pts',(3.92250866190083,-4.04995200513587,15.3489422291135));
#27305=CARTESIAN_POINT('Ctrl Pts',(3.80367977842117,-4.03428517171659,15.3547639001852));
#27306=CARTESIAN_POINT('Ctrl Pts',(3.68555684430889,-4.01338632485481,15.3605855712569));
#27307=CARTESIAN_POINT('Ctrl Pts',(3.56862684375788,-3.98735013724516,15.3664072423285));
#27308=CARTESIAN_POINT('Ctrl Pts',(3.45069380063571,-3.961090607427,15.3722788525423));
#27309=CARTESIAN_POINT('Ctrl Pts',(3.3339746663379,-3.92960526169728,15.3781504627562));
#27310=CARTESIAN_POINT('Ctrl Pts',(3.21895516564525,-3.89304305741501,15.38402207297));
#27311=CARTESIAN_POINT('Ctrl Pts',(3.10475334874284,-3.85674077707256,15.3898519413882));
#27312=CARTESIAN_POINT('Ctrl Pts',(2.99222744075082,-3.81543378496055,15.3956818098063));
#27313=CARTESIAN_POINT('Ctrl Pts',(2.88183347553818,-3.76931659994123,15.4015116782245));
#27314=CARTESIAN_POINT('Ctrl Pts',(2.77025388090635,-3.72270411709305,15.4074041593362));
#27315=CARTESIAN_POINT('Ctrl Pts',(2.66085267758504,-3.67117769267325,15.4132966404478));
#27316=CARTESIAN_POINT('Ctrl Pts',(2.55407500616508,-3.61498571063325,15.4191891215595));
#27317=CARTESIAN_POINT('Ctrl Pts',(2.44729733474513,-3.55879372859326,15.4250816026711));
#27318=CARTESIAN_POINT('Ctrl Pts',(2.3431435318916,-3.49793644933757,15.4309740837828));
#27319=CARTESIAN_POINT('Ctrl Pts',(2.24202757610946,-3.43270647008001,15.4368665648944));
#27320=CARTESIAN_POINT('Ctrl Pts',(2.14194567540971,-3.36814356053517,15.4426987869699));
#27321=CARTESIAN_POINT('Ctrl Pts',(2.04453658637758,-3.29910139922817,15.4485310090453));
#27322=CARTESIAN_POINT('Ctrl Pts',(1.95022553558227,-3.22582829125258,15.4543632311207));
#27323=CARTESIAN_POINT('Ctrl Pts',(1.85602877352911,-3.15264397765764,15.460188385548));
#27324=CARTESIAN_POINT('Ctrl Pts',(1.7649229002841,-3.07523916397955,15.4660135399753));
#27325=CARTESIAN_POINT('Ctrl Pts',(1.67730536800752,-2.99390613016078,15.4718386944026));
#27326=CARTESIAN_POINT('Ctrl Pts',(1.58977140288305,-2.91265066951524,15.4776582929604));
#27327=CARTESIAN_POINT('Ctrl Pts',(1.50571945568293,-2.82747471837483,15.4834778915183));
#27328=CARTESIAN_POINT('Ctrl Pts',(1.42551452648788,-2.73871125451575,15.4892974900762));
#27329=CARTESIAN_POINT('Ctrl Pts',(1.34484678420236,-2.64943559155067,15.4951506699416));
#27330=CARTESIAN_POINT('Ctrl Pts',(1.26807092816672,-2.55653113690343,15.5010038498071));
#27331=CARTESIAN_POINT('Ctrl Pts',(1.19552151049901,-2.46037512952245,15.5068570296725));
#27332=CARTESIAN_POINT('Ctrl Pts',(1.1234623353685,-2.36486888290511,15.5126706574941));
#27333=CARTESIAN_POINT('Ctrl Pts',(1.05557289281068,-2.26615522929675,15.5184842853157));
#27334=CARTESIAN_POINT('Ctrl Pts',(0.992140699584164,-2.16463708066453,
15.5242979131372));
#27335=CARTESIAN_POINT('Ctrl Pts',(0.928716171215153,-2.06313119902331,
15.5301108384665));
#27336=CARTESIAN_POINT('Ctrl Pts',(0.869748036305858,-1.95882184132671,
15.5359237637958));
#27337=CARTESIAN_POINT('Ctrl Pts',(0.81547991001562,-1.85214002525064,15.541736689125));
#27338=CARTESIAN_POINT('Ctrl Pts',(0.761205659274564,-1.7454461695561,15.5475502704743));
#27339=CARTESIAN_POINT('Ctrl Pts',(0.711632656193029,-1.63637968566105,
15.5533638518235));
#27340=CARTESIAN_POINT('Ctrl Pts',(0.666957787042784,-1.52539469051153,
15.5591774331728));
#27341=CARTESIAN_POINT('Ctrl Pts',(0.621749226162056,-1.41308385434119,
15.5650604643122));
#27342=CARTESIAN_POINT('Ctrl Pts',(0.581556761098714,-1.29880876174253,
15.5709434954517));
#27343=CARTESIAN_POINT('Ctrl Pts',(0.546533210655599,-1.18305802587635,
15.5768265265912));
#27344=CARTESIAN_POINT('Ctrl Pts',(0.511873454813608,-1.06850960937103,
15.5826484498492));
#27345=CARTESIAN_POINT('Ctrl Pts',(0.482275781891699,-0.952516472742291,
15.5884703731073));
#27346=CARTESIAN_POINT('Ctrl Pts',(0.457837045881869,-0.835563669656465,
15.5942922963654));
#27347=CARTESIAN_POINT('Ctrl Pts',(0.433013540273867,-0.716769532263069,
15.6002058814455));
#27348=CARTESIAN_POINT('Ctrl Pts',(0.413512868062081,-0.596985686145653,
15.6061194665257));
#27349=CARTESIAN_POINT('Ctrl Pts',(0.399381823433392,-0.476726105709688,
15.6120330516059));
#27350=CARTESIAN_POINT('Ctrl Pts',(0.385250778804703,-0.356466525273724,
15.617946636686));
#27351=CARTESIAN_POINT('Ctrl Pts',(0.376489335374794,-0.235731647345663,
15.6238602217662));
#27352=CARTESIAN_POINT('Ctrl Pts',(0.373089128535008,-0.11503459416781,
15.6297738068464));
#27353=CARTESIAN_POINT('Ctrl Pts',(0.369726628840985,0.00432396944400208,
15.6356218122648));
#27354=CARTESIAN_POINT('Ctrl Pts',(0.371596773978119,0.124007618084114,
15.6414698176831));
#27355=CARTESIAN_POINT('Ctrl Pts',(0.378734248619421,0.243522958102947,
15.6473178231015));
#27356=CARTESIAN_POINT('Ctrl Pts',(0.385863086186289,0.362893672334705,
15.6531587518351));
#27357=CARTESIAN_POINT('Ctrl Pts',(0.398246548617625,0.482096082697366,
15.6589996805687));
#27358=CARTESIAN_POINT('Ctrl Pts',(0.41586733996857,0.600634969494553,15.6648406093023));
#27359=CARTESIAN_POINT('Ctrl Pts',(0.433471282366683,0.719060509730135,
15.6706759529557));
#27360=CARTESIAN_POINT('Ctrl Pts',(0.456302529571249,0.836823391003327,
15.6765112966091));
#27361=CARTESIAN_POINT('Ctrl Pts',(0.48429187559633,0.953432246427892,15.6823466402625));
#27362=CARTESIAN_POINT('Ctrl Pts',(0.512338412306017,1.07027936895118,15.6881939072848));
#27363=CARTESIAN_POINT('Ctrl Pts',(0.545564109953098,1.18596733781551,15.6940411743072));
#27364=CARTESIAN_POINT('Ctrl Pts',(0.583847487984841,1.30001030841721,15.6998884413295));
#27365=CARTESIAN_POINT('Ctrl Pts',(0.622012563543342,1.41370086587849,15.7057176392528));
#27366=CARTESIAN_POINT('Ctrl Pts',(0.665203977606165,1.52575619181223,15.711546837176));
#27367=CARTESIAN_POINT('Ctrl Pts',(0.713251241136526,1.63570933069809,15.7173760350993));
#27368=CARTESIAN_POINT('Ctrl Pts',(0.761291932672498,1.74564742998837,15.7232044356939));
#27369=CARTESIAN_POINT('Ctrl Pts',(0.814186990406992,1.85348354396727,15.7290328362886));
#27370=CARTESIAN_POINT('Ctrl Pts',(0.871717914306646,1.95877101573617,15.7348612368833));
#27371=CARTESIAN_POINT('Ctrl Pts',(0.929254198221601,2.06406829688099,15.7406901804958));
#27372=CARTESIAN_POINT('Ctrl Pts',(0.991427013163506,2.16681610898482,15.7465191241083));
#27373=CARTESIAN_POINT('Ctrl Pts',(1.05797235982619,2.26659322878243,15.7523480677208));
#27374=CARTESIAN_POINT('Ctrl Pts',(1.12488460726435,2.36692047423816,15.7582091494772));
#27375=CARTESIAN_POINT('Ctrl Pts',(1.19621752800744,2.46424382093391,15.7640702312337));
#27376=CARTESIAN_POINT('Ctrl Pts',(1.27165979670493,2.55816626942758,15.7699313129902));
#27377=CARTESIAN_POINT('Ctrl Pts',(1.34679040001563,2.65170070763547,15.7757681815788));
#27378=CARTESIAN_POINT('Ctrl Pts',(1.42599615792973,2.74186202032279,15.7816050501675));
#27379=CARTESIAN_POINT('Ctrl Pts',(1.50893111671808,2.8282936199152,15.7874419187561));
#27380=CARTESIAN_POINT('Ctrl Pts',(1.59238213597053,2.91526303772144,15.7933151070965));
#27381=CARTESIAN_POINT('Ctrl Pts',(1.67960862327778,2.99845588218391,15.7991882954368));
#27382=CARTESIAN_POINT('Ctrl Pts',(1.77022349490056,3.07754927103958,15.8050614837772));
#27383=CARTESIAN_POINT('Ctrl Pts',(1.86083836652335,3.15664265989526,15.8109346721176));
#27384=CARTESIAN_POINT('Ctrl Pts',(1.95484126823265,3.23163637683839,15.816807860458));
#27385=CARTESIAN_POINT('Ctrl Pts',(2.05181547261778,3.30225164129141,15.8226810487983));
#27386=CARTESIAN_POINT('Ctrl Pts',(2.14726457977139,3.37175635119023,15.8284618704796));
#27387=CARTESIAN_POINT('Ctrl Pts',(2.2458864851227,3.43723342380028,15.8342426921609));
#27388=CARTESIAN_POINT('Ctrl Pts',(2.34730393370927,3.49837780622319,15.8400235138421));
#27389=CARTESIAN_POINT('Ctrl Pts',(2.44859973993677,3.55944885070449,15.8457974018764));
#27390=CARTESIAN_POINT('Ctrl Pts',(2.55268406939279,3.61619732635631,15.8515712899107));
#27391=CARTESIAN_POINT('Ctrl Pts',(2.65914838909259,3.66835974786971,15.857345177945));
#27392=CARTESIAN_POINT('Ctrl Pts',(2.76874848648944,3.72205855038348,15.863289128864));
#27393=CARTESIAN_POINT('Ctrl Pts',(2.88087060154035,3.7708966766293,15.8692330797829));
#27394=CARTESIAN_POINT('Ctrl Pts',(2.99503843076587,3.81463568127372,15.8751770307019));
#27395=CARTESIAN_POINT('Ctrl Pts',(3.10576537254859,3.85705644247896,15.8809418377568));
#27396=CARTESIAN_POINT('Ctrl Pts',(3.21841607103216,3.89468086910897,15.8867066448117));
#27397=CARTESIAN_POINT('Ctrl Pts',(3.33253362675537,3.92733930772531,15.8924714518666));
#27398=CARTESIAN_POINT('Ctrl Pts',(3.4466163765667,3.95998778550146,15.8982345006525));
#27399=CARTESIAN_POINT('Ctrl Pts',(3.56216469559778,3.98767317264522,15.9039975494383));
#27400=CARTESIAN_POINT('Ctrl Pts',(3.6787058761839,4.01027547158625,15.9097605982242));
#27401=CARTESIAN_POINT('Ctrl Pts',(3.7952400504662,4.03287641170654,15.9155233005431));
#27402=CARTESIAN_POINT('Ctrl Pts',(3.91276656017482,4.05039479318396,15.9212860028619));
#27403=CARTESIAN_POINT('Ctrl Pts',(4.03080256205276,4.0627617445745,15.9270487051808));
#27404=CARTESIAN_POINT('Ctrl Pts',(4.14886037304497,4.07513098096496,15.9328124722548));
#27405=CARTESIAN_POINT('Ctrl Pts',(4.26742745071431,4.08234685297824,15.9385762393288));
#27406=CARTESIAN_POINT('Ctrl Pts',(4.38601662049575,4.08439242082042,15.9443400064027));
#27407=CARTESIAN_POINT('Ctrl Pts',(4.50471413997829,4.08643985760784,15.9501090395768));
#27408=CARTESIAN_POINT('Ctrl Pts',(4.62343337673524,4.08330755509177,15.9558780727509));
#27409=CARTESIAN_POINT('Ctrl Pts',(4.74168797811218,4.07503069867153,15.9616471059249));
#27410=CARTESIAN_POINT('Ctrl Pts',(4.86000791660193,4.06674926918693,15.9674193265604));
#27411=CARTESIAN_POINT('Ctrl Pts',(4.97786229705627,4.05331767293681,15.9731915471958));
#27412=CARTESIAN_POINT('Ctrl Pts',(5.09477231469533,4.0348226744242,15.9789637678312));
#27413=CARTESIAN_POINT('Ctrl Pts',(5.21183125092389,4.01630411720253,15.9847433410526));
#27414=CARTESIAN_POINT('Ctrl Pts',(5.32794301877643,3.99270937000933,15.990522914274));
#27415=CARTESIAN_POINT('Ctrl Pts',(5.442641425784,3.96417572215487,15.9963024874954));
#27416=CARTESIAN_POINT('Ctrl Pts',(5.46710106308048,3.95809087149762,15.9975349916636));
#27417=CARTESIAN_POINT('Ctrl Pts',(5.49149649048049,3.95178159512065,15.9987674958318));
#27418=CARTESIAN_POINT('Ctrl Pts',(5.51582329814257,3.94524950998694,16.));
#27419=CARTESIAN_POINT('',(3.39856468324527,3.94563850749836,16.));
#27420=CARTESIAN_POINT('Origin',(4.45646910621825,4.66293670342566E-15,
16.));
#27421=CARTESIAN_POINT('',(8.53632693677507,0.0015752080993986,15.1146150285955));
#27422=CARTESIAN_POINT('Ctrl Pts',(8.53632693677507,0.0015752080993986,
15.1146150285955));
#27423=CARTESIAN_POINT('Ctrl Pts',(8.53325914244515,-0.779403576318215,
15.1525336964611));
#27424=CARTESIAN_POINT('Ctrl Pts',(7.94795211119873,-2.88890213248947,15.2547547783107));
#27425=CARTESIAN_POINT('Ctrl Pts',(4.59757515362052,-4.78052237191921,15.4212782741442));
#27426=CARTESIAN_POINT('Ctrl Pts',(0.59094744836049,-2.82224505491953,15.6141855160961));
#27427=CARTESIAN_POINT('Ctrl Pts',(-0.0515142140919883,1.59610399861122,
15.8070927580481));
#27428=CARTESIAN_POINT('Ctrl Pts',(2.12325861577974,3.60370350081894,15.935697586016));
#27429=CARTESIAN_POINT('Ctrl Pts',(3.39856468324527,3.94563850749837,16.));
#27430=CARTESIAN_POINT('Ctrl Pts',(7.69668968132748,2.48593167737241,14.9842676783293));
#27431=CARTESIAN_POINT('Ctrl Pts',(7.91254316798409,2.20967240609126,15.0013330489663));
#27432=CARTESIAN_POINT('Ctrl Pts',(8.37131842804349,1.43864013141511,15.0447821657217));
#27433=CARTESIAN_POINT('Ctrl Pts',(8.53846150297425,0.544978949099729,15.0882312824771));
#27434=CARTESIAN_POINT('Ctrl Pts',(8.53632693677507,0.0015752080993986,
15.1146150285955));
#27435=CARTESIAN_POINT('Ctrl Pts',(1.88874933522258,-2.20462348696943,11.0030161694783));
#27436=CARTESIAN_POINT('Ctrl Pts',(1.17566490599146,-1.37417471128399,11.0673602442838));
#27437=CARTESIAN_POINT('Ctrl Pts',(0.626876868360273,1.01685904464542,11.1960067330733));
#27438=CARTESIAN_POINT('Ctrl Pts',(3.13358816217676,3.73802129086872,11.3889556358469));
#27439=CARTESIAN_POINT('Ctrl Pts',(6.78925200599098,3.20274742655601,11.5818628777988));
#27440=CARTESIAN_POINT('Ctrl Pts',(8.41799749193089,-0.111210130011926,
11.7747701197507));
#27441=CARTESIAN_POINT('Ctrl Pts',(6.60488546490453,-3.33054749553302,11.9676773617027));
#27442=CARTESIAN_POINT('Ctrl Pts',(2.92512050779011,-3.65517177063915,12.1605846036546));
#27443=CARTESIAN_POINT('Ctrl Pts',(0.575862327608668,-0.804564055767342,
12.3534918456065));
#27444=CARTESIAN_POINT('Ctrl Pts',(1.59820716428631,2.74533767611897,12.5463990875585));
#27445=CARTESIAN_POINT('Ctrl Pts',(5.10391712761201,3.90985954717001,12.7393063295104));
#27446=CARTESIAN_POINT('Ctrl Pts',(8.04709879850609,1.67742102317504,12.9322135714623));
#27447=CARTESIAN_POINT('Ctrl Pts',(7.87061306779546,-2.01245497181881,13.1251208134143));
#27448=CARTESIAN_POINT('Ctrl Pts',(4.72779527045753,-3.9538206853119,13.3180280553662));
#27449=CARTESIAN_POINT('Ctrl Pts',(1.349240122848,-2.45997262452168,13.5109352973181));
#27450=CARTESIAN_POINT('Ctrl Pts',(0.670356745591222,1.171191815988,13.70384253927));
#27451=CARTESIAN_POINT('Ctrl Pts',(3.28098566906297,3.78478215455868,13.896749781222));
#27452=CARTESIAN_POINT('Ctrl Pts',(6.91291436436904,3.11001488625209,14.0896570231739));
#27453=CARTESIAN_POINT('Ctrl Pts',(8.41059997631734,-0.26683902657174,14.2825642651258));
#27454=CARTESIAN_POINT('Ctrl Pts',(6.47278403753293,-3.41186708033681,14.4754715070778));
#27455=CARTESIAN_POINT('Ctrl Pts',(2.783140900988,-3.59251490415614,14.6683787490297));
#27456=CARTESIAN_POINT('Ctrl Pts',(0.547306324484669,-0.651909986519413,
14.8612859909816));
#27457=CARTESIAN_POINT('Ctrl Pts',(1.70797095253967,2.85520405387232,15.0541932329336));
#27458=CARTESIAN_POINT('Ctrl Pts',(5.25647654433333,3.88140403742585,15.2471004748855));
#27459=CARTESIAN_POINT('Ctrl Pts',(8.11020963540048,1.53571469214933,15.4400077168373));
#27460=CARTESIAN_POINT('Ctrl Pts',(7.78884317528094,-2.14507759945015,15.6329149587894));
#27461=CARTESIAN_POINT('Ctrl Pts',(4.5733715585354,-3.96053038776695,15.8258222007413));
#27462=CARTESIAN_POINT('Ctrl Pts',(1.25399146895312,-2.33815186545114,16.0187294426932));
#27463=CARTESIAN_POINT('Ctrl Pts',(0.72172977469463,1.32232795848172,16.2116366846452));
#27464=CARTESIAN_POINT('Ctrl Pts',(2.52346883354543,2.98556854525621,16.3402415126131));
#27465=CARTESIAN_POINT('Ctrl Pts',(3.58002459062539,3.26885222834281,16.4045439265971));
#27466=CARTESIAN_POINT('Ctrl Pts',(1.71092191398567,-2.35730467668278,10.8676966229016));
#27467=CARTESIAN_POINT('Ctrl Pts',(0.948452825802773,-1.46934317475766,
10.9320406977071));
#27468=CARTESIAN_POINT('Ctrl Pts',(0.361658475084007,1.0872816132268,11.0606871864966));
#27469=CARTESIAN_POINT('Ctrl Pts',(3.04197204832368,3.99689793862148,11.2536360892702));
#27470=CARTESIAN_POINT('Ctrl Pts',(6.95080887526387,3.42455368523382,11.4465433312221));
#27471=CARTESIAN_POINT('Ctrl Pts',(8.69235312253574,-0.118911987067678,
11.639450573174));
#27472=CARTESIAN_POINT('Ctrl Pts',(6.75367403020043,-3.5612045474153,11.832357815126));
#27473=CARTESIAN_POINT('Ctrl Pts',(2.81906696746642,-3.90831067523958,12.0252650570779));
#27474=CARTESIAN_POINT('Ctrl Pts',(0.307110922541194,-0.860284135845062,
12.2181722990298));
#27475=CARTESIAN_POINT('Ctrl Pts',(1.40025824630285,2.93546602457946,12.4110795409818));
#27476=CARTESIAN_POINT('Ctrl Pts',(5.14875613743306,4.18063685259307,12.6039867829337));
#27477=CARTESIAN_POINT('Ctrl Pts',(8.29576784175946,1.79359080862017,12.7968940248856));
#27478=CARTESIAN_POINT('Ctrl Pts',(8.10705959255911,-2.15182753187632,12.9898012668376));
#27479=CARTESIAN_POINT('Ctrl Pts',(4.74658596274637,-4.22764251916004,13.1827085087895));
#27480=CARTESIAN_POINT('Ctrl Pts',(1.13404899352509,-2.63033801761223,13.3756157507414));
#27481=CARTESIAN_POINT('Ctrl Pts',(0.408149551017793,1.25230269995729,13.5685229926933));
#27482=CARTESIAN_POINT('Ctrl Pts',(3.19957756888897,4.0468972257168,13.7614302346453));
#27483=CARTESIAN_POINT('Ctrl Pts',(7.0830354697174,3.32539895326659,13.9543374765972));
#27484=CARTESIAN_POINT('Ctrl Pts',(8.68444329201153,-0.285318962161525,
14.1472447185491));
#27485=CARTESIAN_POINT('Ctrl Pts',(6.61242391906804,-3.64815591970037,14.3401519605011));
#27486=CARTESIAN_POINT('Ctrl Pts',(2.6672545636313,-3.84131450774899,14.533059202453));
#27487=CARTESIAN_POINT('Ctrl Pts',(0.276577273548778,-0.697058009715255,
14.7259664444049));
#27488=CARTESIAN_POINT('Ctrl Pts',(1.51762372521994,3.05294119783193,14.9188736863569));
#27489=CARTESIAN_POINT('Ctrl Pts',(5.31188105587596,4.15021065664908,15.1117809283088));
#27490=CARTESIAN_POINT('Ctrl Pts',(8.36324941938022,1.64207060627412,15.3046881702608));
#27491=CARTESIAN_POINT('Ctrl Pts',(8.01962672650482,-2.29363493899012,15.4975954122127));
#27492=CARTESIAN_POINT('Ctrl Pts',(4.5814676373469,-4.23481690202856,15.6905026541646));
#27493=CARTESIAN_POINT('Ctrl Pts',(1.03220389453143,-2.50008056241803,15.8834098961165));
#27494=CARTESIAN_POINT('Ctrl Pts',(0.463080419021611,1.41390577532233,16.0763171380685));
#27495=CARTESIAN_POINT('Ctrl Pts',(2.38959890832132,3.19233408148256,16.2049219660364));
#27496=CARTESIAN_POINT('Ctrl Pts',(3.51932642962448,3.49523657477221,16.2692243800204));
#27497=CARTESIAN_POINT('Ctrl Pts',(1.53309449274875,-2.50998586639613,10.7323770763249));
#27498=CARTESIAN_POINT('Ctrl Pts',(0.721240745614079,-1.56451163823132,
10.7967211511304));
#27499=CARTESIAN_POINT('Ctrl Pts',(0.0964400818077463,1.1577041818082,10.9253676399199));
#27500=CARTESIAN_POINT('Ctrl Pts',(2.95035593447059,4.25577458637424,11.1183165426935));
#27501=CARTESIAN_POINT('Ctrl Pts',(7.11236574453675,3.64635994391164,11.3112237846454));
#27502=CARTESIAN_POINT('Ctrl Pts',(8.96670875314062,-0.126613844123434,
11.5041310265973));
#27503=CARTESIAN_POINT('Ctrl Pts',(6.90246259549634,-3.79186159929757,11.6970382685493));
#27504=CARTESIAN_POINT('Ctrl Pts',(2.71301342714273,-4.16144957984,11.8899455105012));
#27505=CARTESIAN_POINT('Ctrl Pts',(0.0383595174737219,-0.91600421592278,
12.0828527524531));
#27506=CARTESIAN_POINT('Ctrl Pts',(1.20230932831938,3.12559437303996,12.2757599944051));
#27507=CARTESIAN_POINT('Ctrl Pts',(5.19359514725411,4.45141415801615,12.468667236357));
#27508=CARTESIAN_POINT('Ctrl Pts',(8.54443688501279,1.9097605940653,12.6615744783089));
#27509=CARTESIAN_POINT('Ctrl Pts',(8.34350611732276,-2.29120009193381,12.8544817202609));
#27510=CARTESIAN_POINT('Ctrl Pts',(4.76537665503522,-4.50146435300819,13.0473889622128));
#27511=CARTESIAN_POINT('Ctrl Pts',(0.91885786420218,-2.8007034107028,13.2402962041647));
#27512=CARTESIAN_POINT('Ctrl Pts',(0.145942356444369,1.3334135839266,13.4332034461166));
#27513=CARTESIAN_POINT('Ctrl Pts',(3.11816946871495,4.30901229687492,13.6261106880686));
#27514=CARTESIAN_POINT('Ctrl Pts',(7.25315657506574,3.54078302028111,13.8190179300205));
#27515=CARTESIAN_POINT('Ctrl Pts',(8.95828660770572,-0.303798897751314,
14.0119251719725));
#27516=CARTESIAN_POINT('Ctrl Pts',(6.75206380060314,-3.88444475906391,14.2048324139244));
#27517=CARTESIAN_POINT('Ctrl Pts',(2.5513682262746,-4.09011411134184,14.3977396558763));
#27518=CARTESIAN_POINT('Ctrl Pts',(0.00584822261288385,-0.742206032911097,
14.5906468978282));
#27519=CARTESIAN_POINT('Ctrl Pts',(1.32727649790022,3.25067834179152,14.7835541397802));
#27520=CARTESIAN_POINT('Ctrl Pts',(5.36728556741858,4.4190172758723,14.9764613817321));
#27521=CARTESIAN_POINT('Ctrl Pts',(8.61628920335996,1.74842652039892,15.1693686236841));
#27522=CARTESIAN_POINT('Ctrl Pts',(8.2504102777287,-2.44219227853008,15.3622758656359));
#27523=CARTESIAN_POINT('Ctrl Pts',(4.58956371615841,-4.50910341629017,15.5551831075879));
#27524=CARTESIAN_POINT('Ctrl Pts',(0.810416320109747,-2.66200925938492,
15.7480903495398));
#27525=CARTESIAN_POINT('Ctrl Pts',(0.204431063348593,1.50548359216295,15.9409975914918));
#27526=CARTESIAN_POINT('Ctrl Pts',(2.25572898309721,3.39909961770891,16.0696024194597));
#27527=CARTESIAN_POINT('Ctrl Pts',(3.45862826862358,3.72162092120162,16.1339048334437));
#27528=CARTESIAN_POINT('Ctrl Pts',(1.35526707151184,-2.66266705610948,10.5970575297482));
#27529=CARTESIAN_POINT('Ctrl Pts',(0.494028665425391,-1.65968010170499,
10.6614016045537));
#27530=CARTESIAN_POINT('Ctrl Pts',(-0.168778311468517,1.22812675038958,
10.7900480933432));
#27531=CARTESIAN_POINT('Ctrl Pts',(2.85873982061751,4.514651234127,10.9829969961168));
#27532=CARTESIAN_POINT('Ctrl Pts',(7.27392261380964,3.86816620258945,11.1759042380687));
#27533=CARTESIAN_POINT('Ctrl Pts',(9.24106438374548,-0.134315701179191,
11.3688114800206));
#27534=CARTESIAN_POINT('Ctrl Pts',(7.05125116079224,-4.02251865117984,11.5617187219726));
#27535=CARTESIAN_POINT('Ctrl Pts',(2.60695988681904,-4.41458848444044,11.7546259639245));
#27536=CARTESIAN_POINT('Ctrl Pts',(-0.23039188759375,-0.971724296000493,
11.9475332058764));
#27537=CARTESIAN_POINT('Ctrl Pts',(1.00436041033591,3.31572272150045,12.1404404478284));
#27538=CARTESIAN_POINT('Ctrl Pts',(5.23843415707517,4.72219146343922,12.3333476897803));
#27539=CARTESIAN_POINT('Ctrl Pts',(8.79310592826617,2.02593037951044,12.5262549317322));
#27540=CARTESIAN_POINT('Ctrl Pts',(8.57995264208641,-2.43057265199133,12.7191621736841));
#27541=CARTESIAN_POINT('Ctrl Pts',(4.78416734732407,-4.77528618685632,12.9120694156361));
#27542=CARTESIAN_POINT('Ctrl Pts',(0.703666734879273,-2.97106880379335,
13.104976657588));
#27543=CARTESIAN_POINT('Ctrl Pts',(-0.11626483812906,1.41452446789591,13.29788389954));
#27544=CARTESIAN_POINT('Ctrl Pts',(3.03676136854093,4.57112736803304,13.4907911414919));
#27545=CARTESIAN_POINT('Ctrl Pts',(7.42327768041408,3.75616708729562,13.6836983834438));
#27546=CARTESIAN_POINT('Ctrl Pts',(9.23212992339991,-0.3222788333411,13.8766056253958));
#27547=CARTESIAN_POINT('Ctrl Pts',(6.89170368213823,-4.12073359842746,14.0695128673477));
#27548=CARTESIAN_POINT('Ctrl Pts',(2.4354818889179,-4.3389137149347,14.2624201092996));
#27549=CARTESIAN_POINT('Ctrl Pts',(-0.264880828323011,-0.787354056106939,
14.4553273512515));
#27550=CARTESIAN_POINT('Ctrl Pts',(1.1369292705805,3.44841548575112,14.6482345932035));
#27551=CARTESIAN_POINT('Ctrl Pts',(5.4226900789612,4.68782389509552,14.8411418351554));
#27552=CARTESIAN_POINT('Ctrl Pts',(8.8693289873397,1.85478243452371,15.0340490771074));
#27553=CARTESIAN_POINT('Ctrl Pts',(8.48119382895259,-2.59074961807004,15.2269563190593));
#27554=CARTESIAN_POINT('Ctrl Pts',(4.59765979496991,-4.78338993055177,15.4198635610112));
#27555=CARTESIAN_POINT('Ctrl Pts',(0.588628745688067,-2.8239379563518,15.6127708029631));
#27556=CARTESIAN_POINT('Ctrl Pts',(-0.0542182923244291,1.59706140900356,
15.8056780449151));
#27557=CARTESIAN_POINT('Ctrl Pts',(2.12185905787311,3.60586515393528,15.934282872883));
#27558=CARTESIAN_POINT('Ctrl Pts',(3.39793010762267,3.94800526763103,15.998585286867));
#27559=CARTESIAN_POINT('',(1.88073622819142,-2.20722158127997,16.0013706388591));
#27560=CARTESIAN_POINT('Ctrl Pts',(3.39856468324527,3.94563850749837,16.));
#27561=CARTESIAN_POINT('Ctrl Pts',(3.28202030975535,3.90360924880686,16.));
#27562=CARTESIAN_POINT('Ctrl Pts',(3.16786744659433,3.85598433920628,16.));
#27563=CARTESIAN_POINT('Ctrl Pts',(3.05633992967595,3.80312375344169,16.));
#27564=CARTESIAN_POINT('Ctrl Pts',(2.94320845217846,3.74950294008397,16.));
#27565=CARTESIAN_POINT('Ctrl Pts',(2.83277776842474,3.69049416048462,16.));
#27566=CARTESIAN_POINT('Ctrl Pts',(2.72531960853723,3.62642595238742,16.));
#27567=CARTESIAN_POINT('Ctrl Pts',(2.61747630627299,3.56212811648006,16.));
#27568=CARTESIAN_POINT('Ctrl Pts',(2.51262629745618,3.49273382302628,16.));
#27569=CARTESIAN_POINT('Ctrl Pts',(2.41108080109129,3.41853797691784,16.));
#27570=CARTESIAN_POINT('Ctrl Pts',(2.31970398669266,3.35177204143373,16.));
#27571=CARTESIAN_POINT('Ctrl Pts',(2.23100318802705,3.28111721609057,16.));
#27572=CARTESIAN_POINT('Ctrl Pts',(2.14523612212338,3.2067697882004,16.));
#27573=CARTESIAN_POINT('Ctrl Pts',(2.12553341153843,3.18969043683141,16.));
#27574=CARTESIAN_POINT('Ctrl Pts',(2.10598565701931,3.17241615849946,16.));
#27575=CARTESIAN_POINT('Ctrl Pts',(2.08659623083789,3.15494923869773,16.));
#27576=CARTESIAN_POINT('Ctrl Pts',(2.07346743197746,3.14312219056115,16.));
#27577=CARTESIAN_POINT('Ctrl Pts',(2.06041075551566,3.13120630250859,16.));
#27578=CARTESIAN_POINT('Ctrl Pts',(2.04743902034581,3.11921338474378,16.));
#27579=CARTESIAN_POINT('Ctrl Pts',(1.95695137795596,3.03555373245333,16.));
#27580=CARTESIAN_POINT('Ctrl Pts',(1.87045372604639,2.94802365738912,16.));
#27581=CARTESIAN_POINT('Ctrl Pts',(1.78820622702511,2.85693355462572,16.));
#27582=CARTESIAN_POINT('Ctrl Pts',(1.70636656276958,2.7662951338121,16.));
#27583=CARTESIAN_POINT('Ctrl Pts',(1.62873453532577,2.67213117469647,16.));
#27584=CARTESIAN_POINT('Ctrl Pts',(1.55560880797602,2.57471863739693,16.));
#27585=CARTESIAN_POINT('Ctrl Pts',(1.48414674748959,2.47952231067405,16.));
#27586=CARTESIAN_POINT('Ctrl Pts',(1.41698799538791,2.38122284820218,16.));
#27587=CARTESIAN_POINT('Ctrl Pts',(1.35445714150433,2.2800616594694,16.));
#27588=CARTESIAN_POINT('Ctrl Pts',(1.30322496354497,2.19717924699847,16.));
#27589=CARTESIAN_POINT('Ctrl Pts',(1.25510007876846,2.11237539198043,16.));
#27590=CARTESIAN_POINT('Ctrl Pts',(1.21028684180597,2.02577869828326,16.));
#27591=CARTESIAN_POINT('Ctrl Pts',(1.19940037733246,2.00474179282054,16.));
#27592=CARTESIAN_POINT('Ctrl Pts',(1.18870946405183,1.98359907557885,16.));
#27593=CARTESIAN_POINT('Ctrl Pts',(1.17821725735083,1.96235238134681,16.));
#27594=CARTESIAN_POINT('Ctrl Pts',(1.17068532266993,1.94710023108889,16.));
#27595=CARTESIAN_POINT('Ctrl Pts',(1.16325564947536,1.93179406050165,16.));
#27596=CARTESIAN_POINT('Ctrl Pts',(1.1559358887606,1.91644852551603,16.));
#27597=CARTESIAN_POINT('Ctrl Pts',(1.10479654173714,1.80923728330855,16.));
#27598=CARTESIAN_POINT('Ctrl Pts',(1.05893622144905,1.69994266655825,16.));
#27599=CARTESIAN_POINT('Ctrl Pts',(1.01863595797368,1.58882409063619,16.));
#27600=CARTESIAN_POINT('Ctrl Pts',(0.978335694498304,1.47770551471412,16.));
#27601=CARTESIAN_POINT('Ctrl Pts',(0.943595041491022,1.36476231430696,16.));
#27602=CARTESIAN_POINT('Ctrl Pts',(0.914749671847378,1.25024175865813,16.));
#27603=CARTESIAN_POINT('Ctrl Pts',(0.885779102083194,1.1352241392674,16.));
#27604=CARTESIAN_POINT('Ctrl Pts',(0.86275565775235,1.01861437498697,16.));
#27605=CARTESIAN_POINT('Ctrl Pts',(0.845598658915959,0.90085030095086,16.));
#27606=CARTESIAN_POINT('Ctrl Pts',(0.831120401325252,0.801472862327414,
16.));
#27607=CARTESIAN_POINT('Ctrl Pts',(0.820820742045749,0.70127314279097,16.));
#27608=CARTESIAN_POINT('Ctrl Pts',(0.814678949007698,0.60052222210086,16.));
#27609=CARTESIAN_POINT('Ctrl Pts',(0.813612852730977,0.583033814276209,
16.));
#27610=CARTESIAN_POINT('Ctrl Pts',(0.812672011048267,0.565527040601622,
16.));
#27611=CARTESIAN_POINT('Ctrl Pts',(0.811856646346995,0.548008964376364,
16.));
#27612=CARTESIAN_POINT('Ctrl Pts',(0.806452329785345,0.431897450933631,
16.));
#27613=CARTESIAN_POINT('Ctrl Pts',(0.806572191820612,0.315663183512141,
16.));
#27614=CARTESIAN_POINT('Ctrl Pts',(0.812080775670422,0.199712141557808,
16.));
#27615=CARTESIAN_POINT('Ctrl Pts',(0.817610950513495,0.0833066274135428,
16.));
#27616=CARTESIAN_POINT('Ctrl Pts',(0.828572461873298,-0.0328143597299322,
16.));
#27617=CARTESIAN_POINT('Ctrl Pts',(0.844880372876002,-0.148231554630927,
16.));
#27618=CARTESIAN_POINT('Ctrl Pts',(0.860929151250057,-0.261814770851201,
16.));
#27619=CARTESIAN_POINT('Ctrl Pts',(0.882156183196351,-0.374717177214322,
16.));
#27620=CARTESIAN_POINT('Ctrl Pts',(0.908525430112972,-0.48651830323896,
16.));
#27621=CARTESIAN_POINT('Ctrl Pts',(0.934174610638338,-0.595266470124897,
16.));
#27622=CARTESIAN_POINT('Ctrl Pts',(0.964689424390745,-0.702973283207877,
16.));
#27623=CARTESIAN_POINT('Ctrl Pts',(1.00007335372366,-0.809221818042884,
16.));
#27624=CARTESIAN_POINT('Ctrl Pts',(1.00618513661092,-0.827573877558135,
16.));
#27625=CARTESIAN_POINT('Ctrl Pts',(1.01244299210376,-0.845884215742526,
16.));
#27626=CARTESIAN_POINT('Ctrl Pts',(1.01884102638095,-0.864133973362507,
16.));
#27627=CARTESIAN_POINT('Ctrl Pts',(1.05633935617679,-0.971094236511956,
16.));
#27628=CARTESIAN_POINT('Ctrl Pts',(1.09868814478405,-1.07609606771823,16.));
#27629=CARTESIAN_POINT('Ctrl Pts',(1.14583717685756,-1.17872972024771,16.));
#27630=CARTESIAN_POINT('Ctrl Pts',(1.19194649734206,-1.27910013653954,16.));
#27631=CARTESIAN_POINT('Ctrl Pts',(1.24264710795939,-1.37720628510166,16.));
#27632=CARTESIAN_POINT('Ctrl Pts',(1.29792934727226,-1.47263173604749,16.));
#27633=CARTESIAN_POINT('Ctrl Pts',(1.30556674318026,-1.48581502886686,16.));
#27634=CARTESIAN_POINT('Ctrl Pts',(1.31329163876066,-1.49894709614249,16.));
#27635=CARTESIAN_POINT('Ctrl Pts',(1.32110405940516,-1.51202677853915,16.));
#27636=CARTESIAN_POINT('Ctrl Pts',(1.33325253512357,-1.53236595524647,16.));
#27637=CARTESIAN_POINT('Ctrl Pts',(1.34561265097563,-1.55257846553154,16.));
#27638=CARTESIAN_POINT('Ctrl Pts',(1.35818455886885,-1.57265987081225,16.));
#27639=CARTESIAN_POINT('Ctrl Pts',(1.37208187483147,-1.59485838169298,16.));
#27640=CARTESIAN_POINT('Ctrl Pts',(1.38623418537527,-1.61689039162208,16.));
#27641=CARTESIAN_POINT('Ctrl Pts',(1.40063305058271,-1.63873806372697,16.));
#27642=CARTESIAN_POINT('Ctrl Pts',(1.45988719596097,-1.72864550576699,16.));
#27643=CARTESIAN_POINT('Ctrl Pts',(1.52335388710929,-1.81549818378269,16.));
#27644=CARTESIAN_POINT('Ctrl Pts',(1.5910140471,-1.89891001383453,16.));
#27645=CARTESIAN_POINT('Ctrl Pts',(1.62378066270062,-1.93930488390621,16.));
#27646=CARTESIAN_POINT('Ctrl Pts',(1.65753128028433,-1.97889221644688,16.));
#27647=CARTESIAN_POINT('Ctrl Pts',(1.69226646643322,-2.01762466210545,16.));
#27648=CARTESIAN_POINT('Ctrl Pts',(1.75164790813293,-2.08383960777761,16.));
#27649=CARTESIAN_POINT('Ctrl Pts',(1.81390655502903,-2.14755714347611,16.));
#27650=CARTESIAN_POINT('Ctrl Pts',(1.87883962139859,-2.20868246298984,16.));
#27651=CARTESIAN_POINT('Ctrl Pts',(1.8825077481285,-2.20570351352142,16.0013706388591));
#27652=CARTESIAN_POINT('Ctrl Pts',(1.89196505514197,-2.21673978501259,16.0009137592394));
#27653=CARTESIAN_POINT('Ctrl Pts',(1.90149334280166,-2.22771523108277,16.0004568796197));
#27654=CARTESIAN_POINT('Ctrl Pts',(1.91109182286969,-2.23862894377632,16.));
#27655=CARTESIAN_POINT('Ctrl Pts',(1.88323467920355,-2.20655152809223,11.));
#27656=CARTESIAN_POINT('Ctrl Pts',(1.8055137100667,-2.1325841428619,11.));
#27657=CARTESIAN_POINT('Ctrl Pts',(1.73182315237859,-2.05488482981754,11.));
#27658=CARTESIAN_POINT('Ctrl Pts',(1.66216469772015,-1.97388508600905,11.));
#27659=CARTESIAN_POINT('Ctrl Pts',(1.59146480714577,-1.89167434717063,11.));
#27660=CARTESIAN_POINT('Ctrl Pts',(1.52491811166235,-1.80606324837128,11.));
#27661=CARTESIAN_POINT('Ctrl Pts',(1.46255293502529,-1.71745376975123,11.));
#27662=CARTESIAN_POINT('Ctrl Pts',(1.39865578991978,-1.62666764489089,11.));
#27663=CARTESIAN_POINT('Ctrl Pts',(1.33914763251816,-1.5327334914365,11.));
#27664=CARTESIAN_POINT('Ctrl Pts',(1.28409326921549,-1.43604026288558,11.));
#27665=CARTESIAN_POINT('Ctrl Pts',(1.23405340579292,-1.34815411435317,11.));
#27666=CARTESIAN_POINT('Ctrl Pts',(1.18769316738891,-1.25798767430718,11.));
#27667=CARTESIAN_POINT('Ctrl Pts',(1.14508996980559,-1.16580920606479,11.));
#27668=CARTESIAN_POINT('Ctrl Pts',(1.13772430980523,-1.1498724854677,11.));
#27669=CARTESIAN_POINT('Ctrl Pts',(1.13047102256546,-1.13387557920784,11.));
#27670=CARTESIAN_POINT('Ctrl Pts',(1.12333059959275,-1.11781982161107,11.));
#27671=CARTESIAN_POINT('Ctrl Pts',(1.1093173856833,-1.0863100964111,11.));
#27672=CARTESIAN_POINT('Ctrl Pts',(1.09575724481632,-1.05461492748262,11.));
#27673=CARTESIAN_POINT('Ctrl Pts',(1.08265349496083,-1.02275315280833,11.));
#27674=CARTESIAN_POINT('Ctrl Pts',(1.03921335903622,-0.917128439431273,
11.));
#27675=CARTESIAN_POINT('Ctrl Pts',(1.00077582995783,-0.809652557756684,
11.));
#27676=CARTESIAN_POINT('Ctrl Pts',(0.967380509038817,-0.700750791635124,
11.));
#27677=CARTESIAN_POINT('Ctrl Pts',(0.933548627493637,-0.590425406218982,
11.));
#27678=CARTESIAN_POINT('Ctrl Pts',(0.90489119584359,-0.478635880663496,
11.));
#27679=CARTESIAN_POINT('Ctrl Pts',(0.881490105760335,-0.36578973307862,
11.));
#27680=CARTESIAN_POINT('Ctrl Pts',(0.858871819872059,-0.256718471082503,
11.));
#27681=CARTESIAN_POINT('Ctrl Pts',(0.841163991177834,-0.14665923747458,
11.));
#27682=CARTESIAN_POINT('Ctrl Pts',(0.828481862514581,-0.0359599154309225,
11.));
#27683=CARTESIAN_POINT('Ctrl Pts',(0.818670645382047,0.0496798942440594,
11.));
#27684=CARTESIAN_POINT('Ctrl Pts',(0.811868056471992,0.135703290008098,
11.));
#27685=CARTESIAN_POINT('Ctrl Pts',(0.808146029432485,0.22195316305556,11.));
#27686=CARTESIAN_POINT('Ctrl Pts',(0.807335597792087,0.240733151850913,
11.));
#27687=CARTESIAN_POINT('Ctrl Pts',(0.806671594065359,0.259518119692736,
11.));
#27688=CARTESIAN_POINT('Ctrl Pts',(0.806154744915036,0.278294214256977,
11.));
#27689=CARTESIAN_POINT('Ctrl Pts',(0.804681400009178,0.33181788409534,11.));
#27690=CARTESIAN_POINT('Ctrl Pts',(0.804402399157995,0.385298168137166,
11.));
#27691=CARTESIAN_POINT('Ctrl Pts',(0.805323214301196,0.43869557367965,11.));
#27692=CARTESIAN_POINT('Ctrl Pts',(0.807360297208648,0.556824541188471,
11.));
#27693=CARTESIAN_POINT('Ctrl Pts',(0.815266164429257,0.674546218612187,
11.));
#27694=CARTESIAN_POINT('Ctrl Pts',(0.829134191190566,0.79144570807364,11.));
#27695=CARTESIAN_POINT('Ctrl Pts',(0.835863260857388,0.84816789516926,11.));
#27696=CARTESIAN_POINT('Ctrl Pts',(0.843996786224402,0.90469679144366,11.));
#27697=CARTESIAN_POINT('Ctrl Pts',(0.853549724724196,0.960986131300249,
11.));
#27698=CARTESIAN_POINT('Ctrl Pts',(0.872837652710683,1.07463752072187,11.));
#27699=CARTESIAN_POINT('Ctrl Pts',(0.897908375714622,1.18731256566191,11.));
#27700=CARTESIAN_POINT('Ctrl Pts',(0.928459425596507,1.2987388881876,11.));
#27701=CARTESIAN_POINT('Ctrl Pts',(0.957176084404771,1.40347478756261,11.));
#27702=CARTESIAN_POINT('Ctrl Pts',(0.9907354529883,1.50710789260008,11.));
#27703=CARTESIAN_POINT('Ctrl Pts',(1.02892793312368,1.60940652439971,11.));
#27704=CARTESIAN_POINT('Ctrl Pts',(1.03665250767009,1.63009681223991,11.));
#27705=CARTESIAN_POINT('Ctrl Pts',(1.0445684264762,1.6507365362987,11.));
#27706=CARTESIAN_POINT('Ctrl Pts',(1.05266336388591,1.67129710445659,11.));
#27707=CARTESIAN_POINT('Ctrl Pts',(1.09577961016135,1.78080931874445,11.));
#27708=CARTESIAN_POINT('Ctrl Pts',(1.14401878611999,1.88821224790122,11.));
#27709=CARTESIAN_POINT('Ctrl Pts',(1.19702431226012,1.99323454026449,11.));
#27710=CARTESIAN_POINT('Ctrl Pts',(1.25115069340324,2.10047763431377,11.));
#27711=CARTESIAN_POINT('Ctrl Pts',(1.31024736452932,2.2052390278035,11.));
#27712=CARTESIAN_POINT('Ctrl Pts',(1.37398970441365,2.30722679719885,11.));
#27713=CARTESIAN_POINT('Ctrl Pts',(1.43857455109351,2.41056257780515,11.));
#27714=CARTESIAN_POINT('Ctrl Pts',(1.50792902729321,2.51105169954105,11.));
#27715=CARTESIAN_POINT('Ctrl Pts',(1.58176693495046,2.60837638822974,11.));
#27716=CARTESIAN_POINT('Ctrl Pts',(1.64789425380196,2.69553786023291,11.));
#27717=CARTESIAN_POINT('Ctrl Pts',(1.71761843767981,2.78016148526227,11.));
#27718=CARTESIAN_POINT('Ctrl Pts',(1.79076460061867,2.86200179764899,11.));
#27719=CARTESIAN_POINT('Ctrl Pts',(1.80462848786612,2.87751354587526,11.));
#27720=CARTESIAN_POINT('Ctrl Pts',(1.81861712160808,2.89292712905613,11.));
#27721=CARTESIAN_POINT('Ctrl Pts',(1.83272383982852,2.9082347498518,11.));
#27722=CARTESIAN_POINT('Ctrl Pts',(1.9176255829498,3.00036416424024,11.));
#27723=CARTESIAN_POINT('Ctrl Pts',(2.00660734119473,3.08844926408247,11.));
#27724=CARTESIAN_POINT('Ctrl Pts',(2.09934472813356,3.17216685573294,11.));
#27725=CARTESIAN_POINT('Ctrl Pts',(2.19205925921466,3.25586381452509,11.));
#27726=CARTESIAN_POINT('Ctrl Pts',(2.28852807468961,3.33519619747782,11.));
#27727=CARTESIAN_POINT('Ctrl Pts',(2.38847157608717,3.40981510006956,11.));
#27728=CARTESIAN_POINT('Ctrl Pts',(2.43485484325298,3.44444535062247,11.));
#27729=CARTESIAN_POINT('Ctrl Pts',(2.48198708286726,3.47805995493347,11.));
#27730=CARTESIAN_POINT('Ctrl Pts',(2.52984313993709,3.5106214115124,11.));
#27731=CARTESIAN_POINT('Ctrl Pts',(2.54582219495995,3.52149362577652,11.));
#27732=CARTESIAN_POINT('Ctrl Pts',(2.56188067251407,3.53224747826245,11.));
#27733=CARTESIAN_POINT('Ctrl Pts',(2.57800967088885,3.54287650131378,11.));
#27734=CARTESIAN_POINT('Ctrl Pts',(2.68352851526793,3.61241350560839,11.));
#27735=CARTESIAN_POINT('Ctrl Pts',(2.79215458366025,3.67667351075176,11.));
#27736=CARTESIAN_POINT('Ctrl Pts',(2.90358985517431,3.73531289711206,11.));
#27737=CARTESIAN_POINT('Ctrl Pts',(2.96812460751363,3.76927232687497,11.));
#27738=CARTESIAN_POINT('Ctrl Pts',(3.0336022952464,3.80134613570095,11.));
#27739=CARTESIAN_POINT('Ctrl Pts',(3.09997070871193,3.83146190442578,11.));
#27740=CARTESIAN_POINT('Ctrl Pts',(3.1966268929033,3.87532125162025,11.));
#27741=CARTESIAN_POINT('Ctrl Pts',(3.29517172468862,3.91502891889752,11.));
#27742=CARTESIAN_POINT('Ctrl Pts',(3.39535148502737,3.95064487077574,11.));
#27743=CARTESIAN_POINT('Ctrl Pts',(5.51501591064331,3.94803438082956,11.0014321153293));
#27744=CARTESIAN_POINT('Ctrl Pts',(6.7910963703372,3.60589174413995,11.0657345293133));
#27745=CARTESIAN_POINT('Ctrl Pts',(8.9671832501964,1.59703309973906,11.1943393572812));
#27746=CARTESIAN_POINT('Ctrl Pts',(8.324343605749,-2.82394025518247,11.3872465992332));
#27747=CARTESIAN_POINT('Ctrl Pts',(4.31527680253589,-4.78343972057373,11.5801538411851));
#27748=CARTESIAN_POINT('Ctrl Pts',(0.431711818820576,-2.59076364645739,
11.773061083137));
#27749=CARTESIAN_POINT('Ctrl Pts',(0.0435744797231438,1.85479343530947,
11.9659683250889));
#27750=CARTESIAN_POINT('Ctrl Pts',(3.49023997463891,4.68786353054347,12.1588755670409));
#27751=CARTESIAN_POINT('Ctrl Pts',(7.77603578183676,3.44844184087651,12.3517828089928));
#27752=CARTESIAN_POINT('Ctrl Pts',(9.1778565836221,-0.787359679550689,12.5446900509448));
#27753=CARTESIAN_POINT('Ctrl Pts',(6.47747259983249,-4.33894876625295,12.7375972928967));
#27754=CARTESIAN_POINT('Ctrl Pts',(2.0212149918786,-4.1207663374878,12.9305045348486));
#27755=CARTESIAN_POINT('Ctrl Pts',(-0.319229843460022,-0.32228151621117,
13.1234117768006));
#27756=CARTESIAN_POINT('Ctrl Pts',(1.48963679342153,3.75619716622437,13.3163190187525));
#27757=CARTESIAN_POINT('Ctrl Pts',(5.87618820434026,4.57116388545287,13.5092262607044));
#27758=CARTESIAN_POINT('Ctrl Pts',(9.02923959854263,1.41453577360683,13.7021335026564));
#27759=CARTESIAN_POINT('Ctrl Pts',(8.20930147313774,-2.97109252818595,13.8950407446083));
#27760=CARTESIAN_POINT('Ctrl Pts',(4.12876825682516,-4.77532441590242,14.0879479865602));
#27761=CARTESIAN_POINT('Ctrl Pts',(0.332952583473522,-2.43059196910973,
14.2808552285121));
#27762=CARTESIAN_POINT('Ctrl Pts',(0.11979767247544,2.02594636783405,14.4737624704641));
#27763=CARTESIAN_POINT('Ctrl Pts',(3.67449769713561,4.72222958280794,14.666669712416));
#27764=CARTESIAN_POINT('Ctrl Pts',(7.9086056122021,3.31574856115804,14.8595769543679));
#27765=CARTESIAN_POINT('Ctrl Pts',(9.14336713327734,-0.97173089265201,15.0524841963199));
#27766=CARTESIAN_POINT('Ctrl Pts',(6.30599397187691,-4.41462580373721,15.2453914382718));
#27767=CARTESIAN_POINT('Ctrl Pts',(1.8616645866995,-4.02254734934239,15.4382986802237));
#27768=CARTESIAN_POINT('Ctrl Pts',(-0.328160969075848,-0.134322510611719,
15.6312059221757));
#27769=CARTESIAN_POINT('Ctrl Pts',(1.63898615201173,3.8682063840671,15.8241131641276));
#27770=CARTESIAN_POINT('Ctrl Pts',(6.05422526983221,4.51467240789339,16.0170204060795));
#27771=CARTESIAN_POINT('Ctrl Pts',(9.08106892242169,1.22887483102134,16.2099276480315));
#27772=CARTESIAN_POINT('Ctrl Pts',(8.41936777485122,-1.65782202753229,16.3385324759994));
#27773=CARTESIAN_POINT('Ctrl Pts',(7.55936623237133,-2.66073791153538,16.4028348899834));
#27774=CARTESIAN_POINT('Ctrl Pts',(5.45442072271799,3.72203409039186,10.8663421353436));
#27775=CARTESIAN_POINT('Ctrl Pts',(6.6574535524538,3.39947698103161,10.9306445493276));
#27776=CARTESIAN_POINT('Ctrl Pts',(8.70897306044462,1.50561293730781,11.0592493772955));
#27777=CARTESIAN_POINT('Ctrl Pts',(8.10293196746261,-2.66228732709529,11.2521566192475));
#27778=CARTESIAN_POINT('Ctrl Pts',(4.32335917937504,-4.50961769627978,11.4450638611994));
#27779=CARTESIAN_POINT('Ctrl Pts',(0.662104016089638,-2.44245862170941,
11.6379711031513));
#27780=CARTESIAN_POINT('Ctrl Pts',(0.296185113536645,1.74861810484191,11.8308783451033));
#27781=CARTESIAN_POINT('Ctrl Pts',(3.54555055284121,4.41951264571341,12.0237855870552));
#27782=CARTESIAN_POINT('Ctrl Pts',(7.58601133917742,3.25104010056242,12.216692829007));
#27783=CARTESIAN_POINT('Ctrl Pts',(8.90758666238144,-0.742288259422881,
12.4096000709591));
#27784=CARTESIAN_POINT('Ctrl Pts',(6.36178278245141,-4.09057107072706,12.602507312911));
#27785=CARTESIAN_POINT('Ctrl Pts',(2.16061806795178,-3.88487822222208,12.7954145548629));
#27786=CARTESIAN_POINT('Ctrl Pts',(-0.0458509299148173,-0.303832913883873,
12.9883217968149));
#27787=CARTESIAN_POINT('Ctrl Pts',(1.65946939863585,3.54117835721147,13.1812290387668));
#27788=CARTESIAN_POINT('Ctrl Pts',(5.79491816017005,4.30949332585313,13.3741362807187));
#27789=CARTESIAN_POINT('Ctrl Pts',(8.76747707074188,1.33356244236586,13.5670435226706));
#27790=CARTESIAN_POINT('Ctrl Pts',(7.99447527785278,-2.80101605226979,13.7599507646226));
#27791=CARTESIAN_POINT('Ctrl Pts',(4.14752708210266,-4.50196694207479,13.9528580065745));
#27792=CARTESIAN_POINT('Ctrl Pts',(0.568998129654688,-2.29145577170941,
14.1457652485264));
#27793=CARTESIAN_POINT('Ctrl Pts',(0.368045004949992,1.90997360180016,14.3386724904784));
#27794=CARTESIAN_POINT('Ctrl Pts',(3.71926067245942,4.45191145629663,14.5315797324303));
#27795=CARTESIAN_POINT('Ctrl Pts',(7.71099237540476,3.12594268168577,14.7244869743822));
#27796=CARTESIAN_POINT('Ctrl Pts',(8.87507151748671,-0.916105373017984,
14.9173942163342));
#27797=CARTESIAN_POINT('Ctrl Pts',(6.20012023408976,-4.16191607084762,15.1103014582861));
#27798=CARTESIAN_POINT('Ctrl Pts',(2.01020092617208,-3.7922816572134,15.303208700238));
#27799=CARTESIAN_POINT('Ctrl Pts',(-0.0542708044146682,-0.126633386485045,
15.49611594219));
#27800=CARTESIAN_POINT('Ctrl Pts',(1.8002694399805,3.64677574746549,15.6890231841419));
#27801=CARTESIAN_POINT('Ctrl Pts',(5.96276371651375,4.25623563227429,15.8819304260938));
#27802=CARTESIAN_POINT('Ctrl Pts',(8.81633948979692,1.15852942823789,16.0748376680458));
#27803=CARTESIAN_POINT('Ctrl Pts',(8.19251659684855,-1.56292207895646,16.2034424960137));
#27804=CARTESIAN_POINT('Ctrl Pts',(7.38174476708876,-2.50842729749781,16.2677449099977));
#27805=CARTESIAN_POINT('Ctrl Pts',(5.39382553479269,3.49603379995416,10.7312521553578));
#27806=CARTESIAN_POINT('Ctrl Pts',(6.52381073457038,3.19306221792327,10.7955545693418));
#27807=CARTESIAN_POINT('Ctrl Pts',(8.45076287069287,1.41419277487655,10.9241593973097));
#27808=CARTESIAN_POINT('Ctrl Pts',(7.8815203291762,-2.50063439900812,11.1170666392617));
#27809=CARTESIAN_POINT('Ctrl Pts',(4.33144155621419,-4.23579567198583,11.3099738812136));
#27810=CARTESIAN_POINT('Ctrl Pts',(0.892496213358695,-2.29415359696143,
11.5028811231655));
#27811=CARTESIAN_POINT('Ctrl Pts',(0.548795747350148,1.64244277437436,11.6957883651175));
#27812=CARTESIAN_POINT('Ctrl Pts',(3.60086113104353,4.15116176088335,11.8886956070694));
#27813=CARTESIAN_POINT('Ctrl Pts',(7.39598689651807,3.05363836024834,12.0816028490213));
#27814=CARTESIAN_POINT('Ctrl Pts',(8.6373167411408,-0.69721683929508,12.2745100909733));
#27815=CARTESIAN_POINT('Ctrl Pts',(6.24609296507032,-3.84219337520115,12.4674173329252));
#27816=CARTESIAN_POINT('Ctrl Pts',(2.30002114402498,-3.64899010695637,12.6603245748771));
#27817=CARTESIAN_POINT('Ctrl Pts',(0.227527983630383,-0.285384311556572,
12.8532318168291));
#27818=CARTESIAN_POINT('Ctrl Pts',(1.82930200385018,3.32615954819857,13.046139058781));
#27819=CARTESIAN_POINT('Ctrl Pts',(5.71364811599984,4.04782276625339,13.2390463007329));
#27820=CARTESIAN_POINT('Ctrl Pts',(8.50571454294112,1.25258911112488,13.4319535426849));
#27821=CARTESIAN_POINT('Ctrl Pts',(7.77964908256783,-2.63093957635364,13.6248607846368));
#27822=CARTESIAN_POINT('Ctrl Pts',(4.16628590738015,-4.22860946824717,13.8177680265887));
#27823=CARTESIAN_POINT('Ctrl Pts',(0.805043675835859,-2.15231957430909,
14.0106752685406));
#27824=CARTESIAN_POINT('Ctrl Pts',(0.616292337424535,1.79400083576627,14.2035825104926));
#27825=CARTESIAN_POINT('Ctrl Pts',(3.76402364778324,4.18159332978533,14.3964897524445));
#27826=CARTESIAN_POINT('Ctrl Pts',(7.51337913860741,2.93613680221351,14.5893969943964));
#27827=CARTESIAN_POINT('Ctrl Pts',(8.6067759016961,-0.860479853383961,14.7823042363484));
#27828=CARTESIAN_POINT('Ctrl Pts',(6.09424649630261,-3.90920633795803,14.9752114783003));
#27829=CARTESIAN_POINT('Ctrl Pts',(2.15873726564465,-3.56201596508441,15.1681187202522));
#27830=CARTESIAN_POINT('Ctrl Pts',(0.219619360246509,-0.11894426235837,
15.3610259622042));
#27831=CARTESIAN_POINT('Ctrl Pts',(1.96155272794927,3.42534511086389,15.5539332041561));
#27832=CARTESIAN_POINT('Ctrl Pts',(5.87130216319528,3.99779885665519,15.746840446108));
#27833=CARTESIAN_POINT('Ctrl Pts',(8.55161005717215,1.08818402545442,15.93974768806));
#27834=CARTESIAN_POINT('Ctrl Pts',(7.96566541884588,-1.46802213038064,16.0683525160279));
#27835=CARTESIAN_POINT('Ctrl Pts',(7.2041233018062,-2.35611668346024,16.1326549300119));
#27836=CARTESIAN_POINT('Ctrl Pts',(5.33323034686737,3.27003350951646,10.5961621753721));
#27837=CARTESIAN_POINT('Ctrl Pts',(6.39016791668697,2.98664745481493,10.6604645893561));
#27838=CARTESIAN_POINT('Ctrl Pts',(8.1925526809411,1.32277261244528,10.789069417324));
#27839=CARTESIAN_POINT('Ctrl Pts',(7.66010869088979,-2.33898147092094,10.981976659276));
#27840=CARTESIAN_POINT('Ctrl Pts',(4.33952393305334,-3.96197364769188,11.1748839012279));
#27841=CARTESIAN_POINT('Ctrl Pts',(1.12288841062775,-2.14584857221345,11.3677911431798));
#27842=CARTESIAN_POINT('Ctrl Pts',(0.801406381163646,1.53626744390679,11.5606983851318));
#27843=CARTESIAN_POINT('Ctrl Pts',(3.65617170924584,3.88281087605329,11.7536056270837));
#27844=CARTESIAN_POINT('Ctrl Pts',(7.20596245385872,2.85623661993425,11.9465128690356));
#27845=CARTESIAN_POINT('Ctrl Pts',(8.36704681990015,-0.652145419167273,
12.1394201109876));
#27846=CARTESIAN_POINT('Ctrl Pts',(6.13040314768924,-3.59381567967527,12.3323273529395));
#27847=CARTESIAN_POINT('Ctrl Pts',(2.43942422009817,-3.41310199169066,12.5252345948914));
#27848=CARTESIAN_POINT('Ctrl Pts',(0.50090689717559,-0.266935709229276,
12.7181418368434));
#27849=CARTESIAN_POINT('Ctrl Pts',(1.9991346090645,3.11114073918567,12.9110490787953));
#27850=CARTESIAN_POINT('Ctrl Pts',(5.63237807182963,3.78615220665366,13.1039563207472));
#27851=CARTESIAN_POINT('Ctrl Pts',(8.24395201514036,1.17161577988392,13.2968635626992));
#27852=CARTESIAN_POINT('Ctrl Pts',(7.56482288728288,-2.46086310043749,13.4897708046511));
#27853=CARTESIAN_POINT('Ctrl Pts',(4.18504473265764,-3.95525199441954,13.682678046603));
#27854=CARTESIAN_POINT('Ctrl Pts',(1.04108922201703,-2.01318337690878,13.875585288555));
#27855=CARTESIAN_POINT('Ctrl Pts',(0.864539669899084,1.67802806973238,14.0684925305069));
#27856=CARTESIAN_POINT('Ctrl Pts',(3.80878662310705,3.91127520327401,14.2613997724588));
#27857=CARTESIAN_POINT('Ctrl Pts',(7.31576590181006,2.74633092274124,14.4543070144107));
#27858=CARTESIAN_POINT('Ctrl Pts',(8.33848028590547,-0.804854333749936,
14.6472142563627));
#27859=CARTESIAN_POINT('Ctrl Pts',(5.98837275851547,-3.65649660506842,14.8401214983146));
#27860=CARTESIAN_POINT('Ctrl Pts',(2.30727360511723,-3.33175027295542,15.0330287402665));
#27861=CARTESIAN_POINT('Ctrl Pts',(0.493509524907691,-0.111255138231699,
15.2259359822185));
#27862=CARTESIAN_POINT('Ctrl Pts',(2.12283601591804,3.20391447426228,15.4188432241704));
#27863=CARTESIAN_POINT('Ctrl Pts',(5.77984060987681,3.73936208103607,15.6117504661223));
#27864=CARTESIAN_POINT('Ctrl Pts',(8.28688062454738,1.01783862267097,15.8046577080743));
#27865=CARTESIAN_POINT('Ctrl Pts',(7.73881424084322,-1.37312218180482,15.9332625360422));
#27866=CARTESIAN_POINT('Ctrl Pts',(7.02650183652363,-2.20380606942267,15.9975649500262));
#27867=CARTESIAN_POINT('Ctrl Pts',(7.02970353323295,-2.20655152809223,16.));
#27868=CARTESIAN_POINT('Ctrl Pts',(7.10742409212087,-2.13258453329759,16.));
#27869=CARTESIAN_POINT('Ctrl Pts',(7.18111417197279,-2.05488553445653,16.));
#27870=CARTESIAN_POINT('Ctrl Pts',(7.25077210344875,-1.97388604470357,16.));
#27871=CARTESIAN_POINT('Ctrl Pts',(7.32147126694797,-1.89167579171358,16.));
#27872=CARTESIAN_POINT('Ctrl Pts',(7.38801721163101,-1.80606513563107,16.));
#27873=CARTESIAN_POINT('Ctrl Pts',(7.45038163639419,-1.71745606959295,16.));
#27874=CARTESIAN_POINT('Ctrl Pts',(7.51427823638975,-1.62667004743177,16.));
#27875=CARTESIAN_POINT('Ctrl Pts',(7.57378581658663,-1.53273594286479,16.));
#27876=CARTESIAN_POINT('Ctrl Pts',(7.62883959427087,-1.43604272751087,16.));
#27877=CARTESIAN_POINT('Ctrl Pts',(7.67887899544011,-1.34815646798496,16.));
#27878=CARTESIAN_POINT('Ctrl Pts',(7.72523875431879,-1.25798988106563,16.));
#27879=CARTESIAN_POINT('Ctrl Pts',(7.76784147269646,-1.16581124461548,16.));
#27880=CARTESIAN_POINT('Ctrl Pts',(7.77520040295186,-1.14988887668907,16.));
#27881=CARTESIAN_POINT('Ctrl Pts',(7.78244716317746,-1.13390643103832,16.));
#27882=CARTESIAN_POINT('Ctrl Pts',(7.78958126330047,-1.11786523846045,16.));
#27883=CARTESIAN_POINT('Ctrl Pts',(7.80313988594662,-1.08737835529271,16.));
#27884=CARTESIAN_POINT('Ctrl Pts',(7.81627446676007,-1.05671763945313,16.));
#27885=CARTESIAN_POINT('Ctrl Pts',(7.82898177222437,-1.02590068301593,16.));
#27886=CARTESIAN_POINT('Ctrl Pts',(7.87265766117147,-0.91998066945996,16.));
#27887=CARTESIAN_POINT('Ctrl Pts',(7.91129968617478,-0.81219338233902,16.));
#27888=CARTESIAN_POINT('Ctrl Pts',(7.94486820109317,-0.702968480620349,
16.));
#27889=CARTESIAN_POINT('Ctrl Pts',(7.97877903504909,-0.592629744604231,
16.));
#27890=CARTESIAN_POINT('Ctrl Pts',(8.00751278739246,-0.480823171231237,
16.));
#27891=CARTESIAN_POINT('Ctrl Pts',(8.03098780517625,-0.367956851668526,
16.));
#27892=CARTESIAN_POINT('Ctrl Pts',(8.05439261017491,-0.255428110493012,
16.));
#27893=CARTESIAN_POINT('Ctrl Pts',(8.07257044534417,-0.14184511283469,16.));
#27894=CARTESIAN_POINT('Ctrl Pts',(8.08539428970214,-0.0275899139920535,
16.));
#27895=CARTESIAN_POINT('Ctrl Pts',(8.09322391903155,0.0421688752543764,
16.));
#27896=CARTESIAN_POINT('Ctrl Pts',(8.09905679884552,0.112178628330393,16.));
#27897=CARTESIAN_POINT('Ctrl Pts',(8.10285465082102,0.182354458664573,16.));
#27898=CARTESIAN_POINT('Ctrl Pts',(8.10369946176583,0.197964679892289,16.));
#27899=CARTESIAN_POINT('Ctrl Pts',(8.10444354709245,0.213583121772062,16.));
#27900=CARTESIAN_POINT('Ctrl Pts',(8.10508643441639,0.229208853518113,16.));
#27901=CARTESIAN_POINT('Ctrl Pts',(8.10577156413731,0.245861310071144,16.));
#27902=CARTESIAN_POINT('Ctrl Pts',(8.10634136964572,0.262512917881839,16.));
#27903=CARTESIAN_POINT('Ctrl Pts',(8.10679559189551,0.279159317031458,16.));
#27904=CARTESIAN_POINT('Ctrl Pts',(8.11003015880494,0.397700167629527,16.));
#27905=CARTESIAN_POINT('Ctrl Pts',(8.10740937540428,0.516026514847005,16.));
#27906=CARTESIAN_POINT('Ctrl Pts',(8.09886096480419,0.633712628060252,16.));
#27907=CARTESIAN_POINT('Ctrl Pts',(8.09088811444019,0.743474993775358,16.));
#27908=CARTESIAN_POINT('Ctrl Pts',(8.07775879624769,0.852681296150461,16.));
#27909=CARTESIAN_POINT('Ctrl Pts',(8.05937589245818,0.960999918180078,16.));
#27910=CARTESIAN_POINT('Ctrl Pts',(8.04008786670114,1.07465184148869,16.));
#27911=CARTESIAN_POINT('Ctrl Pts',(8.01501711848052,1.18732729300118,16.));
#27912=CARTESIAN_POINT('Ctrl Pts',(7.98446609980978,1.29875391107274,16.));
#27913=CARTESIAN_POINT('Ctrl Pts',(7.95574948852459,1.40349002191967,16.));
#27914=CARTESIAN_POINT('Ctrl Pts',(7.92219022346647,1.50712324170997,16.));
#27915=CARTESIAN_POINT('Ctrl Pts',(7.88399788919389,1.60942190462676,16.));
#27916=CARTESIAN_POINT('Ctrl Pts',(7.87627365071178,1.63011137762757,16.));
#27917=CARTESIAN_POINT('Ctrl Pts',(7.86835808505052,1.65075028704105,16.));
#27918=CARTESIAN_POINT('Ctrl Pts',(7.86026351666319,1.67131004319933,16.));
#27919=CARTESIAN_POINT('Ctrl Pts',(7.81704144668225,1.78109171121952,16.));
#27920=CARTESIAN_POINT('Ctrl Pts',(7.768671274096,1.88875360806527,16.));
#27921=CARTESIAN_POINT('Ctrl Pts',(7.71551213318849,1.99402239348199,16.));
#27922=CARTESIAN_POINT('Ctrl Pts',(7.66139636386624,2.10118554945464,16.));
#27923=CARTESIAN_POINT('Ctrl Pts',(7.60231745646377,2.2058693703916,16.));
#27924=CARTESIAN_POINT('Ctrl Pts',(7.53859928916297,2.30778248722832,16.));
#27925=CARTESIAN_POINT('Ctrl Pts',(7.47388703380901,2.41128558406915,16.));
#27926=CARTESIAN_POINT('Ctrl Pts',(7.40438930838696,2.51193162848434,16.));
#27927=CARTESIAN_POINT('Ctrl Pts',(7.33039364440775,2.60940116917617,16.));
#27928=CARTESIAN_POINT('Ctrl Pts',(7.28117391940481,2.67423502201329,16.));
#27929=CARTESIAN_POINT('Ctrl Pts',(7.22996301121353,2.73766311775236,16.));
#27930=CARTESIAN_POINT('Ctrl Pts',(7.17683430579202,2.79958539364976,16.));
#27931=CARTESIAN_POINT('Ctrl Pts',(7.15825036575696,2.82124524500472,16.));
#27932=CARTESIAN_POINT('Ctrl Pts',(7.13943170136375,2.84272080122415,16.));
#27933=CARTESIAN_POINT('Ctrl Pts',(7.12038121960424,2.8640075976673,16.));
#27934=CARTESIAN_POINT('Ctrl Pts',(7.10831155266906,2.8774941092647,16.));
#27935=CARTESIAN_POINT('Ctrl Pts',(7.09614841307943,2.89090530562956,16.));
#27936=CARTESIAN_POINT('Ctrl Pts',(7.08389379300337,2.90423864090636,16.));
#27937=CARTESIAN_POINT('Ctrl Pts',(6.99912039327998,2.99647423483355,16.));
#27938=CARTESIAN_POINT('Ctrl Pts',(6.91026281916338,3.08467093810845,16.));
#27939=CARTESIAN_POINT('Ctrl Pts',(6.81764603140261,3.16850597662426,16.));
#27940=CARTESIAN_POINT('Ctrl Pts',(6.72503476769201,3.25233601486993,16.));
#27941=CARTESIAN_POINT('Ctrl Pts',(6.6286642334695,3.33180568902751,16.));
#27942=CARTESIAN_POINT('Ctrl Pts',(6.52881466382487,3.40656649734515,16.));
#27943=CARTESIAN_POINT('Ctrl Pts',(6.48102994982806,3.44234455684349,16.));
#27944=CARTESIAN_POINT('Ctrl Pts',(6.43244783477714,3.47704370933109,16.));
#27945=CARTESIAN_POINT('Ctrl Pts',(6.38309593333529,3.51062285916835,16.));
#27946=CARTESIAN_POINT('Ctrl Pts',(6.36711687140756,3.52149505049339,16.));
#27947=CARTESIAN_POINT('Ctrl Pts',(6.35105838482246,3.53224887980621,16.));
#27948=CARTESIAN_POINT('Ctrl Pts',(6.33492937498319,3.54287787969292,16.));
#27949=CARTESIAN_POINT('Ctrl Pts',(6.22941110326806,3.61241430562871,16.));
#27950=CARTESIAN_POINT('Ctrl Pts',(6.12078554312154,3.67667379633101,16.));
#27951=CARTESIAN_POINT('Ctrl Pts',(6.00935069340048,3.73531275389524,16.));
#27952=CARTESIAN_POINT('Ctrl Pts',(5.94481649130472,3.76927177432383,16.));
#27953=CARTESIAN_POINT('Ctrl Pts',(5.87933933376081,3.80134522041433,16.));
#27954=CARTESIAN_POINT('Ctrl Pts',(5.81297142537859,3.83146067830186,16.));
#27955=CARTESIAN_POINT('Ctrl Pts',(5.71640347400647,3.87527986959057,16.));
#27956=CARTESIAN_POINT('Ctrl Pts',(5.61795023769426,3.91495500013133,16.));
#27957=CARTESIAN_POINT('Ctrl Pts',(5.51786475809797,3.95054587342593,16.));
#27958=CARTESIAN_POINT('Ctrl Pts',(5.51437352919122,3.94563850749837,11.));
#27959=CARTESIAN_POINT('Ctrl Pts',(5.62948494275764,3.90412601543845,11.));
#27960=CARTESIAN_POINT('Ctrl Pts',(5.74226321989584,3.85715435981311,11.));
#27961=CARTESIAN_POINT('Ctrl Pts',(5.8524831871461,3.80507072374339,11.));
#27962=CARTESIAN_POINT('Ctrl Pts',(5.96574275745869,3.75155074556939,11.));
#27963=CARTESIAN_POINT('Ctrl Pts',(6.07630162648715,3.69263244652674,11.));
#27964=CARTESIAN_POINT('Ctrl Pts',(6.18388799726991,3.62864544490519,11.));
#27965=CARTESIAN_POINT('Ctrl Pts',(6.29199231516529,3.56435039420182,11.));
#27966=CARTESIAN_POINT('Ctrl Pts',(6.39709603311487,3.49493702502777,11.));
#27967=CARTESIAN_POINT('Ctrl Pts',(6.49888670834379,3.42070219646027,11.));
#27968=CARTESIAN_POINT('Ctrl Pts',(6.59974286575969,3.34714890153508,11.));
#27969=CARTESIAN_POINT('Ctrl Pts',(6.69734700891971,3.26886154066444,11.));
#27970=CARTESIAN_POINT('Ctrl Pts',(6.79135148512373,3.18610284976544,11.));
#27971=CARTESIAN_POINT('Ctrl Pts',(6.80306946864777,3.17578669232714,11.));
#27972=CARTESIAN_POINT('Ctrl Pts',(6.81473145720267,3.16540103189161,11.));
#27973=CARTESIAN_POINT('Ctrl Pts',(6.82633672351556,3.15494635733385,11.));
#27974=CARTESIAN_POINT('Ctrl Pts',(6.83946660504027,3.14311822391392,11.));
#27975=CARTESIAN_POINT('Ctrl Pts',(6.85252435343711,3.13120123394603,11.));
#27976=CARTESIAN_POINT('Ctrl Pts',(6.86549714655421,3.11920720081751,11.));
#27977=CARTESIAN_POINT('Ctrl Pts',(6.95598471534232,3.03554665925432,11.));
#27978=CARTESIAN_POINT('Ctrl Pts',(7.04248228827934,2.94801566268217,11.));
#27979=CARTESIAN_POINT('Ctrl Pts',(7.12472970854843,2.85692463994827,11.));
#27980=CARTESIAN_POINT('Ctrl Pts',(7.20656942414708,2.76628516007472,11.));
#27981=CARTESIAN_POINT('Ctrl Pts',(7.28420148981919,2.67212013219767,11.));
#27982=CARTESIAN_POINT('Ctrl Pts',(7.35732724633003,2.57470655107058,11.));
#27983=CARTESIAN_POINT('Ctrl Pts',(7.42878936891669,2.47950915950476,11.));
#27984=CARTESIAN_POINT('Ctrl Pts',(7.49594817041181,2.38120865303378,11.));
#27985=CARTESIAN_POINT('Ctrl Pts',(7.55847906409492,2.28004647451056,11.));
#27986=CARTESIAN_POINT('Ctrl Pts',(7.60971100281839,2.19716369088204,11.));
#27987=CARTESIAN_POINT('Ctrl Pts',(7.65783567486646,2.11235952148364,11.));
#27988=CARTESIAN_POINT('Ctrl Pts',(7.70264873051723,2.02576258719893,11.));
#27989=CARTESIAN_POINT('Ctrl Pts',(7.71353509918498,2.00472572331116,11.));
#27990=CARTESIAN_POINT('Ctrl Pts',(7.72422592037529,1.98358305300933,11.));
#27991=CARTESIAN_POINT('Ctrl Pts',(7.73471803882108,1.96233641130778,11.));
#27992=CARTESIAN_POINT('Ctrl Pts',(7.74225005556775,1.94708400428115,11.));
#27993=CARTESIAN_POINT('Ctrl Pts',(7.74967980897516,1.93177757747585,11.));
#27994=CARTESIAN_POINT('Ctrl Pts',(7.75699964776382,1.91643178757063,11.));
#27995=CARTESIAN_POINT('Ctrl Pts',(7.808138962757,1.80921997506486,11.));
#27996=CARTESIAN_POINT('Ctrl Pts',(7.85399926743267,1.69992489457679,11.));
#27997=CARTESIAN_POINT('Ctrl Pts',(7.89429953689311,1.5888059933625,11.));
#27998=CARTESIAN_POINT('Ctrl Pts',(7.93459980635355,1.47768709214822,11.));
#27999=CARTESIAN_POINT('Ctrl Pts',(7.96934048693593,1.36474370484422,11.));
#28000=CARTESIAN_POINT('Ctrl Pts',(7.99818591109683,1.25022313396199,11.));
#28001=CARTESIAN_POINT('Ctrl Pts',(8.027156518052,1.13520556899906,11.));
#28002=CARTESIAN_POINT('Ctrl Pts',(8.05018003397215,1.01859603432461,11.));
#28003=CARTESIAN_POINT('Ctrl Pts',(8.0673371330803,0.900832334980842,11.));
#28004=CARTESIAN_POINT('Ctrl Pts',(8.08181548590596,0.801455139663204,11.));
#28005=CARTESIAN_POINT('Ctrl Pts',(8.09211525472638,0.701255765578224,11.));
#28006=CARTESIAN_POINT('Ctrl Pts',(8.09825716826101,0.60050527517124,11.));
#28007=CARTESIAN_POINT('Ctrl Pts',(8.09932328478395,0.583016953020385,11.));
#28008=CARTESIAN_POINT('Ctrl Pts',(8.10026414720376,0.565510267575662,11.));
#28009=CARTESIAN_POINT('Ctrl Pts',(8.1010795331039,0.547992282113394,11.));
#28010=CARTESIAN_POINT('Ctrl Pts',(8.10648399092696,0.431881354074675,11.));
#28011=CARTESIAN_POINT('Ctrl Pts',(8.10636428859241,0.315647778133886,11.));
#28012=CARTESIAN_POINT('Ctrl Pts',(8.10085587731003,0.199697504383908,11.));
#28013=CARTESIAN_POINT('Ctrl Pts',(8.0953258767411,0.0832927831430958,11.));
#28014=CARTESIAN_POINT('Ctrl Pts',(8.08436455465527,-0.0328273338256495,
11.));
#28015=CARTESIAN_POINT('Ctrl Pts',(8.06805684234805,-0.148243610557007,
11.));
#28016=CARTESIAN_POINT('Ctrl Pts',(8.05200822940878,-0.261826136251509,
11.));
#28017=CARTESIAN_POINT('Ctrl Pts',(8.03078135261771,-0.374727803014246,
11.));
#28018=CARTESIAN_POINT('Ctrl Pts',(8.00441224541771,-0.486528165984565,
11.));
#28019=CARTESIAN_POINT('Ctrl Pts',(7.97876322263963,-0.59527549803015,11.));
#28020=CARTESIAN_POINT('Ctrl Pts',(7.94824856031495,-0.702981455818624,
11.));
#28021=CARTESIAN_POINT('Ctrl Pts',(7.91286477097122,-0.809229140047758,
11.));
#28022=CARTESIAN_POINT('Ctrl Pts',(7.90675311367846,-0.827580748120317,
11.));
#28023=CARTESIAN_POINT('Ctrl Pts',(7.90049538834023,-0.845890636222599,
11.));
#28024=CARTESIAN_POINT('Ctrl Pts',(7.89409748850863,-0.864139946124484,
11.));
#28025=CARTESIAN_POINT('Ctrl Pts',(7.85663138122071,-0.971007921665021,
11.));
#28026=CARTESIAN_POINT('Ctrl Pts',(7.81432308576492,-1.07592082129095,11.));
#28027=CARTESIAN_POINT('Ctrl Pts',(7.76722270160403,-1.17846998810213,11.));
#28028=CARTESIAN_POINT('Ctrl Pts',(7.72124936093314,-1.27856530293484,11.));
#28029=CARTESIAN_POINT('Ctrl Pts',(7.6707100968929,-1.3764092536002,11.));
#28030=CARTESIAN_POINT('Ctrl Pts',(7.61561456328355,-1.47158897695947,11.));
#28031=CARTESIAN_POINT('Ctrl Pts',(7.59591034615304,-1.505628794938,11.));
#28032=CARTESIAN_POINT('Ctrl Pts',(7.57562304223414,-1.53932749284057,11.));
#28033=CARTESIAN_POINT('Ctrl Pts',(7.55475205970316,-1.57266491022023,11.));
#28034=CARTESIAN_POINT('Ctrl Pts',(7.54414531802266,-1.58960715881424,11.));
#28035=CARTESIAN_POINT('Ctrl Pts',(7.53338923224129,-1.60645371256413,11.));
#28036=CARTESIAN_POINT('Ctrl Pts',(7.52248968612946,-1.62319323259679,11.));
#28037=CARTESIAN_POINT('Ctrl Pts',(7.46367863799964,-1.71351522474309,11.));
#28038=CARTESIAN_POINT('Ctrl Pts',(7.40064685851406,-1.8007992593941,11.));
#28039=CARTESIAN_POINT('Ctrl Pts',(7.33341540428026,-1.88466061294003,11.));
#28040=CARTESIAN_POINT('Ctrl Pts',(7.29706350713731,-1.93000425949821,11.));
#28041=CARTESIAN_POINT('Ctrl Pts',(7.25948321883399,-1.974346648915,11.));
#28042=CARTESIAN_POINT('Ctrl Pts',(7.22067388828633,-2.01762194562246,11.));
#28043=CARTESIAN_POINT('Ctrl Pts',(7.16129250757508,-2.08383661186161,11.));
#28044=CARTESIAN_POINT('Ctrl Pts',(7.09903390488877,-2.14755395179585,11.));
#28045=CARTESIAN_POINT('Ctrl Pts',(7.03410086753636,-2.20867914885338,11.));
#28046=CARTESIAN_POINT('Origin',(4.45646910621825,4.66293670342566E-15,
11.));
#28047=CARTESIAN_POINT('',(-2.54353089378178,4.0414518843274,11.));
#28048=CARTESIAN_POINT('',(-2.54353089378178,-4.04145188432739,11.));
#28049=CARTESIAN_POINT('',(-2.54353089378178,4.0414518843274,11.));
#28050=CARTESIAN_POINT('',(4.45646910621825,8.0829037686548,11.));
#28051=CARTESIAN_POINT('',(4.45646910621825,8.0829037686548,11.));
#28052=CARTESIAN_POINT('',(11.4564691062183,4.0414518843274,11.));
#28053=CARTESIAN_POINT('',(11.4564691062183,4.0414518843274,11.));
#28054=CARTESIAN_POINT('',(11.4564691062183,-4.04145188432739,11.));
#28055=CARTESIAN_POINT('',(11.4564691062183,-4.04145188432739,11.));
#28056=CARTESIAN_POINT('',(4.45646910621825,-8.08290376865479,11.));
#28057=CARTESIAN_POINT('',(4.45646910621825,-8.08290376865479,11.));
#28058=CARTESIAN_POINT('',(-2.54353089378178,-4.04145188432739,11.));
#28059=CARTESIAN_POINT('Origin',(4.45646910621825,-8.08290376865479,11.));
#28060=CARTESIAN_POINT('',(4.45646910621825,-8.08290376865479,16.));
#28061=CARTESIAN_POINT('',(4.45646910621825,-8.08290376865479,11.));
#28062=CARTESIAN_POINT('',(-2.54353089378178,-4.04145188432739,16.));
#28063=CARTESIAN_POINT('',(-2.54353089378178,-4.04145188432739,16.));
#28064=CARTESIAN_POINT('',(-2.54353089378178,-4.04145188432739,11.));
#28065=CARTESIAN_POINT('Origin',(11.4564691062183,-4.04145188432739,11.));
#28066=CARTESIAN_POINT('',(11.4564691062183,-4.04145188432739,16.));
#28067=CARTESIAN_POINT('',(11.4564691062183,-4.04145188432739,11.));
#28068=CARTESIAN_POINT('',(4.45646910621825,-8.08290376865479,16.));
#28069=CARTESIAN_POINT('Origin',(11.4564691062183,4.0414518843274,11.));
#28070=CARTESIAN_POINT('',(11.4564691062183,4.0414518843274,16.));
#28071=CARTESIAN_POINT('',(11.4564691062183,4.0414518843274,11.));
#28072=CARTESIAN_POINT('',(11.4564691062183,-4.04145188432739,16.));
#28073=CARTESIAN_POINT('Origin',(4.45646910621825,8.0829037686548,11.));
#28074=CARTESIAN_POINT('',(4.45646910621825,8.0829037686548,16.));
#28075=CARTESIAN_POINT('',(4.45646910621825,8.0829037686548,11.));
#28076=CARTESIAN_POINT('',(11.4564691062183,4.0414518843274,16.));
#28077=CARTESIAN_POINT('Origin',(-2.54353089378178,4.0414518843274,11.));
#28078=CARTESIAN_POINT('',(-2.54353089378178,4.0414518843274,16.));
#28079=CARTESIAN_POINT('',(-2.54353089378178,4.0414518843274,11.));
#28080=CARTESIAN_POINT('',(4.45646910621825,8.0829037686548,16.));
#28081=CARTESIAN_POINT('Origin',(-2.54353089378178,-4.04145188432739,11.));
#28082=CARTESIAN_POINT('',(-2.54353089378178,4.0414518843274,16.));
#28083=CARTESIAN_POINT('Origin',(4.45646910621825,5.77315972805081E-15,
16.));
#51537=UNCERTAINTY_MEASURE_WITH_UNIT(LENGTH_MEASURE(0.01),#51554,
'DISTANCE_ACCURACY_VALUE',
'Maximum model space distance between geometric entities at asserted c
onnectivities');
#51543=UNCERTAINTY_MEASURE_WITH_UNIT(LENGTH_MEASURE(0.01),#51554,
'DISTANCE_ACCURACY_VALUE',
'Maximum model space distance between geometric entities at asserted c
onnectivities');
#51547=(
GEOMETRIC_REPRESENTATION_CONTEXT(3)
GLOBAL_UNCERTAINTY_ASSIGNED_CONTEXT((#51537))
GLOBAL_UNIT_ASSIGNED_CONTEXT((#51554,#51556,#51557))
REPRESENTATION_CONTEXT('','3D')
);
#51553=(
GEOMETRIC_REPRESENTATION_CONTEXT(3)
GLOBAL_UNCERTAINTY_ASSIGNED_CONTEXT((#51543))
GLOBAL_UNIT_ASSIGNED_CONTEXT((#51554,#51556,#51557))
REPRESENTATION_CONTEXT('','3D')
);
#51554=(
LENGTH_UNIT()
NAMED_UNIT(*)
SI_UNIT(.MILLI.,.METRE.)
);
#51556=(
NAMED_UNIT(*)
PLANE_ANGLE_UNIT()
SI_UNIT($,.RADIAN.)
);
#51557=(
NAMED_UNIT(*)
SI_UNIT($,.STERADIAN.)
SOLID_ANGLE_UNIT()
);
#51561=SHAPE_DEFINITION_REPRESENTATION(#51570,#51587);
#51570=PRODUCT_DEFINITION_SHAPE('',$,#51597);
#51587=SHAPE_REPRESENTATION('',(#4466),#51547);
#51593=PRODUCT_DEFINITION_CONTEXT('part definition',#51622,'design');
#51597=PRODUCT_DEFINITION('Nut_02','Nut_02',#51606,#51593);
#51606=PRODUCT_DEFINITION_FORMATION('',$,#51627);
#51622=APPLICATION_CONTEXT(
'Core Data for Automotive Mechanical Design Process');
#51623=PRODUCT_CONTEXT('part definition',#51622,'mechanical');
#51627=PRODUCT('Nut_02','Nut_02',$,(#51623));
#51634=PRESENTATION_STYLE_ASSIGNMENT((#51637));
#51637=SURFACE_STYLE_USAGE(.BOTH.,#51640);
#51640=SURFACE_SIDE_STYLE('',(#51643));
#51643=SURFACE_STYLE_FILL_AREA(#51646);
#51646=FILL_AREA_STYLE('Opaque(203,203,203)',(#51649));
#51649=FILL_AREA_STYLE_COLOUR('Opaque(203,203,203)',#51652);
#51652=COLOUR_RGB('Opaque(203,203,203)', 0.09019608, 0.27058824, 0.51372549);
ENDSEC;
END-ISO-10303-21;
